ISO-10303-21;
HEADER;
/* Generated by software containing ST-Developer
 * from STEP Tools, Inc. (www.steptools.com) 
 */

FILE_DESCRIPTION(
/* description */ (''),
/* implementation_level */ '2;1');

FILE_NAME(
/* name */ '07_Spindle_Nut_Roller_Carriage.step',
/* time_stamp */ '2026-11-04T18:53:29-08:00',
/* author */ (''),
/* organization */ (''),
/* preprocessor_version */ 'ST-DEVELOPER v20.2',
/* originating_system */ 'Autodesk Translation Framework v15.17.0.0',
/* authorisation */ '');

FILE_SCHEMA (('AUTOMOTIVE_DESIGN { 1 0 10303 214 3 1 1 }'));
ENDSEC;

DATA;
#10=MECHANICAL_DESIGN_GEOMETRIC_PRESENTATION_REPRESENTATION('',(#1333),#100031);
#115=(
BOUNDED_SURFACE()
B_SPLINE_SURFACE(2,2,((#92994,#92995,#92996),(#92997,#92998,#92999),(#93000,
#93001,#93002)),.UNSPECIFIED.,.F.,.F.,.F.)
B_SPLINE_SURFACE_WITH_KNOTS((3,3),(3,3),(1.57079632679489,3.14159265358979),
(0.249866624394877,1.57079632679493),.UNSPECIFIED.)
GEOMETRIC_REPRESENTATION_ITEM()
RATIONAL_B_SPLINE_SURFACE(((1.,0.789707138049851,1.),(0.707106781186533,
0.558407272466459,0.707106781186533),(1.,0.789707138049851,1.)))
REPRESENTATION_ITEM('')
SURFACE()
);
#116=(
BOUNDED_SURFACE()
B_SPLINE_SURFACE(2,2,((#93105,#93106,#93107),(#93108,#93109,#93110),(#93111,
#93112,#93113)),.UNSPECIFIED.,.F.,.F.,.F.)
B_SPLINE_SURFACE_WITH_KNOTS((3,3),(3,3),(1.57079632679486,3.14159265358979),
(-0.510805552608252,0.510805552608253),.UNSPECIFIED.)
GEOMETRIC_REPRESENTATION_ITEM()
RATIONAL_B_SPLINE_SURFACE(((1.,0.872350972065279,1.),(0.707106781186551,
0.616845287922038,0.707106781186551),(1.,0.872350972065279,1.)))
REPRESENTATION_ITEM('')
SURFACE()
);
#197=SPHERICAL_SURFACE('',#21671,0.6);
#198=SPHERICAL_SURFACE('',#21685,0.6);
#199=SPHERICAL_SURFACE('',#21687,0.6);
#200=SPHERICAL_SURFACE('',#21738,0.6);
#201=SPHERICAL_SURFACE('',#21740,0.6);
#202=SPHERICAL_SURFACE('',#21744,0.6);
#203=SPHERICAL_SURFACE('',#21773,0.6);
#204=SPHERICAL_SURFACE('',#21778,0.6);
#205=SPHERICAL_SURFACE('',#21825,0.6);
#206=SPHERICAL_SURFACE('',#21828,0.6);
#207=SPHERICAL_SURFACE('',#21856,0.6);
#208=SPHERICAL_SURFACE('',#21866,0.6);
#209=SPHERICAL_SURFACE('',#21974,0.6);
#210=SPHERICAL_SURFACE('',#21975,0.6);
#211=SPHERICAL_SURFACE('',#21984,0.6);
#212=SPHERICAL_SURFACE('',#21997,0.6);
#213=SPHERICAL_SURFACE('',#21999,0.6);
#214=SPHERICAL_SURFACE('',#22008,0.6);
#215=SPHERICAL_SURFACE('',#22076,0.6);
#216=SPHERICAL_SURFACE('',#22078,0.6);
#802=CIRCLE('',#21613,10.608);
#803=CIRCLE('',#21614,10.008);
#804=CIRCLE('',#21617,10.608);
#805=CIRCLE('',#21618,10.008);
#806=CIRCLE('',#21621,10.008);
#807=CIRCLE('',#21622,10.608);
#808=CIRCLE('',#21625,10.608);
#809=CIRCLE('',#21626,10.008);
#810=CIRCLE('',#21629,10.608);
#811=CIRCLE('',#21630,10.008);
#812=CIRCLE('',#21633,0.6);
#813=CIRCLE('',#21634,0.6);
#814=CIRCLE('',#21638,0.6);
#815=CIRCLE('',#21640,0.6);
#816=CIRCLE('',#21641,0.6);
#817=CIRCLE('',#21642,8.376);
#818=CIRCLE('',#21643,0.6);
#819=CIRCLE('',#21644,0.6);
#820=CIRCLE('',#21646,0.6);
#821=CIRCLE('',#21649,0.6);
#822=CIRCLE('',#21662,1.25);
#823=CIRCLE('',#21664,1.25);
#824=CIRCLE('',#21665,1.25);
#825=CIRCLE('',#21668,0.599999999999999);
#826=CIRCLE('',#21669,0.600000000000001);
#827=CIRCLE('',#21672,0.599999999999999);
#828=CIRCLE('',#21673,0.600000000000001);
#829=CIRCLE('',#21677,0.599999999999999);
#830=CIRCLE('',#21679,0.600000000000001);
#831=CIRCLE('',#21681,0.600000000000001);
#832=CIRCLE('',#21682,0.600000000000001);
#833=CIRCLE('',#21684,0.600000000000001);
#834=CIRCLE('',#21686,0.599999999999999);
#835=CIRCLE('',#21688,0.599999999999999);
#836=CIRCLE('',#21694,0.600000000000001);
#837=CIRCLE('',#21696,0.6);
#838=CIRCLE('',#21698,0.600000000000001);
#839=CIRCLE('',#21699,0.600000000000001);
#840=CIRCLE('',#21700,8.976);
#841=CIRCLE('',#21702,0.6);
#842=CIRCLE('',#21705,0.6);
#843=CIRCLE('',#21707,10.008);
#844=CIRCLE('',#21708,10.608);
#845=CIRCLE('',#21711,10.608);
#846=CIRCLE('',#21712,10.608);
#847=CIRCLE('',#21713,10.608);
#848=CIRCLE('',#21714,10.608);
#849=CIRCLE('',#21716,4.65);
#850=CIRCLE('',#21718,0.6);
#851=CIRCLE('',#21719,4.05);
#852=CIRCLE('',#21720,4.05);
#853=CIRCLE('',#21723,8.976);
#854=CIRCLE('',#21724,8.976);
#855=CIRCLE('',#21726,1.09801213496934);
#856=CIRCLE('',#21727,0.6);
#857=CIRCLE('',#21728,1.632);
#858=CIRCLE('',#21731,0.6);
#859=CIRCLE('',#21733,0.600000000000001);
#860=CIRCLE('',#21734,0.599999999999999);
#861=CIRCLE('',#21736,0.600000000000001);
#862=CIRCLE('',#21737,0.599999999999999);
#863=CIRCLE('',#21739,0.599999999999999);
#864=CIRCLE('',#21741,0.600000000000003);
#865=CIRCLE('',#21743,0.599999999999998);
#866=CIRCLE('',#21745,0.6);
#867=CIRCLE('',#21755,0.600000000000003);
#868=CIRCLE('',#21757,1.25);
#869=CIRCLE('',#21758,1.25);
#870=CIRCLE('',#21759,1.25);
#871=CIRCLE('',#21760,1.25);
#872=CIRCLE('',#21764,1.5);
#873=CIRCLE('',#21765,1.5);
#874=CIRCLE('',#21766,1.5);
#875=CIRCLE('',#21768,0.600000000000001);
#876=CIRCLE('',#21769,0.599999999999998);
#877=CIRCLE('',#21771,0.600000000000001);
#878=CIRCLE('',#21774,0.599999999999999);
#879=CIRCLE('',#21776,0.600000000000001);
#880=CIRCLE('',#21779,0.599999999999999);
#881=CIRCLE('',#21782,0.6);
#882=CIRCLE('',#21783,1.85);
#883=CIRCLE('',#21784,1.85);
#884=CIRCLE('',#21785,2.1);
#885=CIRCLE('',#21787,1.85);
#886=CIRCLE('',#21788,0.6);
#887=CIRCLE('',#21789,1.25);
#888=CIRCLE('',#21790,1.25);
#889=CIRCLE('',#21791,1.85);
#890=CIRCLE('',#21794,0.599999999999999);
#891=CIRCLE('',#21796,1.25);
#892=CIRCLE('',#21798,2.1);
#893=CIRCLE('',#21799,0.6);
#894=CIRCLE('',#21800,1.5);
#895=CIRCLE('',#21801,1.5);
#896=CIRCLE('',#21803,1.5);
#897=CIRCLE('',#21806,0.6);
#898=CIRCLE('',#21808,0.6);
#899=CIRCLE('',#21810,0.599999999999999);
#900=CIRCLE('',#21813,0.6);
#901=CIRCLE('',#21821,0.599999999999999);
#902=CIRCLE('',#21823,0.600000000000001);
#903=CIRCLE('',#21824,0.599999999999999);
#904=CIRCLE('',#21827,0.600000000000001);
#905=CIRCLE('',#21830,2.57398786503066);
#906=CIRCLE('',#21831,2.57398786503066);
#907=CIRCLE('',#21832,0.6);
#908=CIRCLE('',#21833,1.0896);
#909=CIRCLE('',#21834,1.2528);
#910=CIRCLE('',#21835,1.2528);
#911=CIRCLE('',#21840,1.85);
#912=CIRCLE('',#21841,0.6);
#913=CIRCLE('',#21842,1.85);
#914=CIRCLE('',#21857,0.599999999999999);
#915=CIRCLE('',#21862,0.600000000000001);
#916=CIRCLE('',#21864,0.600000000000001);
#917=CIRCLE('',#21865,0.6);
#918=CIRCLE('',#21873,2.1);
#919=CIRCLE('',#21874,0.6);
#920=CIRCLE('',#21875,1.5);
#921=CIRCLE('',#21877,1.5);
#922=CIRCLE('',#21878,1.5);
#923=CIRCLE('',#21880,1.85);
#924=CIRCLE('',#21881,1.85);
#925=CIRCLE('',#21883,0.6);
#926=CIRCLE('',#21884,1.25);
#927=CIRCLE('',#21886,0.600000000000001);
#928=CIRCLE('',#21889,1.25);
#929=CIRCLE('',#21890,1.25);
#930=CIRCLE('',#21892,2.1);
#931=CIRCLE('',#21898,0.6);
#932=CIRCLE('',#21901,0.6);
#933=CIRCLE('',#21908,0.6);
#934=CIRCLE('',#21914,5.712);
#935=CIRCLE('',#21919,5.712);
#936=CIRCLE('',#21924,5.712);
#937=CIRCLE('',#21929,5.712);
#938=CIRCLE('',#21931,0.6);
#939=CIRCLE('',#21932,0.4896);
#940=CIRCLE('',#21933,0.4896);
#941=CIRCLE('',#21943,0.6);
#942=CIRCLE('',#21944,0.6528);
#943=CIRCLE('',#21945,0.6528);
#944=CIRCLE('',#21947,0.6528);
#945=CIRCLE('',#21949,0.6);
#946=CIRCLE('',#21950,0.6528);
#947=CIRCLE('',#21951,0.6528);
#948=CIRCLE('',#21953,0.6528);
#949=CIRCLE('',#21955,0.4896);
#950=CIRCLE('',#21957,2.04);
#951=CIRCLE('',#21958,0.6);
#952=CIRCLE('',#21960,1.85);
#953=CIRCLE('',#21961,0.6);
#954=CIRCLE('',#21962,1.85);
#955=CIRCLE('',#21964,0.599999999999999);
#956=CIRCLE('',#21966,2.1);
#957=CIRCLE('',#21967,0.6);
#958=CIRCLE('',#21970,0.600000000000001);
#959=CIRCLE('',#21971,0.599999999999999);
#960=CIRCLE('',#21973,0.600000000000001);
#961=CIRCLE('',#21976,0.599999999999999);
#962=CIRCLE('',#21978,0.600000000000001);
#963=CIRCLE('',#21980,0.600000000000001);
#964=CIRCLE('',#21983,0.599999999999999);
#965=CIRCLE('',#21985,0.6);
#966=CIRCLE('',#21987,0.6);
#967=CIRCLE('',#21989,0.6);
#968=CIRCLE('',#21991,0.600000000000001);
#969=CIRCLE('',#21993,0.600000000000001);
#970=CIRCLE('',#21994,0.600000000000001);
#971=CIRCLE('',#21996,0.600000000000001);
#972=CIRCLE('',#21998,0.599999999999999);
#973=CIRCLE('',#22000,0.599999999999999);
#974=CIRCLE('',#22003,0.600000000000001);
#975=CIRCLE('',#22006,0.600000000000001);
#976=CIRCLE('',#22010,1.85);
#977=CIRCLE('',#22011,0.6);
#978=CIRCLE('',#22012,1.25);
#979=CIRCLE('',#22013,1.25);
#980=CIRCLE('',#22015,1.25);
#981=CIRCLE('',#22016,1.25);
#982=CIRCLE('',#22017,1.25);
#983=CIRCLE('',#22018,1.25);
#984=CIRCLE('',#22019,1.25);
#985=CIRCLE('',#22021,0.6);
#986=CIRCLE('',#22022,2.1);
#987=CIRCLE('',#22030,0.600000000000001);
#988=CIRCLE('',#22039,0.599999999999999);
#989=CIRCLE('',#22040,0.6);
#990=CIRCLE('',#22048,1.5);
#991=CIRCLE('',#22049,0.6);
#992=CIRCLE('',#22065,0.600000000000005);
#993=CIRCLE('',#22072,0.600000000000001);
#994=CIRCLE('',#22074,0.600000000000001);
#995=CIRCLE('',#22075,0.600000000000001);
#996=CIRCLE('',#22077,0.600000000000003);
#997=CIRCLE('',#22081,0.6);
#998=CIRCLE('',#22086,0.6);
#999=CIRCLE('',#22088,2.1);
#1000=CIRCLE('',#22093,0.600000000000001);
#1001=CIRCLE('',#22105,0.6);
#1002=CIRCLE('',#22106,1.5);
#1003=CIRCLE('',#22107,1.5);
#1004=CIRCLE('',#22109,1.5);
#1005=CIRCLE('',#22110,1.5);
#1006=CIRCLE('',#22113,2.1);
#1249=TOROIDAL_SURFACE('',#21612,10.008,0.6);
#1250=TOROIDAL_SURFACE('',#21616,10.008,0.6);
#1251=TOROIDAL_SURFACE('',#21620,10.008,0.6);
#1252=TOROIDAL_SURFACE('',#21624,10.008,0.6);
#1253=TOROIDAL_SURFACE('',#21628,10.008,0.6);
#1254=TOROIDAL_SURFACE('',#21697,8.376,0.6);
#1255=TOROIDAL_SURFACE('',#21706,10.008,0.6);
#1256=TOROIDAL_SURFACE('',#21717,4.65,0.6);
#1257=TOROIDAL_SURFACE('',#21725,1.09801213496934,0.6);
#1258=TOROIDAL_SURFACE('',#21786,1.85,0.6);
#1259=TOROIDAL_SURFACE('',#21797,2.1,0.6);
#1260=TOROIDAL_SURFACE('',#21805,2.1,0.6);
#1261=TOROIDAL_SURFACE('',#21807,1.85,0.6);
#1262=TOROIDAL_SURFACE('',#21839,1.85,0.6);
#1263=TOROIDAL_SURFACE('',#21872,2.1,0.6);
#1264=TOROIDAL_SURFACE('',#21882,1.85,0.6);
#1265=TOROIDAL_SURFACE('',#21930,1.0896,0.6);
#1266=TOROIDAL_SURFACE('',#21942,1.2528,0.6);
#1267=TOROIDAL_SURFACE('',#21948,1.2528,0.6);
#1268=TOROIDAL_SURFACE('',#21956,2.57398786503066,0.6);
#1269=TOROIDAL_SURFACE('',#21959,1.85,0.6);
#1270=TOROIDAL_SURFACE('',#21965,2.1,0.6);
#1271=TOROIDAL_SURFACE('',#22009,1.85,0.6);
#1272=TOROIDAL_SURFACE('',#22085,2.1,0.6);
#1273=TOROIDAL_SURFACE('',#22087,2.1,0.6);
#1274=TOROIDAL_SURFACE('',#22104,2.1,0.6);
#1275=TOROIDAL_SURFACE('',#22112,2.1,0.6);
#1297=SHAPE_REPRESENTATION_RELATIONSHIP('SRR','None',#100107,#1315);
#1315=ADVANCED_BREP_SHAPE_REPRESENTATION('',(#1351),#100019);
#1333=STYLED_ITEM('',(#100202),#1351);
#1351=MANIFOLD_SOLID_BREP('Body1',#20123);
#1529=PLANE('',#21615);
#1530=PLANE('',#21619);
#1531=PLANE('',#21627);
#1532=PLANE('',#21631);
#1533=PLANE('',#21635);
#1534=PLANE('',#21639);
#1535=PLANE('',#21658);
#1536=PLANE('',#21659);
#1537=PLANE('',#21661);
#1538=PLANE('',#21663);
#1539=PLANE('',#21666);
#1540=PLANE('',#21689);
#1541=PLANE('',#21692);
#1542=PLANE('',#21695);
#1543=PLANE('',#21704);
#1544=PLANE('',#21715);
#1545=PLANE('',#21729);
#1546=PLANE('',#21752);
#1547=PLANE('',#21781);
#1548=PLANE('',#21804);
#1549=PLANE('',#21814);
#1550=PLANE('',#21816);
#1551=PLANE('',#21819);
#1552=PLANE('',#21829);
#1553=PLANE('',#21845);
#1554=PLANE('',#21848);
#1555=PLANE('',#21851);
#1556=PLANE('',#21855);
#1557=PLANE('',#21869);
#1558=PLANE('',#21879);
#1559=PLANE('',#21891);
#1560=PLANE('',#21894);
#1561=PLANE('',#21899);
#1562=PLANE('',#21903);
#1563=PLANE('',#21906);
#1564=PLANE('',#21909);
#1565=PLANE('',#21913);
#1566=PLANE('',#21918);
#1567=PLANE('',#21923);
#1568=PLANE('',#21928);
#1569=PLANE('',#21935);
#1570=PLANE('',#21937);
#1571=PLANE('',#21939);
#1572=PLANE('',#21941);
#1573=PLANE('',#21968);
#1574=PLANE('',#21986);
#1575=PLANE('',#22001);
#1576=PLANE('',#22020);
#1577=PLANE('',#22024);
#1578=PLANE('',#22028);
#1579=PLANE('',#22029);
#1580=PLANE('',#22031);
#1581=PLANE('',#22045);
#1582=PLANE('',#22046);
#1583=PLANE('',#22047);
#1584=PLANE('',#22060);
#1585=PLANE('',#22061);
#1586=PLANE('',#22066);
#1587=PLANE('',#22084);
#1588=PLANE('',#22089);
#1589=PLANE('',#22090);
#1590=PLANE('',#22091);
#1591=PLANE('',#22092);
#1592=PLANE('',#22095);
#1593=PLANE('',#22098);
#1594=PLANE('',#22100);
#1595=PLANE('',#22102);
#1596=PLANE('',#22103);
#1597=PLANE('',#22111);
#1598=PLANE('',#22114);
#1599=PLANE('',#22115);
#1600=PLANE('',#22116);
#1601=PLANE('',#22117);
#1602=PLANE('',#22118);
#1603=PLANE('',#22119);
#1604=PLANE('',#22120);
#1605=PLANE('',#22121);
#1606=PLANE('',#22122);
#1607=PLANE('',#22123);
#1608=PLANE('',#22124);
#1609=PLANE('',#22125);
#1610=PLANE('',#22126);
#1611=PLANE('',#22127);
#1612=PLANE('',#22128);
#1613=PLANE('',#22129);
#1614=PLANE('',#22130);
#1615=PLANE('',#22131);
#1616=PLANE('',#22132);
#1617=PLANE('',#22133);
#1618=PLANE('',#22134);
#1619=PLANE('',#22135);
#1620=PLANE('',#22136);
#1621=PLANE('',#22137);
#1622=PLANE('',#22138);
#1623=PLANE('',#22139);
#1624=PLANE('',#22142);
#1625=PLANE('',#22143);
#1626=PLANE('',#22144);
#1627=PLANE('',#22145);
#1628=PLANE('',#22146);
#1629=PLANE('',#22147);
#1630=PLANE('',#22148);
#1631=PLANE('',#22149);
#1632=PLANE('',#22150);
#1633=PLANE('',#22151);
#1760=FACE_BOUND('',#7006,.T.);
#1761=FACE_BOUND('',#7011,.T.);
#1762=FACE_BOUND('',#7036,.T.);
#1763=FACE_BOUND('',#7043,.T.);
#1764=FACE_BOUND('',#7059,.T.);
#1765=FACE_BOUND('',#7060,.T.);
#1766=FACE_BOUND('',#7061,.T.);
#1767=FACE_BOUND('',#7062,.T.);
#1768=FACE_BOUND('',#7086,.T.);
#1769=FACE_BOUND('',#7091,.T.);
#1770=FACE_BOUND('',#7130,.T.);
#1771=FACE_BOUND('',#7154,.T.);
#1772=FACE_BOUND('',#7155,.T.);
#1773=FACE_BOUND('',#7226,.T.);
#1901=ELLIPSE('',#21637,0.848528137423856,0.6);
#1902=ELLIPSE('',#21647,0.848528137423857,0.6);
#1903=ELLIPSE('',#21651,1.29110397126991,0.6);
#1904=ELLIPSE('',#21652,2.01675243255473,0.6);
#1905=ELLIPSE('',#21653,1.29110397126991,0.6);
#1906=ELLIPSE('',#21654,2.01675243255473,0.6);
#1907=ELLIPSE('',#21655,1.05620174691084,0.6);
#1908=ELLIPSE('',#21656,1.05620174691084,0.6);
#1909=ELLIPSE('',#21657,0.641695030633084,0.6);
#1910=ELLIPSE('',#21660,0.641695030633085,0.600000000000001);
#1911=ELLIPSE('',#21670,0.628456956755705,0.6);
#1912=ELLIPSE('',#21675,0.677615091396383,0.6);
#1913=ELLIPSE('',#21676,0.677615091396385,0.6);
#1914=ELLIPSE('',#21691,0.848528137423857,0.6);
#1915=ELLIPSE('',#21747,1.29110397126991,0.6);
#1916=ELLIPSE('',#21749,1.2911039712699,0.6);
#1917=ELLIPSE('',#21751,0.641695030633084,0.6);
#1918=ELLIPSE('',#21754,0.848528137423857,0.6);
#1919=ELLIPSE('',#21762,0.72905961291191,0.600000000000001);
#1920=ELLIPSE('',#21772,0.848528137423857,0.6);
#1921=ELLIPSE('',#21777,0.848528137423857,0.6);
#1922=ELLIPSE('',#21793,0.848528137423857,0.6);
#1923=ELLIPSE('',#21811,0.848528137423857,0.6);
#1924=ELLIPSE('',#21818,0.848528137423857,0.6);
#1925=ELLIPSE('',#21837,0.848528137423857,0.6);
#1926=ELLIPSE('',#21844,0.84852813742386,0.6);
#1927=ELLIPSE('',#21847,0.729059612911909,0.6);
#1928=ELLIPSE('',#21850,1.05620174691084,0.6);
#1929=ELLIPSE('',#21853,0.848528137423857,0.6);
#1930=ELLIPSE('',#21854,0.677615091396383,0.6);
#1931=ELLIPSE('',#21859,2.01675243255473,0.6);
#1932=ELLIPSE('',#21868,0.848528137423857,0.6);
#1933=ELLIPSE('',#21871,0.848528137423857,0.6);
#1934=ELLIPSE('',#21887,0.848528137423857,0.6);
#1935=ELLIPSE('',#21896,0.848528137423856,0.6);
#1936=ELLIPSE('',#21902,0.848528137423857,0.6);
#1937=ELLIPSE('',#21905,0.848528137423857,0.6);
#1938=ELLIPSE('',#21911,0.848528137423857,0.6);
#1939=ELLIPSE('',#21912,0.848528137423857,0.6);
#1940=ELLIPSE('',#21916,0.848528137423857,0.6);
#1941=ELLIPSE('',#21917,0.848528137423857,0.6);
#1942=ELLIPSE('',#21921,0.848528137423857,0.6);
#1943=ELLIPSE('',#21922,0.848528137423857,0.6);
#1944=ELLIPSE('',#21926,0.848528137423857,0.6);
#1945=ELLIPSE('',#21927,0.848528137423857,0.6);
#1946=ELLIPSE('',#21981,0.848528137423857,0.6);
#1947=ELLIPSE('',#22007,0.848528137423857,0.6);
#1948=ELLIPSE('',#22026,2.01675243255473,0.6);
#1949=ELLIPSE('',#22027,1.2911039712699,0.6);
#1950=ELLIPSE('',#22033,0.848528137423857,0.6);
#1951=ELLIPSE('',#22034,0.848528137423856,0.6);
#1952=ELLIPSE('',#22035,1.29110397126991,0.6);
#1953=ELLIPSE('',#22036,1.2911039712699,0.6);
#1954=ELLIPSE('',#22038,2.01675243255473,0.6);
#1955=ELLIPSE('',#22041,0.848528137423857,0.6);
#1956=ELLIPSE('',#22042,2.01675243255472,0.6);
#1957=ELLIPSE('',#22043,1.05620174691084,0.6);
#1958=ELLIPSE('',#22044,1.05620174691084,0.6);
#1959=ELLIPSE('',#22051,0.729059612911909,0.6);
#1960=ELLIPSE('',#22052,1.05620174691084,0.6);
#1961=ELLIPSE('',#22053,0.641695030633084,0.6);
#1962=ELLIPSE('',#22055,0.729059612911907,0.6);
#1963=ELLIPSE('',#22056,1.05620174691084,0.6);
#1964=ELLIPSE('',#22057,0.641695030633084,0.6);
#1965=ELLIPSE('',#22059,1.29110397126991,0.6);
#1966=ELLIPSE('',#22062,0.641695030633084,0.6);
#1967=ELLIPSE('',#22063,1.05620174691084,0.6);
#1968=ELLIPSE('',#22067,0.641695030633084,0.6);
#1969=ELLIPSE('',#22068,1.05620174691084,0.6);
#1970=ELLIPSE('',#22069,1.05620174691084,0.6);
#1971=ELLIPSE('',#22080,0.848528137423857,0.6);
#1972=ELLIPSE('',#22082,2.01675243255473,0.6);
#1973=ELLIPSE('',#22096,1.05620174691084,0.6);
#2786=LINE('',#91011,#4073);
#2787=LINE('',#91050,#4074);
#2788=LINE('',#91051,#4075);
#2789=LINE('',#91106,#4076);
#2790=LINE('',#91108,#4077);
#2791=LINE('',#91160,#4078);
#2792=LINE('',#91199,#4079);
#2793=LINE('',#91200,#4080);
#2794=LINE('',#91206,#4081);
#2795=LINE('',#91209,#4082);
#2796=LINE('',#91212,#4083);
#2797=LINE('',#91214,#4084);
#2798=LINE('',#91215,#4085);
#2799=LINE('',#91220,#4086);
#2800=LINE('',#91224,#4087);
#2801=LINE('',#91228,#4088);
#2802=LINE('',#91232,#4089);
#2803=LINE('',#91236,#4090);
#2804=LINE('',#91240,#4091);
#2805=LINE('',#91244,#4092);
#2806=LINE('',#91246,#4093);
#2807=LINE('',#91248,#4094);
#2808=LINE('',#91249,#4095);
#2809=LINE('',#91251,#4096);
#2810=LINE('',#91252,#4097);
#2811=LINE('',#91268,#4098);
#2812=LINE('',#91272,#4099);
#2813=LINE('',#91277,#4100);
#2814=LINE('',#91290,#4101);
#2815=LINE('',#91312,#4102);
#2816=LINE('',#91318,#4103);
#2817=LINE('',#91322,#4104);
#2818=LINE('',#91326,#4105);
#2819=LINE('',#91330,#4106);
#2820=LINE('',#91332,#4107);
#2821=LINE('',#91333,#4108);
#2822=LINE('',#91338,#4109);
#2823=LINE('',#91339,#4110);
#2824=LINE('',#91342,#4111);
#2825=LINE('',#91345,#4112);
#2826=LINE('',#91348,#4113);
#2827=LINE('',#91350,#4114);
#2828=LINE('',#91352,#4115);
#2829=LINE('',#91356,#4116);
#2830=LINE('',#91358,#4117);
#2831=LINE('',#91361,#4118);
#2832=LINE('',#91365,#4119);
#2833=LINE('',#91367,#4120);
#2834=LINE('',#91369,#4121);
#2835=LINE('',#91371,#4122);
#2836=LINE('',#91372,#4123);
#2837=LINE('',#91376,#4124);
#2838=LINE('',#91380,#4125);
#2839=LINE('',#91397,#4126);
#2840=LINE('',#91401,#4127);
#2841=LINE('',#91406,#4128);
#2842=LINE('',#91407,#4129);
#2843=LINE('',#91412,#4130);
#2844=LINE('',#91415,#4131);
#2845=LINE('',#91429,#4132);
#2846=LINE('',#91431,#4133);
#2847=LINE('',#91438,#4134);
#2848=LINE('',#91440,#4135);
#2849=LINE('',#91442,#4136);
#2850=LINE('',#91443,#4137);
#2851=LINE('',#91446,#4138);
#2852=LINE('',#91449,#4139);
#2853=LINE('',#91451,#4140);
#2854=LINE('',#91453,#4141);
#2855=LINE('',#91455,#4142);
#2856=LINE('',#91457,#4143);
#2857=LINE('',#91459,#4144);
#2858=LINE('',#91460,#4145);
#2859=LINE('',#91463,#4146);
#2860=LINE('',#91469,#4147);
#2861=LINE('',#91471,#4148);
#2862=LINE('',#91472,#4149);
#2863=LINE('',#91483,#4150);
#2864=LINE('',#91495,#4151);
#2865=LINE('',#91498,#4152);
#2866=LINE('',#91502,#4153);
#2867=LINE('',#91503,#4154);
#2868=LINE('',#91568,#4155);
#2869=LINE('',#91569,#4156);
#2870=LINE('',#91572,#4157);
#2871=LINE('',#91575,#4158);
#2872=LINE('',#91595,#4159);
#2873=LINE('',#91596,#4160);
#2874=LINE('',#91617,#4161);
#2875=LINE('',#91620,#4162);
#2876=LINE('',#91655,#4163);
#2877=LINE('',#91813,#4164);
#2878=LINE('',#91834,#4165);
#2879=LINE('',#91841,#4166);
#2880=LINE('',#91844,#4167);
#2881=LINE('',#91848,#4168);
#2882=LINE('',#91851,#4169);
#2883=LINE('',#91857,#4170);
#2884=LINE('',#91865,#4171);
#2885=LINE('',#91886,#4172);
#2886=LINE('',#91890,#4173);
#2887=LINE('',#91896,#4174);
#2888=LINE('',#91900,#4175);
#2889=LINE('',#91902,#4176);
#2890=LINE('',#91905,#4177);
#2891=LINE('',#91918,#4178);
#2892=LINE('',#91921,#4179);
#2893=LINE('',#91923,#4180);
#2894=LINE('',#91926,#4181);
#2895=LINE('',#91931,#4182);
#2896=LINE('',#91933,#4183);
#2897=LINE('',#91954,#4184);
#2898=LINE('',#91982,#4185);
#2899=LINE('',#91985,#4186);
#2900=LINE('',#91987,#4187);
#2901=LINE('',#91993,#4188);
#2902=LINE('',#92000,#4189);
#2903=LINE('',#92007,#4190);
#2904=LINE('',#92009,#4191);
#2905=LINE('',#92013,#4192);
#2906=LINE('',#92016,#4193);
#2907=LINE('',#92020,#4194);
#2908=LINE('',#92022,#4195);
#2909=LINE('',#92024,#4196);
#2910=LINE('',#92029,#4197);
#2911=LINE('',#92059,#4198);
#2912=LINE('',#92063,#4199);
#2913=LINE('',#92066,#4200);
#2914=LINE('',#92070,#4201);
#2915=LINE('',#92082,#4202);
#2916=LINE('',#92084,#4203);
#2917=LINE('',#92085,#4204);
#2918=LINE('',#92108,#4205);
#2919=LINE('',#92112,#4206);
#2920=LINE('',#92115,#4207);
#2921=LINE('',#92117,#4208);
#2922=LINE('',#92119,#4209);
#2923=LINE('',#92122,#4210);
#2924=LINE('',#92124,#4211);
#2925=LINE('',#92126,#4212);
#2926=LINE('',#92127,#4213);
#2927=LINE('',#92130,#4214);
#2928=LINE('',#92132,#4215);
#2929=LINE('',#92138,#4216);
#2930=LINE('',#92145,#4217);
#2931=LINE('',#92146,#4218);
#2932=LINE('',#92151,#4219);
#2933=LINE('',#92153,#4220);
#2934=LINE('',#92155,#4221);
#2935=LINE('',#92159,#4222);
#2936=LINE('',#92161,#4223);
#2937=LINE('',#92163,#4224);
#2938=LINE('',#92165,#4225);
#2939=LINE('',#92167,#4226);
#2940=LINE('',#92169,#4227);
#2941=LINE('',#92171,#4228);
#2942=LINE('',#92172,#4229);
#2943=LINE('',#92174,#4230);
#2944=LINE('',#92176,#4231);
#2945=LINE('',#92177,#4232);
#2946=LINE('',#92179,#4233);
#2947=LINE('',#92180,#4234);
#2948=LINE('',#92183,#4235);
#2949=LINE('',#92185,#4236);
#2950=LINE('',#92187,#4237);
#2951=LINE('',#92188,#4238);
#2952=LINE('',#92191,#4239);
#2953=LINE('',#92193,#4240);
#2954=LINE('',#92197,#4241);
#2955=LINE('',#92199,#4242);
#2956=LINE('',#92200,#4243);
#2957=LINE('',#92208,#4244);
#2958=LINE('',#92210,#4245);
#2959=LINE('',#92235,#4246);
#2960=LINE('',#92236,#4247);
#2961=LINE('',#92239,#4248);
#2962=LINE('',#92241,#4249);
#2963=LINE('',#92242,#4250);
#2964=LINE('',#92246,#4251);
#2965=LINE('',#92249,#4252);
#2966=LINE('',#92250,#4253);
#2967=LINE('',#92254,#4254);
#2968=LINE('',#92257,#4255);
#2969=LINE('',#92258,#4256);
#2970=LINE('',#92260,#4257);
#2971=LINE('',#92265,#4258);
#2972=LINE('',#92270,#4259);
#2973=LINE('',#92280,#4260);
#2974=LINE('',#92284,#4261);
#2975=LINE('',#92286,#4262);
#2976=LINE('',#92288,#4263);
#2977=LINE('',#92290,#4264);
#2978=LINE('',#92292,#4265);
#2979=LINE('',#92293,#4266);
#2980=LINE('',#92297,#4267);
#2981=LINE('',#92309,#4268);
#2982=LINE('',#92315,#4269);
#2983=LINE('',#92317,#4270);
#2984=LINE('',#92319,#4271);
#2985=LINE('',#92321,#4272);
#2986=LINE('',#92323,#4273);
#2987=LINE('',#92351,#4274);
#2988=LINE('',#92353,#4275);
#2989=LINE('',#92357,#4276);
#2990=LINE('',#92364,#4277);
#2991=LINE('',#92366,#4278);
#2992=LINE('',#92372,#4279);
#2993=LINE('',#92374,#4280);
#2994=LINE('',#92375,#4281);
#2995=LINE('',#92376,#4282);
#2996=LINE('',#92380,#4283);
#2997=LINE('',#92383,#4284);
#2998=LINE('',#92385,#4285);
#2999=LINE('',#92386,#4286);
#3000=LINE('',#92390,#4287);
#3001=LINE('',#92393,#4288);
#3002=LINE('',#92394,#4289);
#3003=LINE('',#92399,#4290);
#3004=LINE('',#92403,#4291);
#3005=LINE('',#92405,#4292);
#3006=LINE('',#92409,#4293);
#3007=LINE('',#92410,#4294);
#3008=LINE('',#92415,#4295);
#3009=LINE('',#92419,#4296);
#3010=LINE('',#92421,#4297);
#3011=LINE('',#92425,#4298);
#3012=LINE('',#92426,#4299);
#3013=LINE('',#92431,#4300);
#3014=LINE('',#92435,#4301);
#3015=LINE('',#92437,#4302);
#3016=LINE('',#92441,#4303);
#3017=LINE('',#92442,#4304);
#3018=LINE('',#92464,#4305);
#3019=LINE('',#92468,#4306);
#3020=LINE('',#92470,#4307);
#3021=LINE('',#92474,#4308);
#3022=LINE('',#92475,#4309);
#3023=LINE('',#92483,#4310);
#3024=LINE('',#92485,#4311);
#3025=LINE('',#92487,#4312);
#3026=LINE('',#92489,#4313);
#3027=LINE('',#92491,#4314);
#3028=LINE('',#92493,#4315);
#3029=LINE('',#92495,#4316);
#3030=LINE('',#92497,#4317);
#3031=LINE('',#92506,#4318);
#3032=LINE('',#92516,#4319);
#3033=LINE('',#92520,#4320);
#3034=LINE('',#92548,#4321);
#3035=LINE('',#92551,#4322);
#3036=LINE('',#92557,#4323);
#3037=LINE('',#92558,#4324);
#3038=LINE('',#92560,#4325);
#3039=LINE('',#92561,#4326);
#3040=LINE('',#92576,#4327);
#3041=LINE('',#92584,#4328);
#3042=LINE('',#92586,#4329);
#3043=LINE('',#92588,#4330);
#3044=LINE('',#92590,#4331);
#3045=LINE('',#92592,#4332);
#3046=LINE('',#92596,#4333);
#3047=LINE('',#92598,#4334);
#3048=LINE('',#92600,#4335);
#3049=LINE('',#92601,#4336);
#3050=LINE('',#92608,#4337);
#3051=LINE('',#92609,#4338);
#3052=LINE('',#92613,#4339);
#3053=LINE('',#92617,#4340);
#3054=LINE('',#92624,#4341);
#3055=LINE('',#92626,#4342);
#3056=LINE('',#92627,#4343);
#3057=LINE('',#92645,#4344);
#3058=LINE('',#92656,#4345);
#3059=LINE('',#92660,#4346);
#3060=LINE('',#92714,#4347);
#3061=LINE('',#92718,#4348);
#3062=LINE('',#92744,#4349);
#3063=LINE('',#92748,#4350);
#3064=LINE('',#92760,#4351);
#3065=LINE('',#92770,#4352);
#3066=LINE('',#92772,#4353);
#3067=LINE('',#92776,#4354);
#3068=LINE('',#92777,#4355);
#3069=LINE('',#92780,#4356);
#3070=LINE('',#92783,#4357);
#3071=LINE('',#92784,#4358);
#3072=LINE('',#92788,#4359);
#3073=LINE('',#92790,#4360);
#3074=LINE('',#92792,#4361);
#3075=LINE('',#92793,#4362);
#3076=LINE('',#92799,#4363);
#3077=LINE('',#92805,#4364);
#3078=LINE('',#92811,#4365);
#3079=LINE('',#92819,#4366);
#3080=LINE('',#92823,#4367);
#3081=LINE('',#92826,#4368);
#3082=LINE('',#92829,#4369);
#3083=LINE('',#92830,#4370);
#3084=LINE('',#92834,#4371);
#3085=LINE('',#92836,#4372);
#3086=LINE('',#92838,#4373);
#3087=LINE('',#92839,#4374);
#3088=LINE('',#92842,#4375);
#3089=LINE('',#92844,#4376);
#3090=LINE('',#92854,#4377);
#3091=LINE('',#92873,#4378);
#3092=LINE('',#92876,#4379);
#3093=LINE('',#92881,#4380);
#3094=LINE('',#92883,#4381);
#3095=LINE('',#92886,#4382);
#3096=LINE('',#92889,#4383);
#3097=LINE('',#92891,#4384);
#3098=LINE('',#92896,#4385);
#3099=LINE('',#92898,#4386);
#3100=LINE('',#92900,#4387);
#3101=LINE('',#92905,#4388);
#3102=LINE('',#92910,#4389);
#3103=LINE('',#92912,#4390);
#3104=LINE('',#92914,#4391);
#3105=LINE('',#92919,#4392);
#3106=LINE('',#92933,#4393);
#3107=LINE('',#92957,#4394);
#3108=LINE('',#92986,#4395);
#3109=LINE('',#92988,#4396);
#3110=LINE('',#92989,#4397);
#3111=LINE('',#92991,#4398);
#3112=LINE('',#93005,#4399);
#3113=LINE('',#93010,#4400);
#3114=LINE('',#93012,#4401);
#3115=LINE('',#93024,#4402);
#3116=LINE('',#93026,#4403);
#3117=LINE('',#93029,#4404);
#3118=LINE('',#93031,#4405);
#3119=LINE('',#93032,#4406);
#3120=LINE('',#93034,#4407);
#3121=LINE('',#93036,#4408);
#3122=LINE('',#93038,#4409);
#3123=LINE('',#93041,#4410);
#3124=LINE('',#93043,#4411);
#3125=LINE('',#93044,#4412);
#3126=LINE('',#93046,#4413);
#3127=LINE('',#93055,#4414);
#3128=LINE('',#93058,#4415);
#3129=LINE('',#93104,#4416);
#3130=LINE('',#93128,#4417);
#3131=LINE('',#93131,#4418);
#3132=LINE('',#93135,#4419);
#3133=LINE('',#93136,#4420);
#3134=LINE('',#93138,#4421);
#3135=LINE('',#93141,#4422);
#3136=LINE('',#93145,#4423);
#3137=LINE('',#93146,#4424);
#3138=LINE('',#93148,#4425);
#3139=LINE('',#93151,#4426);
#3140=LINE('',#93155,#4427);
#3141=LINE('',#93156,#4428);
#3142=LINE('',#93158,#4429);
#3143=LINE('',#93162,#4430);
#3144=LINE('',#93163,#4431);
#3145=LINE('',#93165,#4432);
#3146=LINE('',#93167,#4433);
#3147=LINE('',#93175,#4434);
#3148=LINE('',#93176,#4435);
#3149=LINE('',#93178,#4436);
#3150=LINE('',#93179,#4437);
#4073=VECTOR('',#25895,10.);
#4074=VECTOR('',#25904,10.);
#4075=VECTOR('',#25905,10.);
#4076=VECTOR('',#25914,10.);
#4077=VECTOR('',#25915,10.);
#4078=VECTOR('',#25924,10.);
#4079=VECTOR('',#25933,10.);
#4080=VECTOR('',#25934,10.);
#4081=VECTOR('',#25939,10.);
#4082=VECTOR('',#25942,10.);
#4083=VECTOR('',#25945,10.);
#4084=VECTOR('',#25946,10.);
#4085=VECTOR('',#25947,10.);
#4086=VECTOR('',#25952,10.);
#4087=VECTOR('',#25957,10.);
#4088=VECTOR('',#25960,10.);
#4089=VECTOR('',#25963,10.);
#4090=VECTOR('',#25966,10.);
#4091=VECTOR('',#25969,10.);
#4092=VECTOR('',#25972,10.);
#4093=VECTOR('',#25973,10.);
#4094=VECTOR('',#25974,10.);
#4095=VECTOR('',#25975,10.);
#4096=VECTOR('',#25976,10.);
#4097=VECTOR('',#25977,10.);
#4098=VECTOR('',#25982,10.);
#4099=VECTOR('',#25987,10.);
#4100=VECTOR('',#25992,10.);
#4101=VECTOR('',#25997,10.);
#4102=VECTOR('',#25998,10.);
#4103=VECTOR('',#26003,10.);
#4104=VECTOR('',#26006,10.);
#4105=VECTOR('',#26009,10.);
#4106=VECTOR('',#26014,10.);
#4107=VECTOR('',#26015,10.);
#4108=VECTOR('',#26016,10.);
#4109=VECTOR('',#26021,10.);
#4110=VECTOR('',#26022,10.);
#4111=VECTOR('',#26025,10.);
#4112=VECTOR('',#26028,10.);
#4113=VECTOR('',#26031,10.);
#4114=VECTOR('',#26032,10.);
#4115=VECTOR('',#26033,10.);
#4116=VECTOR('',#26036,10.);
#4117=VECTOR('',#26037,10.);
#4118=VECTOR('',#26040,10.);
#4119=VECTOR('',#26043,10.);
#4120=VECTOR('',#26044,10.);
#4121=VECTOR('',#26045,10.);
#4122=VECTOR('',#26046,10.);
#4123=VECTOR('',#26047,10.);
#4124=VECTOR('',#26050,10.);
#4125=VECTOR('',#26053,10.);
#4126=VECTOR('',#26068,10.);
#4127=VECTOR('',#26073,10.);
#4128=VECTOR('',#26078,10.);
#4129=VECTOR('',#26079,10.);
#4130=VECTOR('',#26084,10.);
#4131=VECTOR('',#26087,10.);
#4132=VECTOR('',#26090,10.);
#4133=VECTOR('',#26093,10.);
#4134=VECTOR('',#26104,10.);
#4135=VECTOR('',#26105,10.);
#4136=VECTOR('',#26106,10.);
#4137=VECTOR('',#26107,10.);
#4138=VECTOR('',#26110,10.);
#4139=VECTOR('',#26115,10.);
#4140=VECTOR('',#26116,10.);
#4141=VECTOR('',#26117,10.);
#4142=VECTOR('',#26118,10.);
#4143=VECTOR('',#26119,10.);
#4144=VECTOR('',#26120,10.);
#4145=VECTOR('',#26121,10.);
#4146=VECTOR('',#26124,10.);
#4147=VECTOR('',#26131,10.);
#4148=VECTOR('',#26132,10.);
#4149=VECTOR('',#26133,10.);
#4150=VECTOR('',#26146,10.);
#4151=VECTOR('',#26149,10.);
#4152=VECTOR('',#26152,10.);
#4153=VECTOR('',#26155,10.);
#4154=VECTOR('',#26156,10.);
#4155=VECTOR('',#26165,10.);
#4156=VECTOR('',#26166,10.);
#4157=VECTOR('',#26169,10.);
#4158=VECTOR('',#26172,10.);
#4159=VECTOR('',#26175,10.);
#4160=VECTOR('',#26176,10.);
#4161=VECTOR('',#26179,10.);
#4162=VECTOR('',#26182,10.);
#4163=VECTOR('',#26197,4.05);
#4164=VECTOR('',#26204,10.);
#4165=VECTOR('',#26217,10.);
#4166=VECTOR('',#26224,10.);
#4167=VECTOR('',#26227,10.);
#4168=VECTOR('',#26232,10.);
#4169=VECTOR('',#26235,10.);
#4170=VECTOR('',#26246,10.);
#4171=VECTOR('',#26257,10.);
#4172=VECTOR('',#26262,10.);
#4173=VECTOR('',#26267,10.);
#4174=VECTOR('',#26276,10.);
#4175=VECTOR('',#26281,1.25);
#4176=VECTOR('',#26282,10.);
#4177=VECTOR('',#26285,10.);
#4178=VECTOR('',#26286,10.);
#4179=VECTOR('',#26289,10.);
#4180=VECTOR('',#26290,10.);
#4181=VECTOR('',#26293,10.);
#4182=VECTOR('',#26298,10.);
#4183=VECTOR('',#26299,10.);
#4184=VECTOR('',#26300,10.);
#4185=VECTOR('',#26305,1.5);
#4186=VECTOR('',#26308,10.);
#4187=VECTOR('',#26309,10.);
#4188=VECTOR('',#26316,10.);
#4189=VECTOR('',#26325,10.);
#4190=VECTOR('',#26334,10.);
#4191=VECTOR('',#26337,10.);
#4192=VECTOR('',#26344,10.);
#4193=VECTOR('',#26347,10.);
#4194=VECTOR('',#26350,10.);
#4195=VECTOR('',#26351,10.);
#4196=VECTOR('',#26352,10.);
#4197=VECTOR('',#26357,10.);
#4198=VECTOR('',#26374,10.);
#4199=VECTOR('',#26377,10.);
#4200=VECTOR('',#26380,10.);
#4201=VECTOR('',#26385,1.25);
#4202=VECTOR('',#26400,1.5);
#4203=VECTOR('',#26403,10.);
#4204=VECTOR('',#26404,10.);
#4205=VECTOR('',#26417,10.);
#4206=VECTOR('',#26422,10.);
#4207=VECTOR('',#26425,10.);
#4208=VECTOR('',#26428,10.);
#4209=VECTOR('',#26431,10.);
#4210=VECTOR('',#26434,10.);
#4211=VECTOR('',#26435,10.);
#4212=VECTOR('',#26436,10.);
#4213=VECTOR('',#26437,10.);
#4214=VECTOR('',#26442,10.);
#4215=VECTOR('',#26445,10.);
#4216=VECTOR('',#26456,10.);
#4217=VECTOR('',#26467,10.);
#4218=VECTOR('',#26468,10.);
#4219=VECTOR('',#26473,10.);
#4220=VECTOR('',#26474,10.);
#4221=VECTOR('',#26475,10.);
#4222=VECTOR('',#26478,10.);
#4223=VECTOR('',#26479,10.);
#4224=VECTOR('',#26480,10.);
#4225=VECTOR('',#26481,10.);
#4226=VECTOR('',#26482,10.);
#4227=VECTOR('',#26483,10.);
#4228=VECTOR('',#26484,10.);
#4229=VECTOR('',#26485,10.);
#4230=VECTOR('',#26486,10.);
#4231=VECTOR('',#26487,10.);
#4232=VECTOR('',#26488,10.);
#4233=VECTOR('',#26489,10.);
#4234=VECTOR('',#26490,10.);
#4235=VECTOR('',#26491,10.);
#4236=VECTOR('',#26492,10.);
#4237=VECTOR('',#26493,10.);
#4238=VECTOR('',#26494,10.);
#4239=VECTOR('',#26495,10.);
#4240=VECTOR('',#26496,10.);
#4241=VECTOR('',#26499,10.);
#4242=VECTOR('',#26500,10.);
#4243=VECTOR('',#26501,10.);
#4244=VECTOR('',#26510,10.);
#4245=VECTOR('',#26513,10.);
#4246=VECTOR('',#26526,10.);
#4247=VECTOR('',#26527,10.);
#4248=VECTOR('',#26530,10.);
#4249=VECTOR('',#26531,10.);
#4250=VECTOR('',#26532,10.);
#4251=VECTOR('',#26537,10.);
#4252=VECTOR('',#26540,10.);
#4253=VECTOR('',#26541,10.);
#4254=VECTOR('',#26546,10.);
#4255=VECTOR('',#26549,10.);
#4256=VECTOR('',#26550,10.);
#4257=VECTOR('',#26553,10.);
#4258=VECTOR('',#26560,10.);
#4259=VECTOR('',#26569,10.);
#4260=VECTOR('',#26586,10.);
#4261=VECTOR('',#26591,10.);
#4262=VECTOR('',#26592,10.);
#4263=VECTOR('',#26593,10.);
#4264=VECTOR('',#26594,10.);
#4265=VECTOR('',#26595,10.);
#4266=VECTOR('',#26596,10.);
#4267=VECTOR('',#26601,10.);
#4268=VECTOR('',#26616,1.5);
#4269=VECTOR('',#26621,10.);
#4270=VECTOR('',#26622,10.);
#4271=VECTOR('',#26623,10.);
#4272=VECTOR('',#26624,10.);
#4273=VECTOR('',#26625,10.);
#4274=VECTOR('',#26646,1.25);
#4275=VECTOR('',#26649,10.);
#4276=VECTOR('',#26654,10.);
#4277=VECTOR('',#26665,10.);
#4278=VECTOR('',#26668,10.);
#4279=VECTOR('',#26675,10.);
#4280=VECTOR('',#26678,10.);
#4281=VECTOR('',#26679,10.);
#4282=VECTOR('',#26680,10.);
#4283=VECTOR('',#26685,10.);
#4284=VECTOR('',#26688,10.);
#4285=VECTOR('',#26689,10.);
#4286=VECTOR('',#26690,10.);
#4287=VECTOR('',#26695,10.);
#4288=VECTOR('',#26698,10.);
#4289=VECTOR('',#26699,10.);
#4290=VECTOR('',#26704,10.);
#4291=VECTOR('',#26709,10.);
#4292=VECTOR('',#26710,10.);
#4293=VECTOR('',#26713,10.);
#4294=VECTOR('',#26714,10.);
#4295=VECTOR('',#26719,10.);
#4296=VECTOR('',#26724,10.);
#4297=VECTOR('',#26725,10.);
#4298=VECTOR('',#26728,10.);
#4299=VECTOR('',#26729,10.);
#4300=VECTOR('',#26734,10.);
#4301=VECTOR('',#26739,10.);
#4302=VECTOR('',#26740,10.);
#4303=VECTOR('',#26743,10.);
#4304=VECTOR('',#26744,10.);
#4305=VECTOR('',#26749,10.);
#4306=VECTOR('',#26754,10.);
#4307=VECTOR('',#26755,10.);
#4308=VECTOR('',#26758,10.);
#4309=VECTOR('',#26759,10.);
#4310=VECTOR('',#26770,10.);
#4311=VECTOR('',#26773,10.);
#4312=VECTOR('',#26776,10.);
#4313=VECTOR('',#26779,10.);
#4314=VECTOR('',#26782,10.);
#4315=VECTOR('',#26785,10.);
#4316=VECTOR('',#26788,10.);
#4317=VECTOR('',#26791,10.);
#4318=VECTOR('',#26802,0.6528);
#4319=VECTOR('',#26815,0.6528);
#4320=VECTOR('',#26820,0.4896);
#4321=VECTOR('',#26839,10.);
#4322=VECTOR('',#26842,10.);
#4323=VECTOR('',#26851,10.);
#4324=VECTOR('',#26852,10.);
#4325=VECTOR('',#26853,10.);
#4326=VECTOR('',#26854,10.);
#4327=VECTOR('',#26879,10.);
#4328=VECTOR('',#26892,10.);
#4329=VECTOR('',#26893,10.);
#4330=VECTOR('',#26894,10.);
#4331=VECTOR('',#26895,10.);
#4332=VECTOR('',#26896,10.);
#4333=VECTOR('',#26899,10.);
#4334=VECTOR('',#26900,10.);
#4335=VECTOR('',#26901,10.);
#4336=VECTOR('',#26902,10.);
#4337=VECTOR('',#26911,10.);
#4338=VECTOR('',#26912,10.);
#4339=VECTOR('',#26917,10.);
#4340=VECTOR('',#26924,10.);
#4341=VECTOR('',#26935,10.);
#4342=VECTOR('',#26936,10.);
#4343=VECTOR('',#26937,10.);
#4344=VECTOR('',#26964,1.25);
#4345=VECTOR('',#26967,10.);
#4346=VECTOR('',#26970,10.);
#4347=VECTOR('',#26973,10.);
#4348=VECTOR('',#26976,10.);
#4349=VECTOR('',#26977,10.);
#4350=VECTOR('',#26980,10.);
#4351=VECTOR('',#26983,10.);
#4352=VECTOR('',#26996,10.);
#4353=VECTOR('',#26997,10.);
#4354=VECTOR('',#27002,10.);
#4355=VECTOR('',#27003,10.);
#4356=VECTOR('',#27006,10.);
#4357=VECTOR('',#27009,10.);
#4358=VECTOR('',#27010,10.);
#4359=VECTOR('',#27013,10.);
#4360=VECTOR('',#27014,10.);
#4361=VECTOR('',#27015,10.);
#4362=VECTOR('',#27016,10.);
#4363=VECTOR('',#27021,10.);
#4364=VECTOR('',#27026,10.);
#4365=VECTOR('',#27033,10.);
#4366=VECTOR('',#27042,10.);
#4367=VECTOR('',#27045,10.);
#4368=VECTOR('',#27048,10.);
#4369=VECTOR('',#27051,10.);
#4370=VECTOR('',#27052,10.);
#4371=VECTOR('',#27055,10.);
#4372=VECTOR('',#27056,10.);
#4373=VECTOR('',#27057,10.);
#4374=VECTOR('',#27058,10.);
#4375=VECTOR('',#27061,10.);
#4376=VECTOR('',#27062,10.);
#4377=VECTOR('',#27073,10.);
#4378=VECTOR('',#27074,10.);
#4379=VECTOR('',#27077,10.);
#4380=VECTOR('',#27084,10.);
#4381=VECTOR('',#27085,10.);
#4382=VECTOR('',#27090,10.);
#4383=VECTOR('',#27093,10.);
#4384=VECTOR('',#27096,10.);
#4385=VECTOR('',#27101,10.);
#4386=VECTOR('',#27102,10.);
#4387=VECTOR('',#27103,10.);
#4388=VECTOR('',#27110,10.);
#4389=VECTOR('',#27115,10.);
#4390=VECTOR('',#27116,10.);
#4391=VECTOR('',#27117,10.);
#4392=VECTOR('',#27124,10.);
#4393=VECTOR('',#27149,10.);
#4394=VECTOR('',#27152,10.);
#4395=VECTOR('',#27165,10.);
#4396=VECTOR('',#27166,10.);
#4397=VECTOR('',#27167,10.);
#4398=VECTOR('',#27170,10.);
#4399=VECTOR('',#27179,10.);
#4400=VECTOR('',#27184,10.);
#4401=VECTOR('',#27185,10.);
#4402=VECTOR('',#27186,10.);
#4403=VECTOR('',#27189,10.);
#4404=VECTOR('',#27192,10.);
#4405=VECTOR('',#27193,10.);
#4406=VECTOR('',#27194,10.);
#4407=VECTOR('',#27197,10.);
#4408=VECTOR('',#27200,10.);
#4409=VECTOR('',#27203,10.);
#4410=VECTOR('',#27206,10.);
#4411=VECTOR('',#27207,10.);
#4412=VECTOR('',#27208,10.);
#4413=VECTOR('',#27211,10.);
#4414=VECTOR('',#27222,1.5);
#4415=VECTOR('',#27225,10.);
#4416=VECTOR('',#27230,10.);
#4417=VECTOR('',#27237,10.);
#4418=VECTOR('',#27242,10.);
#4419=VECTOR('',#27247,10.);
#4420=VECTOR('',#27248,10.);
#4421=VECTOR('',#27251,10.);
#4422=VECTOR('',#27256,10.);
#4423=VECTOR('',#27261,10.);
#4424=VECTOR('',#27262,10.);
#4425=VECTOR('',#27265,10.);
#4426=VECTOR('',#27270,10.);
#4427=VECTOR('',#27275,10.);
#4428=VECTOR('',#27276,10.);
#4429=VECTOR('',#27279,10.);
#4430=VECTOR('',#27284,10.);
#4431=VECTOR('',#27285,10.);
#4432=VECTOR('',#27288,10.);
#4433=VECTOR('',#27291,10.);
#4434=VECTOR('',#27306,10.);
#4435=VECTOR('',#27307,10.);
#4436=VECTOR('',#27310,10.);
#4437=VECTOR('',#27311,10.);
#4862=CYLINDRICAL_SURFACE('',#21623,0.6);
#4863=CYLINDRICAL_SURFACE('',#21632,0.6);
#4864=CYLINDRICAL_SURFACE('',#21636,0.6);
#4865=CYLINDRICAL_SURFACE('',#21645,0.6);
#4866=CYLINDRICAL_SURFACE('',#21648,0.6);
#4867=CYLINDRICAL_SURFACE('',#21650,0.6);
#4868=CYLINDRICAL_SURFACE('',#21667,0.6);
#4869=CYLINDRICAL_SURFACE('',#21674,0.6);
#4870=CYLINDRICAL_SURFACE('',#21678,0.6);
#4871=CYLINDRICAL_SURFACE('',#21680,0.6);
#4872=CYLINDRICAL_SURFACE('',#21683,0.6);
#4873=CYLINDRICAL_SURFACE('',#21690,0.6);
#4874=CYLINDRICAL_SURFACE('',#21693,0.6);
#4875=CYLINDRICAL_SURFACE('',#21701,0.6);
#4876=CYLINDRICAL_SURFACE('',#21703,0.6);
#4877=CYLINDRICAL_SURFACE('',#21709,0.6);
#4878=CYLINDRICAL_SURFACE('',#21710,10.608);
#4879=CYLINDRICAL_SURFACE('',#21721,4.05);
#4880=CYLINDRICAL_SURFACE('',#21722,8.976);
#4881=CYLINDRICAL_SURFACE('',#21730,0.6);
#4882=CYLINDRICAL_SURFACE('',#21732,0.6);
#4883=CYLINDRICAL_SURFACE('',#21735,0.6);
#4884=CYLINDRICAL_SURFACE('',#21742,0.6);
#4885=CYLINDRICAL_SURFACE('',#21746,0.6);
#4886=CYLINDRICAL_SURFACE('',#21748,0.6);
#4887=CYLINDRICAL_SURFACE('',#21750,0.6);
#4888=CYLINDRICAL_SURFACE('',#21753,0.6);
#4889=CYLINDRICAL_SURFACE('',#21756,1.25);
#4890=CYLINDRICAL_SURFACE('',#21761,0.600000000000001);
#4891=CYLINDRICAL_SURFACE('',#21763,1.5);
#4892=CYLINDRICAL_SURFACE('',#21767,0.6);
#4893=CYLINDRICAL_SURFACE('',#21770,0.6);
#4894=CYLINDRICAL_SURFACE('',#21775,0.6);
#4895=CYLINDRICAL_SURFACE('',#21780,0.6);
#4896=CYLINDRICAL_SURFACE('',#21792,0.6);
#4897=CYLINDRICAL_SURFACE('',#21795,1.25);
#4898=CYLINDRICAL_SURFACE('',#21802,1.5);
#4899=CYLINDRICAL_SURFACE('',#21809,0.6);
#4900=CYLINDRICAL_SURFACE('',#21812,0.6);
#4901=CYLINDRICAL_SURFACE('',#21815,0.6);
#4902=CYLINDRICAL_SURFACE('',#21817,0.6);
#4903=CYLINDRICAL_SURFACE('',#21820,0.6);
#4904=CYLINDRICAL_SURFACE('',#21822,0.6);
#4905=CYLINDRICAL_SURFACE('',#21826,0.6);
#4906=CYLINDRICAL_SURFACE('',#21836,0.6);
#4907=CYLINDRICAL_SURFACE('',#21838,0.6);
#4908=CYLINDRICAL_SURFACE('',#21843,0.6);
#4909=CYLINDRICAL_SURFACE('',#21846,0.6);
#4910=CYLINDRICAL_SURFACE('',#21849,0.6);
#4911=CYLINDRICAL_SURFACE('',#21852,0.6);
#4912=CYLINDRICAL_SURFACE('',#21858,0.6);
#4913=CYLINDRICAL_SURFACE('',#21860,0.6);
#4914=CYLINDRICAL_SURFACE('',#21861,0.6);
#4915=CYLINDRICAL_SURFACE('',#21863,0.6);
#4916=CYLINDRICAL_SURFACE('',#21867,0.6);
#4917=CYLINDRICAL_SURFACE('',#21870,0.6);
#4918=CYLINDRICAL_SURFACE('',#21876,1.5);
#4919=CYLINDRICAL_SURFACE('',#21885,0.6);
#4920=CYLINDRICAL_SURFACE('',#21888,1.25);
#4921=CYLINDRICAL_SURFACE('',#21893,0.6);
#4922=CYLINDRICAL_SURFACE('',#21895,0.6);
#4923=CYLINDRICAL_SURFACE('',#21897,0.6);
#4924=CYLINDRICAL_SURFACE('',#21900,0.6);
#4925=CYLINDRICAL_SURFACE('',#21904,0.6);
#4926=CYLINDRICAL_SURFACE('',#21907,0.6);
#4927=CYLINDRICAL_SURFACE('',#21910,0.6);
#4928=CYLINDRICAL_SURFACE('',#21915,0.6);
#4929=CYLINDRICAL_SURFACE('',#21920,0.6);
#4930=CYLINDRICAL_SURFACE('',#21925,0.6);
#4931=CYLINDRICAL_SURFACE('',#21934,0.6);
#4932=CYLINDRICAL_SURFACE('',#21936,0.6);
#4933=CYLINDRICAL_SURFACE('',#21938,0.6);
#4934=CYLINDRICAL_SURFACE('',#21940,0.6);
#4935=CYLINDRICAL_SURFACE('',#21946,0.6528);
#4936=CYLINDRICAL_SURFACE('',#21952,0.6528);
#4937=CYLINDRICAL_SURFACE('',#21954,0.4896);
#4938=CYLINDRICAL_SURFACE('',#21963,0.6);
#4939=CYLINDRICAL_SURFACE('',#21969,0.6);
#4940=CYLINDRICAL_SURFACE('',#21972,0.6);
#4941=CYLINDRICAL_SURFACE('',#21977,0.6);
#4942=CYLINDRICAL_SURFACE('',#21979,0.6);
#4943=CYLINDRICAL_SURFACE('',#21982,0.6);
#4944=CYLINDRICAL_SURFACE('',#21988,0.6);
#4945=CYLINDRICAL_SURFACE('',#21990,0.6);
#4946=CYLINDRICAL_SURFACE('',#21992,0.6);
#4947=CYLINDRICAL_SURFACE('',#21995,0.6);
#4948=CYLINDRICAL_SURFACE('',#22002,0.6);
#4949=CYLINDRICAL_SURFACE('',#22004,0.6);
#4950=CYLINDRICAL_SURFACE('',#22005,0.6);
#4951=CYLINDRICAL_SURFACE('',#22014,1.25);
#4952=CYLINDRICAL_SURFACE('',#22023,0.6);
#4953=CYLINDRICAL_SURFACE('',#22025,0.6);
#4954=CYLINDRICAL_SURFACE('',#22032,0.6);
#4955=CYLINDRICAL_SURFACE('',#22037,0.6);
#4956=CYLINDRICAL_SURFACE('',#22050,0.6);
#4957=CYLINDRICAL_SURFACE('',#22054,0.6);
#4958=CYLINDRICAL_SURFACE('',#22058,0.6);
#4959=CYLINDRICAL_SURFACE('',#22064,0.6);
#4960=CYLINDRICAL_SURFACE('',#22070,0.6);
#4961=CYLINDRICAL_SURFACE('',#22071,0.6);
#4962=CYLINDRICAL_SURFACE('',#22073,0.6);
#4963=CYLINDRICAL_SURFACE('',#22079,0.6);
#4964=CYLINDRICAL_SURFACE('',#22083,0.6);
#4965=CYLINDRICAL_SURFACE('',#22094,0.6);
#4966=CYLINDRICAL_SURFACE('',#22097,0.6);
#4967=CYLINDRICAL_SURFACE('',#22099,0.6);
#4968=CYLINDRICAL_SURFACE('',#22101,0.6);
#4969=CYLINDRICAL_SURFACE('',#22108,1.5);
#4970=CYLINDRICAL_SURFACE('',#22140,5.712);
#4971=CYLINDRICAL_SURFACE('',#22141,5.712);
#5740=FACE_OUTER_BOUND('',#6963,.T.);
#5741=FACE_OUTER_BOUND('',#6964,.T.);
#5742=FACE_OUTER_BOUND('',#6965,.T.);
#5743=FACE_OUTER_BOUND('',#6966,.T.);
#5744=FACE_OUTER_BOUND('',#6967,.T.);
#5745=FACE_OUTER_BOUND('',#6968,.T.);
#5746=FACE_OUTER_BOUND('',#6969,.T.);
#5747=FACE_OUTER_BOUND('',#6970,.T.);
#5748=FACE_OUTER_BOUND('',#6971,.T.);
#5749=FACE_OUTER_BOUND('',#6972,.T.);
#5750=FACE_OUTER_BOUND('',#6973,.T.);
#5751=FACE_OUTER_BOUND('',#6974,.T.);
#5752=FACE_OUTER_BOUND('',#6975,.T.);
#5753=FACE_OUTER_BOUND('',#6976,.T.);
#5754=FACE_OUTER_BOUND('',#6977,.T.);
#5755=FACE_OUTER_BOUND('',#6978,.T.);
#5756=FACE_OUTER_BOUND('',#6979,.T.);
#5757=FACE_OUTER_BOUND('',#6980,.T.);
#5758=FACE_OUTER_BOUND('',#6981,.T.);
#5759=FACE_OUTER_BOUND('',#6982,.T.);
#5760=FACE_OUTER_BOUND('',#6983,.T.);
#5761=FACE_OUTER_BOUND('',#6984,.T.);
#5762=FACE_OUTER_BOUND('',#6985,.T.);
#5763=FACE_OUTER_BOUND('',#6986,.T.);
#5764=FACE_OUTER_BOUND('',#6987,.T.);
#5765=FACE_OUTER_BOUND('',#6988,.T.);
#5766=FACE_OUTER_BOUND('',#6989,.T.);
#5767=FACE_OUTER_BOUND('',#6990,.T.);
#5768=FACE_OUTER_BOUND('',#6991,.T.);
#5769=FACE_OUTER_BOUND('',#6992,.T.);
#5770=FACE_OUTER_BOUND('',#6993,.T.);
#5771=FACE_OUTER_BOUND('',#6994,.T.);
#5772=FACE_OUTER_BOUND('',#6995,.T.);
#5773=FACE_OUTER_BOUND('',#6996,.T.);
#5774=FACE_OUTER_BOUND('',#6997,.T.);
#5775=FACE_OUTER_BOUND('',#6998,.T.);
#5776=FACE_OUTER_BOUND('',#6999,.T.);
#5777=FACE_OUTER_BOUND('',#7000,.T.);
#5778=FACE_OUTER_BOUND('',#7001,.T.);
#5779=FACE_OUTER_BOUND('',#7002,.T.);
#5780=FACE_OUTER_BOUND('',#7003,.T.);
#5781=FACE_OUTER_BOUND('',#7004,.T.);
#5782=FACE_OUTER_BOUND('',#7005,.T.);
#5783=FACE_OUTER_BOUND('',#7007,.T.);
#5784=FACE_OUTER_BOUND('',#7008,.T.);
#5785=FACE_OUTER_BOUND('',#7009,.T.);
#5786=FACE_OUTER_BOUND('',#7010,.T.);
#5787=FACE_OUTER_BOUND('',#7012,.T.);
#5788=FACE_OUTER_BOUND('',#7013,.T.);
#5789=FACE_OUTER_BOUND('',#7014,.T.);
#5790=FACE_OUTER_BOUND('',#7015,.T.);
#5791=FACE_OUTER_BOUND('',#7016,.T.);
#5792=FACE_OUTER_BOUND('',#7017,.T.);
#5793=FACE_OUTER_BOUND('',#7018,.T.);
#5794=FACE_OUTER_BOUND('',#7019,.T.);
#5795=FACE_OUTER_BOUND('',#7020,.T.);
#5796=FACE_OUTER_BOUND('',#7021,.T.);
#5797=FACE_OUTER_BOUND('',#7022,.T.);
#5798=FACE_OUTER_BOUND('',#7023,.T.);
#5799=FACE_OUTER_BOUND('',#7024,.T.);
#5800=FACE_OUTER_BOUND('',#7025,.T.);
#5801=FACE_OUTER_BOUND('',#7026,.T.);
#5802=FACE_OUTER_BOUND('',#7027,.T.);
#5803=FACE_OUTER_BOUND('',#7028,.T.);
#5804=FACE_OUTER_BOUND('',#7029,.T.);
#5805=FACE_OUTER_BOUND('',#7030,.T.);
#5806=FACE_OUTER_BOUND('',#7031,.T.);
#5807=FACE_OUTER_BOUND('',#7032,.T.);
#5808=FACE_OUTER_BOUND('',#7033,.T.);
#5809=FACE_OUTER_BOUND('',#7034,.T.);
#5810=FACE_OUTER_BOUND('',#7035,.T.);
#5811=FACE_OUTER_BOUND('',#7037,.T.);
#5812=FACE_OUTER_BOUND('',#7038,.T.);
#5813=FACE_OUTER_BOUND('',#7039,.T.);
#5814=FACE_OUTER_BOUND('',#7040,.T.);
#5815=FACE_OUTER_BOUND('',#7041,.T.);
#5816=FACE_OUTER_BOUND('',#7042,.T.);
#5817=FACE_OUTER_BOUND('',#7044,.T.);
#5818=FACE_OUTER_BOUND('',#7045,.T.);
#5819=FACE_OUTER_BOUND('',#7046,.T.);
#5820=FACE_OUTER_BOUND('',#7047,.T.);
#5821=FACE_OUTER_BOUND('',#7048,.T.);
#5822=FACE_OUTER_BOUND('',#7049,.T.);
#5823=FACE_OUTER_BOUND('',#7050,.T.);
#5824=FACE_OUTER_BOUND('',#7051,.T.);
#5825=FACE_OUTER_BOUND('',#7052,.T.);
#5826=FACE_OUTER_BOUND('',#7053,.T.);
#5827=FACE_OUTER_BOUND('',#7054,.T.);
#5828=FACE_OUTER_BOUND('',#7055,.T.);
#5829=FACE_OUTER_BOUND('',#7056,.T.);
#5830=FACE_OUTER_BOUND('',#7057,.T.);
#5831=FACE_OUTER_BOUND('',#7058,.T.);
#5832=FACE_OUTER_BOUND('',#7063,.T.);
#5833=FACE_OUTER_BOUND('',#7064,.T.);
#5834=FACE_OUTER_BOUND('',#7065,.T.);
#5835=FACE_OUTER_BOUND('',#7066,.T.);
#5836=FACE_OUTER_BOUND('',#7067,.T.);
#5837=FACE_OUTER_BOUND('',#7068,.T.);
#5838=FACE_OUTER_BOUND('',#7069,.T.);
#5839=FACE_OUTER_BOUND('',#7070,.T.);
#5840=FACE_OUTER_BOUND('',#7071,.T.);
#5841=FACE_OUTER_BOUND('',#7072,.T.);
#5842=FACE_OUTER_BOUND('',#7073,.T.);
#5843=FACE_OUTER_BOUND('',#7074,.T.);
#5844=FACE_OUTER_BOUND('',#7075,.T.);
#5845=FACE_OUTER_BOUND('',#7076,.T.);
#5846=FACE_OUTER_BOUND('',#7077,.T.);
#5847=FACE_OUTER_BOUND('',#7078,.T.);
#5848=FACE_OUTER_BOUND('',#7079,.T.);
#5849=FACE_OUTER_BOUND('',#7080,.T.);
#5850=FACE_OUTER_BOUND('',#7081,.T.);
#5851=FACE_OUTER_BOUND('',#7082,.T.);
#5852=FACE_OUTER_BOUND('',#7083,.T.);
#5853=FACE_OUTER_BOUND('',#7084,.T.);
#5854=FACE_OUTER_BOUND('',#7085,.T.);
#5855=FACE_OUTER_BOUND('',#7087,.T.);
#5856=FACE_OUTER_BOUND('',#7088,.T.);
#5857=FACE_OUTER_BOUND('',#7089,.T.);
#5858=FACE_OUTER_BOUND('',#7090,.T.);
#5859=FACE_OUTER_BOUND('',#7092,.T.);
#5860=FACE_OUTER_BOUND('',#7093,.T.);
#5861=FACE_OUTER_BOUND('',#7094,.T.);
#5862=FACE_OUTER_BOUND('',#7095,.T.);
#5863=FACE_OUTER_BOUND('',#7096,.T.);
#5864=FACE_OUTER_BOUND('',#7097,.T.);
#5865=FACE_OUTER_BOUND('',#7098,.T.);
#5866=FACE_OUTER_BOUND('',#7099,.T.);
#5867=FACE_OUTER_BOUND('',#7100,.T.);
#5868=FACE_OUTER_BOUND('',#7101,.T.);
#5869=FACE_OUTER_BOUND('',#7102,.T.);
#5870=FACE_OUTER_BOUND('',#7103,.T.);
#5871=FACE_OUTER_BOUND('',#7104,.T.);
#5872=FACE_OUTER_BOUND('',#7105,.T.);
#5873=FACE_OUTER_BOUND('',#7106,.T.);
#5874=FACE_OUTER_BOUND('',#7107,.T.);
#5875=FACE_OUTER_BOUND('',#7108,.T.);
#5876=FACE_OUTER_BOUND('',#7109,.T.);
#5877=FACE_OUTER_BOUND('',#7110,.T.);
#5878=FACE_OUTER_BOUND('',#7111,.T.);
#5879=FACE_OUTER_BOUND('',#7112,.T.);
#5880=FACE_OUTER_BOUND('',#7113,.T.);
#5881=FACE_OUTER_BOUND('',#7114,.T.);
#5882=FACE_OUTER_BOUND('',#7115,.T.);
#5883=FACE_OUTER_BOUND('',#7116,.T.);
#5884=FACE_OUTER_BOUND('',#7117,.T.);
#5885=FACE_OUTER_BOUND('',#7118,.T.);
#5886=FACE_OUTER_BOUND('',#7119,.T.);
#5887=FACE_OUTER_BOUND('',#7120,.T.);
#5888=FACE_OUTER_BOUND('',#7121,.T.);
#5889=FACE_OUTER_BOUND('',#7122,.T.);
#5890=FACE_OUTER_BOUND('',#7123,.T.);
#5891=FACE_OUTER_BOUND('',#7124,.T.);
#5892=FACE_OUTER_BOUND('',#7125,.T.);
#5893=FACE_OUTER_BOUND('',#7126,.T.);
#5894=FACE_OUTER_BOUND('',#7127,.T.);
#5895=FACE_OUTER_BOUND('',#7128,.T.);
#5896=FACE_OUTER_BOUND('',#7129,.T.);
#5897=FACE_OUTER_BOUND('',#7131,.T.);
#5898=FACE_OUTER_BOUND('',#7132,.T.);
#5899=FACE_OUTER_BOUND('',#7133,.T.);
#5900=FACE_OUTER_BOUND('',#7134,.T.);
#5901=FACE_OUTER_BOUND('',#7135,.T.);
#5902=FACE_OUTER_BOUND('',#7136,.T.);
#5903=FACE_OUTER_BOUND('',#7137,.T.);
#5904=FACE_OUTER_BOUND('',#7138,.T.);
#5905=FACE_OUTER_BOUND('',#7139,.T.);
#5906=FACE_OUTER_BOUND('',#7140,.T.);
#5907=FACE_OUTER_BOUND('',#7141,.T.);
#5908=FACE_OUTER_BOUND('',#7142,.T.);
#5909=FACE_OUTER_BOUND('',#7143,.T.);
#5910=FACE_OUTER_BOUND('',#7144,.T.);
#5911=FACE_OUTER_BOUND('',#7145,.T.);
#5912=FACE_OUTER_BOUND('',#7146,.T.);
#5913=FACE_OUTER_BOUND('',#7147,.T.);
#5914=FACE_OUTER_BOUND('',#7148,.T.);
#5915=FACE_OUTER_BOUND('',#7149,.T.);
#5916=FACE_OUTER_BOUND('',#7150,.T.);
#5917=FACE_OUTER_BOUND('',#7151,.T.);
#5918=FACE_OUTER_BOUND('',#7152,.T.);
#5919=FACE_OUTER_BOUND('',#7153,.T.);
#5920=FACE_OUTER_BOUND('',#7156,.T.);
#5921=FACE_OUTER_BOUND('',#7157,.T.);
#5922=FACE_OUTER_BOUND('',#7158,.T.);
#5923=FACE_OUTER_BOUND('',#7159,.T.);
#5924=FACE_OUTER_BOUND('',#7160,.T.);
#5925=FACE_OUTER_BOUND('',#7161,.T.);
#5926=FACE_OUTER_BOUND('',#7162,.T.);
#5927=FACE_OUTER_BOUND('',#7163,.T.);
#5928=FACE_OUTER_BOUND('',#7164,.T.);
#5929=FACE_OUTER_BOUND('',#7165,.T.);
#5930=FACE_OUTER_BOUND('',#7166,.T.);
#5931=FACE_OUTER_BOUND('',#7167,.T.);
#5932=FACE_OUTER_BOUND('',#7168,.T.);
#5933=FACE_OUTER_BOUND('',#7169,.T.);
#5934=FACE_OUTER_BOUND('',#7170,.T.);
#5935=FACE_OUTER_BOUND('',#7171,.T.);
#5936=FACE_OUTER_BOUND('',#7172,.T.);
#5937=FACE_OUTER_BOUND('',#7173,.T.);
#5938=FACE_OUTER_BOUND('',#7174,.T.);
#5939=FACE_OUTER_BOUND('',#7175,.T.);
#5940=FACE_OUTER_BOUND('',#7176,.T.);
#5941=FACE_OUTER_BOUND('',#7177,.T.);
#5942=FACE_OUTER_BOUND('',#7178,.T.);
#5943=FACE_OUTER_BOUND('',#7179,.T.);
#5944=FACE_OUTER_BOUND('',#7180,.T.);
#5945=FACE_OUTER_BOUND('',#7181,.T.);
#5946=FACE_OUTER_BOUND('',#7182,.T.);
#5947=FACE_OUTER_BOUND('',#7183,.T.);
#5948=FACE_OUTER_BOUND('',#7184,.T.);
#5949=FACE_OUTER_BOUND('',#7185,.T.);
#5950=FACE_OUTER_BOUND('',#7186,.T.);
#5951=FACE_OUTER_BOUND('',#7187,.T.);
#5952=FACE_OUTER_BOUND('',#7188,.T.);
#5953=FACE_OUTER_BOUND('',#7189,.T.);
#5954=FACE_OUTER_BOUND('',#7190,.T.);
#5955=FACE_OUTER_BOUND('',#7191,.T.);
#5956=FACE_OUTER_BOUND('',#7192,.T.);
#5957=FACE_OUTER_BOUND('',#7193,.T.);
#5958=FACE_OUTER_BOUND('',#7194,.T.);
#5959=FACE_OUTER_BOUND('',#7195,.T.);
#5960=FACE_OUTER_BOUND('',#7196,.T.);
#5961=FACE_OUTER_BOUND('',#7197,.T.);
#5962=FACE_OUTER_BOUND('',#7198,.T.);
#5963=FACE_OUTER_BOUND('',#7199,.T.);
#5964=FACE_OUTER_BOUND('',#7200,.T.);
#5965=FACE_OUTER_BOUND('',#7201,.T.);
#5966=FACE_OUTER_BOUND('',#7202,.T.);
#5967=FACE_OUTER_BOUND('',#7203,.T.);
#5968=FACE_OUTER_BOUND('',#7204,.T.);
#5969=FACE_OUTER_BOUND('',#7205,.T.);
#5970=FACE_OUTER_BOUND('',#7206,.T.);
#5971=FACE_OUTER_BOUND('',#7207,.T.);
#5972=FACE_OUTER_BOUND('',#7208,.T.);
#5973=FACE_OUTER_BOUND('',#7209,.T.);
#5974=FACE_OUTER_BOUND('',#7210,.T.);
#5975=FACE_OUTER_BOUND('',#7211,.T.);
#5976=FACE_OUTER_BOUND('',#7212,.T.);
#5977=FACE_OUTER_BOUND('',#7213,.T.);
#5978=FACE_OUTER_BOUND('',#7214,.T.);
#5979=FACE_OUTER_BOUND('',#7215,.T.);
#5980=FACE_OUTER_BOUND('',#7216,.T.);
#5981=FACE_OUTER_BOUND('',#7217,.T.);
#5982=FACE_OUTER_BOUND('',#7218,.T.);
#5983=FACE_OUTER_BOUND('',#7219,.T.);
#5984=FACE_OUTER_BOUND('',#7220,.T.);
#5985=FACE_OUTER_BOUND('',#7221,.T.);
#5986=FACE_OUTER_BOUND('',#7222,.T.);
#5987=FACE_OUTER_BOUND('',#7223,.T.);
#5988=FACE_OUTER_BOUND('',#7224,.T.);
#5989=FACE_OUTER_BOUND('',#7225,.T.);
#5990=FACE_OUTER_BOUND('',#7227,.T.);
#5991=FACE_OUTER_BOUND('',#7228,.T.);
#5992=FACE_OUTER_BOUND('',#7229,.T.);
#5993=FACE_OUTER_BOUND('',#7230,.T.);
#5994=FACE_OUTER_BOUND('',#7231,.T.);
#5995=FACE_OUTER_BOUND('',#7232,.T.);
#5996=FACE_OUTER_BOUND('',#7233,.T.);
#5997=FACE_OUTER_BOUND('',#7234,.T.);
#5998=FACE_OUTER_BOUND('',#7235,.T.);
#5999=FACE_OUTER_BOUND('',#7236,.T.);
#6000=FACE_OUTER_BOUND('',#7237,.T.);
#6001=FACE_OUTER_BOUND('',#7238,.T.);
#6002=FACE_OUTER_BOUND('',#7239,.T.);
#6003=FACE_OUTER_BOUND('',#7240,.T.);
#6004=FACE_OUTER_BOUND('',#7241,.T.);
#6963=EDGE_LOOP('',(#16737,#16738,#16739,#16740));
#6964=EDGE_LOOP('',(#16741,#16742));
#6965=EDGE_LOOP('',(#16743,#16744,#16745,#16746,#16747));
#6966=EDGE_LOOP('',(#16748,#16749,#16750));
#6967=EDGE_LOOP('',(#16751,#16752,#16753,#16754,#16755));
#6968=EDGE_LOOP('',(#16756,#16757,#16758,#16759));
#6969=EDGE_LOOP('',(#16760,#16761,#16762,#16763,#16764));
#6970=EDGE_LOOP('',(#16765,#16766,#16767,#16768));
#6971=EDGE_LOOP('',(#16769,#16770,#16771,#16772,#16773));
#6972=EDGE_LOOP('',(#16774,#16775,#16776));
#6973=EDGE_LOOP('',(#16777,#16778,#16779,#16780));
#6974=EDGE_LOOP('',(#16781,#16782,#16783,#16784));
#6975=EDGE_LOOP('',(#16785,#16786,#16787,#16788));
#6976=EDGE_LOOP('',(#16789,#16790,#16791,#16792,#16793,#16794,#16795,#16796,
#16797,#16798,#16799,#16800,#16801,#16802,#16803,#16804,#16805,#16806,#16807,
#16808));
#6977=EDGE_LOOP('',(#16809,#16810,#16811,#16812,#16813));
#6978=EDGE_LOOP('',(#16814,#16815,#16816,#16817));
#6979=EDGE_LOOP('',(#16818,#16819,#16820,#16821,#16822,#16823,#16824,#16825,
#16826,#16827,#16828,#16829,#16830,#16831,#16832));
#6980=EDGE_LOOP('',(#16833,#16834,#16835,#16836));
#6981=EDGE_LOOP('',(#16837,#16838,#16839,#16840));
#6982=EDGE_LOOP('',(#16841,#16842,#16843,#16844));
#6983=EDGE_LOOP('',(#16845,#16846,#16847,#16848,#16849,#16850,#16851,#16852,
#16853));
#6984=EDGE_LOOP('',(#16854,#16855,#16856,#16857,#16858));
#6985=EDGE_LOOP('',(#16859,#16860,#16861,#16862,#16863,#16864));
#6986=EDGE_LOOP('',(#16865,#16866,#16867,#16868,#16869));
#6987=EDGE_LOOP('',(#16870,#16871,#16872,#16873,#16874,#16875,#16876,#16877));
#6988=EDGE_LOOP('',(#16878,#16879,#16880,#16881,#16882));
#6989=EDGE_LOOP('',(#16883,#16884,#16885,#16886));
#6990=EDGE_LOOP('',(#16887,#16888,#16889,#16890,#16891));
#6991=EDGE_LOOP('',(#16892,#16893,#16894));
#6992=EDGE_LOOP('',(#16895,#16896,#16897));
#6993=EDGE_LOOP('',(#16898,#16899,#16900,#16901,#16902,#16903));
#6994=EDGE_LOOP('',(#16904,#16905,#16906,#16907));
#6995=EDGE_LOOP('',(#16908,#16909,#16910,#16911,#16912,#16913,#16914,#16915,
#16916,#16917));
#6996=EDGE_LOOP('',(#16918,#16919,#16920,#16921));
#6997=EDGE_LOOP('',(#16922,#16923,#16924,#16925,#16926,#16927));
#6998=EDGE_LOOP('',(#16928,#16929,#16930,#16931));
#6999=EDGE_LOOP('',(#16932,#16933,#16934,#16935,#16936));
#7000=EDGE_LOOP('',(#16937,#16938,#16939,#16940,#16941));
#7001=EDGE_LOOP('',(#16942,#16943,#16944,#16945,#16946));
#7002=EDGE_LOOP('',(#16947,#16948,#16949,#16950));
#7003=EDGE_LOOP('',(#16951,#16952,#16953,#16954));
#7004=EDGE_LOOP('',(#16955,#16956,#16957,#16958,#16959,#16960,#16961,#16962,
#16963,#16964,#16965,#16966,#16967,#16968,#16969,#16970,#16971,#16972,#16973,
#16974));
#7005=EDGE_LOOP('',(#16975,#16976));
#7006=EDGE_LOOP('',(#16977));
#7007=EDGE_LOOP('',(#16978,#16979,#16980,#16981,#16982));
#7008=EDGE_LOOP('',(#16983,#16984,#16985,#16986,#16987,#16988));
#7009=EDGE_LOOP('',(#16989,#16990,#16991,#16992,#16993));
#7010=EDGE_LOOP('',(#16994,#16995,#16996,#16997,#16998,#16999));
#7011=EDGE_LOOP('',(#17000));
#7012=EDGE_LOOP('',(#17001,#17002,#17003,#17004));
#7013=EDGE_LOOP('',(#17005));
#7014=EDGE_LOOP('',(#17006,#17007,#17008,#17009,#17010));
#7015=EDGE_LOOP('',(#17011,#17012,#17013,#17014));
#7016=EDGE_LOOP('',(#17015,#17016,#17017,#17018));
#7017=EDGE_LOOP('',(#17019,#17020,#17021));
#7018=EDGE_LOOP('',(#17022,#17023,#17024));
#7019=EDGE_LOOP('',(#17025,#17026,#17027,#17028));
#7020=EDGE_LOOP('',(#17029,#17030,#17031));
#7021=EDGE_LOOP('',(#17032,#17033,#17034,#17035,#17036,#17037));
#7022=EDGE_LOOP('',(#17038,#17039,#17040,#17041));
#7023=EDGE_LOOP('',(#17042,#17043,#17044,#17045,#17046));
#7024=EDGE_LOOP('',(#17047,#17048,#17049,#17050));
#7025=EDGE_LOOP('',(#17051,#17052,#17053,#17054,#17055,#17056,#17057));
#7026=EDGE_LOOP('',(#17058,#17059,#17060,#17061,#17062,#17063,#17064,#17065,
#17066,#17067,#17068,#17069,#17070,#17071,#17072,#17073,#17074,#17075));
#7027=EDGE_LOOP('',(#17076,#17077,#17078,#17079,#17080,#17081,#17082,#17083,
#17084));
#7028=EDGE_LOOP('',(#17085,#17086,#17087,#17088,#17089,#17090,#17091,#17092));
#7029=EDGE_LOOP('',(#17093,#17094,#17095,#17096));
#7030=EDGE_LOOP('',(#17097,#17098,#17099,#17100));
#7031=EDGE_LOOP('',(#17101,#17102,#17103));
#7032=EDGE_LOOP('',(#17104,#17105,#17106,#17107));
#7033=EDGE_LOOP('',(#17108,#17109,#17110));
#7034=EDGE_LOOP('',(#17111,#17112,#17113,#17114));
#7035=EDGE_LOOP('',(#17115,#17116,#17117,#17118,#17119,#17120,#17121,#17122,
#17123,#17124,#17125,#17126,#17127));
#7036=EDGE_LOOP('',(#17128));
#7037=EDGE_LOOP('',(#17129,#17130,#17131,#17132,#17133,#17134,#17135));
#7038=EDGE_LOOP('',(#17136,#17137,#17138,#17139,#17140,#17141));
#7039=EDGE_LOOP('',(#17142,#17143,#17144,#17145,#17146));
#7040=EDGE_LOOP('',(#17147,#17148,#17149,#17150,#17151));
#7041=EDGE_LOOP('',(#17152,#17153,#17154,#17155,#17156));
#7042=EDGE_LOOP('',(#17157,#17158,#17159,#17160,#17161,#17162,#17163));
#7043=EDGE_LOOP('',(#17164));
#7044=EDGE_LOOP('',(#17165,#17166,#17167,#17168));
#7045=EDGE_LOOP('',(#17169,#17170,#17171,#17172,#17173,#17174));
#7046=EDGE_LOOP('',(#17175,#17176,#17177,#17178,#17179,#17180));
#7047=EDGE_LOOP('',(#17181,#17182,#17183,#17184));
#7048=EDGE_LOOP('',(#17185,#17186,#17187,#17188));
#7049=EDGE_LOOP('',(#17189,#17190,#17191,#17192,#17193));
#7050=EDGE_LOOP('',(#17194,#17195,#17196,#17197,#17198,#17199,#17200,#17201));
#7051=EDGE_LOOP('',(#17202,#17203,#17204,#17205,#17206));
#7052=EDGE_LOOP('',(#17207,#17208,#17209,#17210,#17211,#17212));
#7053=EDGE_LOOP('',(#17213,#17214,#17215,#17216));
#7054=EDGE_LOOP('',(#17217,#17218,#17219,#17220));
#7055=EDGE_LOOP('',(#17221,#17222,#17223));
#7056=EDGE_LOOP('',(#17224,#17225,#17226,#17227));
#7057=EDGE_LOOP('',(#17228,#17229,#17230));
#7058=EDGE_LOOP('',(#17231,#17232,#17233,#17234,#17235,#17236,#17237,#17238,
#17239,#17240,#17241,#17242,#17243,#17244,#17245,#17246,#17247,#17248,#17249,
#17250,#17251,#17252,#17253,#17254,#17255,#17256,#17257,#17258,#17259,#17260,
#17261,#17262,#17263,#17264));
#7059=EDGE_LOOP('',(#17265,#17266,#17267,#17268));
#7060=EDGE_LOOP('',(#17269,#17270,#17271,#17272,#17273,#17274));
#7061=EDGE_LOOP('',(#17275));
#7062=EDGE_LOOP('',(#17276));
#7063=EDGE_LOOP('',(#17277,#17278,#17279,#17280));
#7064=EDGE_LOOP('',(#17281,#17282,#17283,#17284));
#7065=EDGE_LOOP('',(#17285,#17286,#17287,#17288,#17289,#17290));
#7066=EDGE_LOOP('',(#17291,#17292,#17293,#17294,#17295,#17296));
#7067=EDGE_LOOP('',(#17297,#17298,#17299,#17300));
#7068=EDGE_LOOP('',(#17301,#17302,#17303,#17304,#17305));
#7069=EDGE_LOOP('',(#17306,#17307,#17308,#17309));
#7070=EDGE_LOOP('',(#17310,#17311,#17312,#17313));
#7071=EDGE_LOOP('',(#17314,#17315,#17316,#17317));
#7072=EDGE_LOOP('',(#17318,#17319,#17320,#17321,#17322,#17323,#17324));
#7073=EDGE_LOOP('',(#17325,#17326,#17327,#17328));
#7074=EDGE_LOOP('',(#17329,#17330,#17331));
#7075=EDGE_LOOP('',(#17332,#17333,#17334,#17335,#17336,#17337,#17338));
#7076=EDGE_LOOP('',(#17339,#17340,#17341,#17342));
#7077=EDGE_LOOP('',(#17343,#17344,#17345,#17346));
#7078=EDGE_LOOP('',(#17347,#17348,#17349,#17350));
#7079=EDGE_LOOP('',(#17351,#17352,#17353));
#7080=EDGE_LOOP('',(#17354,#17355,#17356,#17357,#17358));
#7081=EDGE_LOOP('',(#17359,#17360,#17361,#17362,#17363,#17364,#17365,#17366));
#7082=EDGE_LOOP('',(#17367,#17368,#17369,#17370,#17371));
#7083=EDGE_LOOP('',(#17372,#17373,#17374,#17375));
#7084=EDGE_LOOP('',(#17376,#17377,#17378,#17379,#17380));
#7085=EDGE_LOOP('',(#17381,#17382,#17383,#17384,#17385,#17386,#17387));
#7086=EDGE_LOOP('',(#17388));
#7087=EDGE_LOOP('',(#17389,#17390,#17391,#17392,#17393,#17394));
#7088=EDGE_LOOP('',(#17395,#17396,#17397,#17398,#17399,#17400));
#7089=EDGE_LOOP('',(#17401,#17402,#17403,#17404,#17405));
#7090=EDGE_LOOP('',(#17406,#17407,#17408,#17409,#17410,#17411,#17412));
#7091=EDGE_LOOP('',(#17413));
#7092=EDGE_LOOP('',(#17414,#17415,#17416,#17417));
#7093=EDGE_LOOP('',(#17418,#17419,#17420,#17421));
#7094=EDGE_LOOP('',(#17422,#17423,#17424,#17425));
#7095=EDGE_LOOP('',(#17426,#17427,#17428,#17429));
#7096=EDGE_LOOP('',(#17430,#17431,#17432,#17433));
#7097=EDGE_LOOP('',(#17434,#17435,#17436,#17437));
#7098=EDGE_LOOP('',(#17438,#17439,#17440,#17441,#17442,#17443,#17444,#17445,
#17446,#17447));
#7099=EDGE_LOOP('',(#17448,#17449,#17450,#17451));
#7100=EDGE_LOOP('',(#17452,#17453,#17454,#17455,#17456,#17457));
#7101=EDGE_LOOP('',(#17458,#17459,#17460,#17461));
#7102=EDGE_LOOP('',(#17462,#17463,#17464,#17465));
#7103=EDGE_LOOP('',(#17466,#17467,#17468,#17469));
#7104=EDGE_LOOP('',(#17470,#17471,#17472,#17473,#17474,#17475));
#7105=EDGE_LOOP('',(#17476,#17477,#17478,#17479));
#7106=EDGE_LOOP('',(#17480,#17481,#17482,#17483,#17484,#17485));
#7107=EDGE_LOOP('',(#17486,#17487,#17488,#17489));
#7108=EDGE_LOOP('',(#17490,#17491,#17492,#17493,#17494,#17495));
#7109=EDGE_LOOP('',(#17496,#17497,#17498,#17499,#17500,#17501,#17502));
#7110=EDGE_LOOP('',(#17503,#17504,#17505,#17506,#17507,#17508));
#7111=EDGE_LOOP('',(#17509,#17510,#17511,#17512,#17513,#17514,#17515));
#7112=EDGE_LOOP('',(#17516,#17517,#17518,#17519));
#7113=EDGE_LOOP('',(#17520,#17521,#17522,#17523));
#7114=EDGE_LOOP('',(#17524,#17525,#17526,#17527));
#7115=EDGE_LOOP('',(#17528,#17529,#17530,#17531));
#7116=EDGE_LOOP('',(#17532,#17533,#17534,#17535));
#7117=EDGE_LOOP('',(#17536,#17537,#17538,#17539));
#7118=EDGE_LOOP('',(#17540,#17541,#17542,#17543));
#7119=EDGE_LOOP('',(#17544,#17545,#17546,#17547));
#7120=EDGE_LOOP('',(#17548,#17549,#17550,#17551,#17552));
#7121=EDGE_LOOP('',(#17553,#17554,#17555,#17556,#17557));
#7122=EDGE_LOOP('',(#17558,#17559,#17560,#17561,#17562));
#7123=EDGE_LOOP('',(#17563,#17564,#17565,#17566,#17567));
#7124=EDGE_LOOP('',(#17568,#17569,#17570,#17571,#17572));
#7125=EDGE_LOOP('',(#17573,#17574,#17575,#17576,#17577,#17578));
#7126=EDGE_LOOP('',(#17579,#17580,#17581,#17582,#17583,#17584,#17585));
#7127=EDGE_LOOP('',(#17586,#17587,#17588,#17589,#17590,#17591));
#7128=EDGE_LOOP('',(#17592,#17593,#17594,#17595,#17596));
#7129=EDGE_LOOP('',(#17597,#17598,#17599,#17600,#17601,#17602,#17603,#17604,
#17605,#17606,#17607,#17608,#17609));
#7130=EDGE_LOOP('',(#17610));
#7131=EDGE_LOOP('',(#17611,#17612,#17613,#17614));
#7132=EDGE_LOOP('',(#17615,#17616,#17617,#17618));
#7133=EDGE_LOOP('',(#17619,#17620,#17621));
#7134=EDGE_LOOP('',(#17622,#17623,#17624));
#7135=EDGE_LOOP('',(#17625,#17626,#17627,#17628));
#7136=EDGE_LOOP('',(#17629,#17630,#17631,#17632));
#7137=EDGE_LOOP('',(#17633,#17634,#17635,#17636));
#7138=EDGE_LOOP('',(#17637,#17638,#17639));
#7139=EDGE_LOOP('',(#17640,#17641,#17642,#17643,#17644,#17645,#17646,#17647,
#17648,#17649,#17650));
#7140=EDGE_LOOP('',(#17651,#17652,#17653,#17654));
#7141=EDGE_LOOP('',(#17655,#17656,#17657,#17658,#17659));
#7142=EDGE_LOOP('',(#17660,#17661,#17662,#17663));
#7143=EDGE_LOOP('',(#17664,#17665,#17666,#17667,#17668));
#7144=EDGE_LOOP('',(#17669,#17670,#17671));
#7145=EDGE_LOOP('',(#17672,#17673,#17674));
#7146=EDGE_LOOP('',(#17675,#17676,#17677,#17678,#17679,#17680));
#7147=EDGE_LOOP('',(#17681,#17682,#17683,#17684));
#7148=EDGE_LOOP('',(#17685,#17686,#17687,#17688));
#7149=EDGE_LOOP('',(#17689,#17690,#17691,#17692));
#7150=EDGE_LOOP('',(#17693,#17694,#17695));
#7151=EDGE_LOOP('',(#17696,#17697,#17698,#17699,#17700));
#7152=EDGE_LOOP('',(#17701,#17702,#17703,#17704,#17705,#17706,#17707,#17708,
#17709,#17710,#17711,#17712,#17713,#17714,#17715,#17716,#17717,#17718,#17719,
#17720));
#7153=EDGE_LOOP('',(#17721,#17722,#17723,#17724,#17725,#17726));
#7154=EDGE_LOOP('',(#17727));
#7155=EDGE_LOOP('',(#17728));
#7156=EDGE_LOOP('',(#17729,#17730,#17731,#17732));
#7157=EDGE_LOOP('',(#17733,#17734,#17735,#17736));
#7158=EDGE_LOOP('',(#17737,#17738,#17739,#17740,#17741,#17742));
#7159=EDGE_LOOP('',(#17743,#17744,#17745,#17746));
#7160=EDGE_LOOP('',(#17747,#17748,#17749,#17750,#17751,#17752,#17753));
#7161=EDGE_LOOP('',(#17754,#17755,#17756,#17757));
#7162=EDGE_LOOP('',(#17758,#17759,#17760,#17761,#17762,#17763));
#7163=EDGE_LOOP('',(#17764,#17765,#17766,#17767,#17768,#17769,#17770,#17771,
#17772,#17773,#17774,#17775,#17776,#17777));
#7164=EDGE_LOOP('',(#17778,#17779,#17780,#17781));
#7165=EDGE_LOOP('',(#17782,#17783,#17784,#17785));
#7166=EDGE_LOOP('',(#17786,#17787,#17788,#17789,#17790));
#7167=EDGE_LOOP('',(#17791,#17792,#17793,#17794,#17795,#17796,#17797,#17798,
#17799,#17800));
#7168=EDGE_LOOP('',(#17801,#17802,#17803,#17804,#17805,#17806,#17807));
#7169=EDGE_LOOP('',(#17808,#17809,#17810,#17811,#17812,#17813));
#7170=EDGE_LOOP('',(#17814,#17815,#17816,#17817));
#7171=EDGE_LOOP('',(#17818,#17819,#17820,#17821,#17822,#17823,#17824,#17825));
#7172=EDGE_LOOP('',(#17826,#17827,#17828,#17829));
#7173=EDGE_LOOP('',(#17830,#17831,#17832,#17833,#17834,#17835,#17836,#17837));
#7174=EDGE_LOOP('',(#17838,#17839,#17840,#17841));
#7175=EDGE_LOOP('',(#17842,#17843,#17844,#17845));
#7176=EDGE_LOOP('',(#17846,#17847,#17848,#17849));
#7177=EDGE_LOOP('',(#17850,#17851,#17852));
#7178=EDGE_LOOP('',(#17853,#17854,#17855));
#7179=EDGE_LOOP('',(#17856,#17857,#17858,#17859,#17860,#17861,#17862,#17863,
#17864,#17865,#17866,#17867,#17868,#17869));
#7180=EDGE_LOOP('',(#17870,#17871,#17872,#17873));
#7181=EDGE_LOOP('',(#17874,#17875,#17876,#17877,#17878,#17879));
#7182=EDGE_LOOP('',(#17880,#17881,#17882,#17883));
#7183=EDGE_LOOP('',(#17884,#17885,#17886,#17887,#17888));
#7184=EDGE_LOOP('',(#17889,#17890,#17891,#17892,#17893));
#7185=EDGE_LOOP('',(#17894,#17895,#17896,#17897));
#7186=EDGE_LOOP('',(#17898,#17899,#17900,#17901,#17902));
#7187=EDGE_LOOP('',(#17903,#17904,#17905,#17906,#17907));
#7188=EDGE_LOOP('',(#17908,#17909,#17910,#17911));
#7189=EDGE_LOOP('',(#17912,#17913,#17914,#17915));
#7190=EDGE_LOOP('',(#17916,#17917,#17918,#17919,#17920,#17921,#17922));
#7191=EDGE_LOOP('',(#17923,#17924,#17925,#17926));
#7192=EDGE_LOOP('',(#17927,#17928,#17929,#17930));
#7193=EDGE_LOOP('',(#17931,#17932,#17933,#17934,#17935,#17936));
#7194=EDGE_LOOP('',(#17937,#17938,#17939,#17940));
#7195=EDGE_LOOP('',(#17941,#17942,#17943,#17944,#17945,#17946));
#7196=EDGE_LOOP('',(#17947,#17948,#17949,#17950));
#7197=EDGE_LOOP('',(#17951,#17952,#17953,#17954));
#7198=EDGE_LOOP('',(#17955,#17956,#17957,#17958,#17959));
#7199=EDGE_LOOP('',(#17960,#17961,#17962,#17963,#17964,#17965,#17966,#17967,
#17968,#17969));
#7200=EDGE_LOOP('',(#17970,#17971,#17972,#17973));
#7201=EDGE_LOOP('',(#17974,#17975,#17976,#17977));
#7202=EDGE_LOOP('',(#17978,#17979,#17980,#17981,#17982));
#7203=EDGE_LOOP('',(#17983,#17984,#17985,#17986,#17987));
#7204=EDGE_LOOP('',(#17988,#17989,#17990,#17991,#17992));
#7205=EDGE_LOOP('',(#17993,#17994,#17995,#17996));
#7206=EDGE_LOOP('',(#17997,#17998,#17999,#18000));
#7207=EDGE_LOOP('',(#18001,#18002,#18003,#18004));
#7208=EDGE_LOOP('',(#18005,#18006,#18007,#18008));
#7209=EDGE_LOOP('',(#18009,#18010,#18011));
#7210=EDGE_LOOP('',(#18012,#18013,#18014,#18015));
#7211=EDGE_LOOP('',(#18016,#18017,#18018,#18019,#18020));
#7212=EDGE_LOOP('',(#18021,#18022,#18023,#18024));
#7213=EDGE_LOOP('',(#18025,#18026,#18027,#18028));
#7214=EDGE_LOOP('',(#18029,#18030,#18031));
#7215=EDGE_LOOP('',(#18032,#18033,#18034,#18035));
#7216=EDGE_LOOP('',(#18036,#18037,#18038,#18039,#18040,#18041));
#7217=EDGE_LOOP('',(#18042,#18043,#18044,#18045));
#7218=EDGE_LOOP('',(#18046,#18047,#18048,#18049));
#7219=EDGE_LOOP('',(#18050,#18051,#18052));
#7220=EDGE_LOOP('',(#18053,#18054,#18055,#18056));
#7221=EDGE_LOOP('',(#18057,#18058,#18059,#18060));
#7222=EDGE_LOOP('',(#18061,#18062,#18063,#18064,#18065,#18066));
#7223=EDGE_LOOP('',(#18067,#18068,#18069,#18070,#18071));
#7224=EDGE_LOOP('',(#18072,#18073,#18074));
#7225=EDGE_LOOP('',(#18075));
#7226=EDGE_LOOP('',(#18076));
#7227=EDGE_LOOP('',(#18077));
#7228=EDGE_LOOP('',(#18078));
#7229=EDGE_LOOP('',(#18079));
#7230=EDGE_LOOP('',(#18080,#18081,#18082,#18083));
#7231=EDGE_LOOP('',(#18084,#18085,#18086,#18087));
#7232=EDGE_LOOP('',(#18088,#18089,#18090,#18091));
#7233=EDGE_LOOP('',(#18092,#18093,#18094,#18095));
#7234=EDGE_LOOP('',(#18096,#18097,#18098,#18099));
#7235=EDGE_LOOP('',(#18100,#18101,#18102,#18103));
#7236=EDGE_LOOP('',(#18104,#18105,#18106,#18107,#18108,#18109));
#7237=EDGE_LOOP('',(#18110,#18111,#18112,#18113));
#7238=EDGE_LOOP('',(#18114,#18115,#18116,#18117,#18118,#18119,#18120,#18121,
#18122,#18123));
#7239=EDGE_LOOP('',(#18124,#18125,#18126,#18127));
#7240=EDGE_LOOP('',(#18128,#18129,#18130,#18131));
#7241=EDGE_LOOP('',(#18132,#18133,#18134,#18135,#18136));
#7928=B_SPLINE_CURVE_WITH_KNOTS('',3,(#90986,#90987,#90988,#90989,#90990,
#90991,#90992,#90993,#90994,#90995),.UNSPECIFIED.,.F.,.F.,(4,2,2,2,4),(0.,
0.0198203077394276,0.0433989762369911,0.0727052081845461,0.108839631579722),
 .UNSPECIFIED.);
#7929=B_SPLINE_CURVE_WITH_KNOTS('',3,(#90999,#91000,#91001,#91002,#91003,
#91004,#91005,#91006,#91007,#91008),.UNSPECIFIED.,.F.,.F.,(4,2,2,2,4),(0.335564963946802,
0.371699387341978,0.401005619289533,0.424584287787096,0.444404595526524),
 .UNSPECIFIED.);
#7930=B_SPLINE_CURVE_WITH_KNOTS('',3,(#91015,#91016,#91017,#91018,#91019,
#91020,#91021,#91022,#91023,#91024,#91025,#91026),.UNSPECIFIED.,.F.,.F.,
(4,2,2,2,2,4),(0.,0.00831861880117899,0.0174994849977743,0.0424016409784866,
0.0803702669813532,0.139810685907233),.UNSPECIFIED.);
#7931=B_SPLINE_CURVE_WITH_KNOTS('',3,(#91030,#91031,#91032,#91033,#91034,
#91035,#91036,#91037),.UNSPECIFIED.,.F.,.F.,(4,2,2,4),(0.567555107088231,
0.577206887836704,0.594334223162494,0.613200757592396),.UNSPECIFIED.);
#7932=B_SPLINE_CURVE_WITH_KNOTS('',3,(#91039,#91040,#91041,#91042,#91043,
#91044,#91045,#91046),.UNSPECIFIED.,.F.,.F.,(4,2,2,4),(0.268421316333155,
0.291025391015721,0.313464123275544,0.318616532882621),.UNSPECIFIED.);
#7933=B_SPLINE_CURVE_WITH_KNOTS('',3,(#91057,#91058,#91059,#91060,#91061,
#91062,#91063,#91064),.UNSPECIFIED.,.F.,.F.,(4,2,2,4),(-0.373632853319188,
-0.370925235245078,-0.34375119436819,-0.312176495568083),.UNSPECIFIED.);
#7934=B_SPLINE_CURVE_WITH_KNOTS('',3,(#91066,#91067,#91068,#91069,#91070,
#91071,#91072,#91073),.UNSPECIFIED.,.F.,.F.,(4,2,2,4),(0.102055810558895,
0.10300662226153,0.123623520705077,0.14314601433674),.UNSPECIFIED.);
#7935=B_SPLINE_CURVE_WITH_KNOTS('',3,(#91076,#91077,#91078,#91079,#91080,
#91081,#91082,#91083,#91084,#91085,#91086,#91087,#91088,#91089,#91090,#91091,
#91092,#91093,#91094,#91095,#91096,#91097,#91098,#91099,#91100,#91101,#91102,
#91103),.UNSPECIFIED.,.F.,.F.,(4,3,3,3,3,3,3,3,3,4),(0.,0.0144825766165643,
0.0225740708747328,0.0346938168103142,0.0456054571019101,0.0576817551653054,
0.0695937263660513,0.0828019048720541,0.0960623063922353,0.0964246649222208),
 .UNSPECIFIED.);
#7936=B_SPLINE_CURVE_WITH_KNOTS('',3,(#91109,#91110,#91111,#91112,#91113,
#91114,#91115,#91116,#91117,#91118,#91119,#91120,#91121,#91122,#91123,#91124,
#91125,#91126,#91127,#91128,#91129,#91130,#91131,#91132,#91133,#91134,#91135,
#91136),.UNSPECIFIED.,.F.,.F.,(4,3,3,3,3,3,3,3,3,4),(-0.0962049341565272,
-0.0817008546465319,-0.0735973466051622,-0.0614596059708162,-0.0505317647059319,
-0.0384375364526582,-0.0265078790450698,-0.013280089798481,0.,0.000362896539003327),
 .UNSPECIFIED.);
#7937=B_SPLINE_CURVE_WITH_KNOTS('',3,(#91141,#91142,#91143,#91144,#91145,
#91146,#91147,#91148),.UNSPECIFIED.,.F.,.F.,(4,2,2,4),(0.620143406782201,
0.624498876460084,0.646574469367965,0.671320484075565),.UNSPECIFIED.);
#7938=B_SPLINE_CURVE_WITH_KNOTS('',3,(#91150,#91151,#91152,#91153,#91154,
#91155,#91156,#91157),.UNSPECIFIED.,.F.,.F.,(4,2,2,4),(-0.102413024431803,
-0.0708383256316961,-0.0436642847548089,-0.0409566666806992),
 .UNSPECIFIED.);
#7939=B_SPLINE_CURVE_WITH_KNOTS('',3,(#91164,#91165,#91166,#91167,#91168,
#91169,#91170,#91171),.UNSPECIFIED.,.F.,.F.,(4,2,2,4),(0.105220546930268,
0.118812208671315,0.137355851603631,0.150522503003572),.UNSPECIFIED.);
#7940=B_SPLINE_CURVE_WITH_KNOTS('',3,(#91175,#91176,#91177,#91178,#91179,
#91180,#91181,#91182,#91183,#91184,#91185,#91186),.UNSPECIFIED.,.F.,.F.,
(4,2,2,2,2,4),(0.481937503575851,0.54137792250173,0.579346548504597,0.604248704485309,
0.613429570681904,0.621748189483083),.UNSPECIFIED.);
#7941=B_SPLINE_CURVE_WITH_KNOTS('',3,(#91189,#91190,#91191,#91192,#91193,
#91194,#91195,#91196),.UNSPECIFIED.,.F.,.F.,(4,2,2,4),(0.0392364555962475,
0.0443888652033245,0.066827597463148,0.0894316721457135),.UNSPECIFIED.);
#7942=B_SPLINE_CURVE_WITH_KNOTS('',3,(#91255,#91256,#91257,#91258,#91259,
#91260,#91261,#91262,#91263,#91264),.UNSPECIFIED.,.F.,.F.,(4,2,2,2,4),(0.198387340813371,
0.203960430205622,0.218045744690312,0.232131059175001,0.241802651428953),
 .UNSPECIFIED.);
#7943=B_SPLINE_CURVE_WITH_KNOTS('',3,(#91281,#91282,#91283,#91284,#91285,
#91286),.UNSPECIFIED.,.F.,.F.,(4,2,4),(0.00719864469771614,0.0137080667973639,
0.0162984458358511),.UNSPECIFIED.);
#7944=B_SPLINE_CURVE_WITH_KNOTS('',3,(#91292,#91293,#91294,#91295,#91296,
#91297,#91298,#91299,#91300,#91301,#91302,#91303,#91304,#91305,#91306,#91307,
#91308,#91309,#91310),.UNSPECIFIED.,.F.,.F.,(4,2,2,2,3,2,2,2,4),(0.582619764185682,
0.587048813927463,0.608772997184351,0.63176112026293,0.65474924334151,0.67542743189983,
0.69610562045815,0.716170507416666,0.720537010002502),.UNSPECIFIED.);
#7945=B_SPLINE_CURVE_WITH_KNOTS('',3,(#91384,#91385,#91386,#91387,#91388,
#91389),.UNSPECIFIED.,.F.,.F.,(4,2,4),(-0.209156427629457,-0.206361653740428,
-0.198150656776162),.UNSPECIFIED.);
#7946=B_SPLINE_CURVE_WITH_KNOTS('',3,(#91418,#91419,#91420,#91421,#91422,
#91423,#91424,#91425,#91426,#91427),.UNSPECIFIED.,.F.,.F.,(4,2,2,2,4),(0.0519371314826972,
0.0616087237366522,0.0756940382213414,0.0897793527060307,0.0953524420982795),
 .UNSPECIFIED.);
#7947=B_SPLINE_CURVE_WITH_KNOTS('',3,(#91484,#91485,#91486,#91487,#91488,
#91489,#91490,#91491,#91492,#91493),.UNSPECIFIED.,.F.,.F.,(4,2,2,2,4),(0.198387340813371,
0.203960430205622,0.218045744690312,0.232131059175001,0.241802651428953),
 .UNSPECIFIED.);
#7948=B_SPLINE_CURVE_WITH_KNOTS('',3,(#91509,#91510,#91511,#91512,#91513,
#91514,#91515,#91516,#91517,#91518,#91519,#91520,#91521,#91522,#91523,#91524,
#91525,#91526,#91527,#91528,#91529,#91530,#91531,#91532,#91533,#91534,#91535,
#91536),.UNSPECIFIED.,.F.,.F.,(4,3,3,3,3,3,3,3,3,4),(-0.000362896539001219,
0.,0.0132800897984686,0.0265078790450441,0.0400863342838971,0.0505317647058842,
0.0641209451936965,0.0735973466050953,0.0904711570682583,0.0962049341564403),
 .UNSPECIFIED.);
#7949=B_SPLINE_CURVE_WITH_KNOTS('',3,(#91539,#91540,#91541,#91542,#91543,
#91544,#91545,#91546,#91547,#91548,#91549,#91550,#91551,#91552,#91553,#91554,
#91555,#91556,#91557,#91558,#91559,#91560,#91561,#91562,#91563,#91564,#91565,
#91566),.UNSPECIFIED.,.F.,.F.,(4,3,3,3,3,3,3,3,3,4),(-0.0964246649222091,
-0.0960623063922242,-0.0828019048720443,-0.0695937263660441,-0.0560354017445019,
-0.0456054571019059,-0.032036423132379,-0.0225740708747317,-0.00572527652771826,
0.),.UNSPECIFIED.);
#7950=B_SPLINE_CURVE_WITH_KNOTS('',3,(#91577,#91578,#91579,#91580,#91581,
#91582,#91583,#91584),.UNSPECIFIED.,.F.,.F.,(4,2,2,4),(-0.322668635476185,
-0.317356379278157,-0.294587204940379,-0.2718180306026),.UNSPECIFIED.);
#7951=B_SPLINE_CURVE_WITH_KNOTS('',3,(#91587,#91588,#91589,#91590,#91591,
#91592,#91593,#91594),.UNSPECIFIED.,.F.,.F.,(4,2,2,4),(-0.101192488668761,
-0.073104459771632,-0.045016430874503,-0.0417266688079848),
 .UNSPECIFIED.);
#7952=B_SPLINE_CURVE_WITH_KNOTS('',3,(#91598,#91599,#91600,#91601,#91602,
#91603,#91604,#91605),.UNSPECIFIED.,.F.,.F.,(4,2,2,4),(-0.35842166827265,
-0.355131906206132,-0.327043877309003,-0.298955848411874),.UNSPECIFIED.);
#7953=B_SPLINE_CURVE_WITH_KNOTS('',3,(#91608,#91609,#91610,#91611,#91612,
#91613,#91614,#91615),.UNSPECIFIED.,.F.,.F.,(4,2,2,4),(-0.0907502340909058,
-0.0679810597531271,-0.0452118854153484,-0.0398996293942076),
 .UNSPECIFIED.);
#7954=B_SPLINE_CURVE_WITH_KNOTS('',3,(#91633,#91634,#91635,#91636,#91637,
#91638,#91639,#91640,#91641,#91642,#91643),.UNSPECIFIED.,.F.,.F.,(4,1,1,
1,1,1,1,1,4),(0.,0.177176435663881,0.354352871327763,0.531529306991644,
0.708705742655525,0.885882178319406,1.06305861398329,1.18117623775921,1.24023145903364),
 .UNSPECIFIED.);
#7955=B_SPLINE_CURVE_WITH_KNOTS('',3,(#91644,#91645,#91646,#91647,#91648,
#91649,#91650,#91651,#91652,#91653,#91654),.UNSPECIFIED.,.F.,.F.,(4,1,1,
1,1,1,1,1,4),(1.24023145903364,1.29929386153513,1.41741148531105,1.65364673286289,
1.77176435663881,1.94894079230269,2.12611722796658,2.30329366363046,2.48047009929434),
 .UNSPECIFIED.);
#7956=B_SPLINE_CURVE_WITH_KNOTS('',3,(#91765,#91766,#91767,#91768,#91769,
#91770),.UNSPECIFIED.,.F.,.F.,(4,1,1,4),(-1.,-0.571428571428571,-0.285714285714286,
0.),.UNSPECIFIED.);
#7957=B_SPLINE_CURVE_WITH_KNOTS('',3,(#91771,#91772,#91773,#91774,#91775,
#91776,#91777,#91778,#91779,#91780,#91781,#91782,#91783,#91784,#91785,#91786,
#91787,#91788),.UNSPECIFIED.,.T.,.F.,(4,1,1,1,1,1,1,1,1,1,1,1,1,1,1,4),
(-2.48047009929434,-2.30329366363046,-2.12611722796658,-1.94894079230269,
-1.77176435663881,-1.65364673286289,-1.41741148531105,-1.29929386153513,
-1.18117623775921,-1.06305861398329,-0.885882178319406,-0.708705742655525,
-0.531529306991644,-0.354352871327763,-0.177176435663881,0.),
 .UNSPECIFIED.);
#7958=B_SPLINE_CURVE_WITH_KNOTS('',3,(#91793,#91794,#91795,#91796,#91797,
#91798,#91799,#91800,#91801,#91802,#91803,#91804,#91805,#91806,#91807,#91808,
#91809,#91810),.UNSPECIFIED.,.F.,.F.,(4,2,2,2,2,2,2,2,4),(1.09281023327069,
1.11399476693488,1.22799035827166,1.26102591181177,1.27988731437487,1.29913397363528,
1.33595457523744,1.42951419043064,1.46012340372434),.UNSPECIFIED.);
#7959=B_SPLINE_CURVE_WITH_KNOTS('',3,(#91823,#91824,#91825,#91826,#91827,
#91828,#91829,#91830,#91831,#91832),.UNSPECIFIED.,.F.,.F.,(4,2,2,2,4),(0.345676914394354,
0.355348506648306,0.369433821132995,0.383519135617684,0.389092225009936),
 .UNSPECIFIED.);
#7960=B_SPLINE_CURVE_WITH_KNOTS('',3,(#91867,#91868,#91869,#91870,#91871,
#91872,#91873,#91874,#91875,#91876),.UNSPECIFIED.,.F.,.F.,(4,2,2,2,4),(-0.190661625341085,
-0.178777035039909,-0.166892444738732,-0.14312326413638,-0.130096727258007),
 .UNSPECIFIED.);
#7961=B_SPLINE_CURVE_WITH_KNOTS('',3,(#91877,#91878,#91879,#91880,#91881,
#91882),.UNSPECIFIED.,.F.,.F.,(4,2,4),(-0.130096727258007,-0.117129563552769,
-0.0911358629691591),.UNSPECIFIED.);
#7962=B_SPLINE_CURVE_WITH_KNOTS('',3,(#91907,#91908,#91909,#91910,#91911,
#91912,#91913,#91914,#91915,#91916),.UNSPECIFIED.,.F.,.F.,(4,2,2,2,4),(0.193462588866382,
0.216085589979445,0.238708591092508,0.26177940398235,0.284850216872191),
 .UNSPECIFIED.);
#7963=B_SPLINE_CURVE_WITH_KNOTS('',3,(#91935,#91936,#91937,#91938,#91939,
#91940,#91941,#91942,#91943,#91944,#91945,#91946,#91947,#91948,#91949,#91950,
#91951,#91952),.UNSPECIFIED.,.F.,.F.,(4,2,2,2,2,2,2,2,4),(-0.415205355258057,
-0.40606214045211,-0.378053329963949,-0.350044519475788,-0.294026898499466,
-0.238009277523144,-0.210000467034983,-0.181991656546822,-0.172848441740874),
 .UNSPECIFIED.);
#7964=B_SPLINE_CURVE_WITH_KNOTS('',3,(#91956,#91957,#91958,#91959,#91960,
#91961,#91962,#91963,#91964,#91965),.UNSPECIFIED.,.F.,.F.,(4,2,2,2,4),(-0.261823472878211,
-0.204378823595008,-0.175621234943912,-0.146863646292815,-0.143979996599966),
 .UNSPECIFIED.);
#7965=B_SPLINE_CURVE_WITH_KNOTS('',3,(#91966,#91967,#91968,#91969,#91970,
#91971,#91972,#91973,#91974,#91975,#91976,#91977),.UNSPECIFIED.,.F.,.F.,
(4,2,2,2,2,4),(-0.252564986900111,-0.250043378084573,-0.229478062042114,
-0.208912745999654,-0.167782113914736,-0.167733445562344),.UNSPECIFIED.);
#7966=B_SPLINE_CURVE_WITH_KNOTS('',3,(#92043,#92044,#92045,#92046,#92047,
#92048,#92049,#92050,#92051,#92052,#92053,#92054,#92055,#92056),
 .UNSPECIFIED.,.F.,.F.,(4,2,2,2,2,2,4),(-0.000843143910697069,0.,0.0635581866099015,
0.111277859499319,0.158997532388736,0.222555718998638,0.223398862910045),
 .UNSPECIFIED.);
#7967=B_SPLINE_CURVE_WITH_KNOTS('',3,(#92090,#92091,#92092,#92093,#92094,
#92095,#92096,#92097,#92098,#92099,#92100,#92101,#92102,#92103),
 .UNSPECIFIED.,.F.,.F.,(4,2,2,2,2,2,4),(-0.000843143910697069,0.,0.0635581866099015,
0.111277859499319,0.158997532388736,0.222555718998638,0.223398862910045),
 .UNSPECIFIED.);
#7968=B_SPLINE_CURVE_WITH_KNOTS('',3,(#92218,#92219,#92220,#92221,#92222,
#92223,#92224,#92225,#92226,#92227,#92228,#92229,#92230,#92231),
 .UNSPECIFIED.,.F.,.F.,(4,2,2,2,2,2,4),(-0.000843143936325221,0.,0.0635581870754678,
0.11127786061665,0.158997534157832,0.222555721233299,0.223398865170335),
 .UNSPECIFIED.);
#7969=B_SPLINE_CURVE_WITH_KNOTS('',3,(#92329,#92330,#92331,#92332,#92333,
#92334,#92335,#92336,#92337,#92338,#92339,#92340,#92341,#92342),
 .UNSPECIFIED.,.F.,.F.,(4,2,2,2,2,2,4),(-0.000843143910697069,0.,0.0635581866099015,
0.111277859499319,0.158997532388736,0.222555718998638,0.223398862910045),
 .UNSPECIFIED.);
#7970=B_SPLINE_CURVE_WITH_KNOTS('',3,(#92445,#92446,#92447,#92448,#92449,
#92450,#92451,#92452),.UNSPECIFIED.,.F.,.F.,(4,2,2,4),(-0.170972401837901,
-0.1704030415541,-0.130663926012498,-0.0852015207771597),.UNSPECIFIED.);
#7971=B_SPLINE_CURVE_WITH_KNOTS('',3,(#92453,#92454,#92455,#92456,#92457,
#92458,#92459,#92460),.UNSPECIFIED.,.F.,.F.,(4,2,2,4),(-0.0852015207771597,
-0.0397391155418221,0.,0.000569360283792102),.UNSPECIFIED.);
#7972=B_SPLINE_CURVE_WITH_KNOTS('',3,(#92533,#92534,#92535,#92536,#92537,
#92538,#92539,#92540,#92541,#92542,#92543,#92544,#92545,#92546),
 .UNSPECIFIED.,.F.,.F.,(4,2,2,2,2,2,4),(-0.000843143910697069,0.,0.0635581866099015,
0.111277859499319,0.158997532388736,0.222555718998638,0.223398862910045),
 .UNSPECIFIED.);
#7973=B_SPLINE_CURVE_WITH_KNOTS('',3,(#92647,#92648,#92649,#92650,#92651,
#92652),.UNSPECIFIED.,.F.,.F.,(4,2,4),(0.091135862969159,0.117129563552768,
0.130096727258013),.UNSPECIFIED.);
#7974=B_SPLINE_CURVE_WITH_KNOTS('',3,(#92664,#92665,#92666,#92667,#92668,
#92669,#92670,#92671,#92672,#92673,#92674,#92675,#92676,#92677,#92678,#92679,
#92680,#92681,#92682,#92683,#92684,#92685,#92686,#92687,#92688,#92689,#92690,
#92691,#92692,#92693,#92694,#92695,#92696,#92697,#92698,#92699,#92700,#92701,
#92702,#92703,#92704,#92705,#92706,#92707,#92708,#92709,#92710,#92711,#92712),
 .UNSPECIFIED.,.F.,.F.,(4,3,3,3,3,3,3,3,3,3,3,3,3,3,3,3,4),(-0.000437248893796375,
-0.000327936670347281,-0.000218624446898187,0.,0.00769621191313966,0.0157118108669416,
0.024299765927154,0.0286905322178578,0.0386811779250504,0.0500503744658259,
0.0512366156247202,0.0620983057078456,0.0708608493966852,0.0729599957909709,
0.081430010034257,0.0896747028777473,0.0949866108739304),.UNSPECIFIED.);
#7975=B_SPLINE_CURVE_WITH_KNOTS('',3,(#92720,#92721,#92722,#92723,#92724,
#92725,#92726,#92727,#92728,#92729),.UNSPECIFIED.,.F.,.F.,(4,2,2,2,4),(0.105097916683049,
0.124999987614685,0.147923775725783,0.170693182296083,0.193462588866383),
 .UNSPECIFIED.);
#7976=B_SPLINE_CURVE_WITH_KNOTS('',3,(#92731,#92732,#92733,#92734,#92735,
#92736,#92737,#92738,#92739,#92740,#92741,#92742),.UNSPECIFIED.,.F.,.F.,
(4,2,2,2,2,4),(0.190661625341083,0.202546215642259,0.214430805943435,0.238199986545788,
0.264193687129397,0.287183234818408),.UNSPECIFIED.);
#7977=B_SPLINE_CURVE_WITH_KNOTS('',3,(#92749,#92750,#92751,#92752,#92753,
#92754,#92755,#92756,#92757,#92758),.UNSPECIFIED.,.F.,.F.,(4,2,2,2,4),(0.130096727258013,
0.143123264136378,0.16689244473873,0.178777035039906,0.190661625341083),
 .UNSPECIFIED.);
#7978=B_SPLINE_CURVE_WITH_KNOTS('',3,(#92856,#92857,#92858,#92859,#92860,
#92861,#92862,#92863,#92864,#92865,#92866,#92867,#92868,#92869,#92870,#92871),
 .UNSPECIFIED.,.F.,.F.,(4,3,3,3,3,4),(-0.0505851231124638,-0.0494104061932021,
-0.0393505169387521,-0.0372626146808706,-0.0276893855942847,-0.0247052030966232),
 .UNSPECIFIED.);
#7979=B_SPLINE_CURVE_WITH_KNOTS('',3,(#92934,#92935,#92936,#92937,#92938,
#92939,#92940,#92941,#92942,#92943,#92944,#92945,#92946,#92947,#92948,#92949,
#92950,#92951,#92952,#92953,#92954,#92955),.UNSPECIFIED.,.F.,.F.,(4,3,3,
3,3,3,3,4),(-0.0474813620491253,-0.0386630667071124,-0.0351633788899156,
-0.0253798710348694,-0.0187891022782665,-0.00732222521866259,0.,0.000730628320777441),
 .UNSPECIFIED.);
#7980=B_SPLINE_CURVE_WITH_KNOTS('',3,(#92963,#92964,#92965,#92966,#92967,
#92968,#92969,#92970,#92971,#92972),.UNSPECIFIED.,.F.,.F.,(4,2,2,2,4),(-0.296437784487761,
-0.268297213606933,-0.240327871275254,-0.215765565720465,-0.195631865775833),
 .UNSPECIFIED.);
#7981=B_SPLINE_CURVE_WITH_KNOTS('',3,(#92975,#92976,#92977,#92978,#92979,
#92980,#92981,#92982,#92983,#92984),.UNSPECIFIED.,.F.,.F.,(4,2,2,2,4),(-0.195631865775833,
-0.175498165831202,-0.150935860276413,-0.122966517944734,-0.0948259470639069),
 .UNSPECIFIED.);
#7982=B_SPLINE_CURVE_WITH_KNOTS('',3,(#93014,#93015,#93016,#93017,#93018,
#93019,#93020,#93021,#93022,#93023),.UNSPECIFIED.,.F.,.F.,(4,2,2,2,4),(0.0948259470639078,
0.122966517944735,0.150935860276413,0.175498165831201,0.195631865775832),
 .UNSPECIFIED.);
#7983=B_SPLINE_CURVE_WITH_KNOTS('',3,(#93059,#93060,#93061,#93062,#93063,
#93064,#93065,#93066,#93067,#93068,#93069,#93070,#93071,#93072,#93073,#93074,
#93075,#93076,#93077,#93078,#93079,#93080,#93081,#93082,#93083,#93084,#93085,
#93086,#93087,#93088,#93089,#93090,#93091,#93092,#93093,#93094,#93095,#93096,
#93097,#93098,#93099,#93100,#93101),.UNSPECIFIED.,.F.,.F.,(4,3,3,3,3,3,
3,3,3,3,3,3,3,3,4),(0.,0.00819151153137603,0.0168429948726552,0.0224161551166588,
0.0314142253231794,0.0424572406680403,0.0446099777430671,0.0563743860269171,
0.066180614352991,0.0674313049384604,0.0761831144290232,0.0844743257223039,
0.0922212797822719,0.0946135652781465,0.0947043969996347),.UNSPECIFIED.);
#7984=B_SPLINE_CURVE_WITH_KNOTS('',3,(#93117,#93118,#93119,#93120,#93121,
#93122,#93123,#93124,#93125,#93126),.UNSPECIFIED.,.F.,.F.,(4,2,2,2,4),(-0.195631865775832,
-0.175498165831201,-0.150935860276413,-0.122966517944735,-0.0948259470639078),
 .UNSPECIFIED.);
#9276=VERTEX_POINT('',#90984);
#9277=VERTEX_POINT('',#90985);
#9278=VERTEX_POINT('',#90996);
#9279=VERTEX_POINT('',#90998);
#9280=VERTEX_POINT('',#91013);
#9281=VERTEX_POINT('',#91014);
#9282=VERTEX_POINT('',#91027);
#9283=VERTEX_POINT('',#91029);
#9284=VERTEX_POINT('',#91038);
#9285=VERTEX_POINT('',#91049);
#9286=VERTEX_POINT('',#91053);
#9287=VERTEX_POINT('',#91054);
#9288=VERTEX_POINT('',#91056);
#9289=VERTEX_POINT('',#91065);
#9290=VERTEX_POINT('',#91074);
#9291=VERTEX_POINT('',#91105);
#9292=VERTEX_POINT('',#91107);
#9293=VERTEX_POINT('',#91138);
#9294=VERTEX_POINT('',#91140);
#9295=VERTEX_POINT('',#91149);
#9296=VERTEX_POINT('',#91162);
#9297=VERTEX_POINT('',#91163);
#9298=VERTEX_POINT('',#91172);
#9299=VERTEX_POINT('',#91174);
#9300=VERTEX_POINT('',#91187);
#9301=VERTEX_POINT('',#91198);
#9302=VERTEX_POINT('',#91202);
#9303=VERTEX_POINT('',#91203);
#9304=VERTEX_POINT('',#91205);
#9305=VERTEX_POINT('',#91207);
#9306=VERTEX_POINT('',#91211);
#9307=VERTEX_POINT('',#91213);
#9308=VERTEX_POINT('',#91217);
#9309=VERTEX_POINT('',#91219);
#9310=VERTEX_POINT('',#91223);
#9311=VERTEX_POINT('',#91225);
#9312=VERTEX_POINT('',#91227);
#9313=VERTEX_POINT('',#91229);
#9314=VERTEX_POINT('',#91231);
#9315=VERTEX_POINT('',#91233);
#9316=VERTEX_POINT('',#91235);
#9317=VERTEX_POINT('',#91237);
#9318=VERTEX_POINT('',#91239);
#9319=VERTEX_POINT('',#91241);
#9320=VERTEX_POINT('',#91243);
#9321=VERTEX_POINT('',#91245);
#9322=VERTEX_POINT('',#91247);
#9323=VERTEX_POINT('',#91250);
#9324=VERTEX_POINT('',#91254);
#9325=VERTEX_POINT('',#91265);
#9326=VERTEX_POINT('',#91267);
#9327=VERTEX_POINT('',#91271);
#9328=VERTEX_POINT('',#91275);
#9329=VERTEX_POINT('',#91276);
#9330=VERTEX_POINT('',#91278);
#9331=VERTEX_POINT('',#91280);
#9332=VERTEX_POINT('',#91287);
#9333=VERTEX_POINT('',#91289);
#9334=VERTEX_POINT('',#91291);
#9335=VERTEX_POINT('',#91311);
#9336=VERTEX_POINT('',#91313);
#9337=VERTEX_POINT('',#91315);
#9338=VERTEX_POINT('',#91317);
#9339=VERTEX_POINT('',#91319);
#9340=VERTEX_POINT('',#91321);
#9341=VERTEX_POINT('',#91323);
#9342=VERTEX_POINT('',#91325);
#9343=VERTEX_POINT('',#91329);
#9344=VERTEX_POINT('',#91331);
#9345=VERTEX_POINT('',#91335);
#9346=VERTEX_POINT('',#91337);
#9347=VERTEX_POINT('',#91341);
#9348=VERTEX_POINT('',#91343);
#9349=VERTEX_POINT('',#91347);
#9350=VERTEX_POINT('',#91349);
#9351=VERTEX_POINT('',#91351);
#9352=VERTEX_POINT('',#91353);
#9353=VERTEX_POINT('',#91355);
#9354=VERTEX_POINT('',#91357);
#9355=VERTEX_POINT('',#91359);
#9356=VERTEX_POINT('',#91363);
#9357=VERTEX_POINT('',#91364);
#9358=VERTEX_POINT('',#91366);
#9359=VERTEX_POINT('',#91368);
#9360=VERTEX_POINT('',#91370);
#9361=VERTEX_POINT('',#91374);
#9362=VERTEX_POINT('',#91375);
#9363=VERTEX_POINT('',#91377);
#9364=VERTEX_POINT('',#91379);
#9365=VERTEX_POINT('',#91390);
#9366=VERTEX_POINT('',#91394);
#9367=VERTEX_POINT('',#91396);
#9368=VERTEX_POINT('',#91399);
#9369=VERTEX_POINT('',#91403);
#9370=VERTEX_POINT('',#91404);
#9371=VERTEX_POINT('',#91409);
#9372=VERTEX_POINT('',#91411);
#9373=VERTEX_POINT('',#91413);
#9374=VERTEX_POINT('',#91417);
#9375=VERTEX_POINT('',#91428);
#9376=VERTEX_POINT('',#91437);
#9377=VERTEX_POINT('',#91439);
#9378=VERTEX_POINT('',#91441);
#9379=VERTEX_POINT('',#91445);
#9380=VERTEX_POINT('',#91450);
#9381=VERTEX_POINT('',#91452);
#9382=VERTEX_POINT('',#91454);
#9383=VERTEX_POINT('',#91456);
#9384=VERTEX_POINT('',#91458);
#9385=VERTEX_POINT('',#91462);
#9386=VERTEX_POINT('',#91466);
#9387=VERTEX_POINT('',#91468);
#9388=VERTEX_POINT('',#91470);
#9389=VERTEX_POINT('',#91474);
#9390=VERTEX_POINT('',#91476);
#9391=VERTEX_POINT('',#91480);
#9392=VERTEX_POINT('',#91481);
#9393=VERTEX_POINT('',#91497);
#9394=VERTEX_POINT('',#91499);
#9395=VERTEX_POINT('',#91501);
#9396=VERTEX_POINT('',#91505);
#9397=VERTEX_POINT('',#91506);
#9398=VERTEX_POINT('',#91508);
#9399=VERTEX_POINT('',#91537);
#9400=VERTEX_POINT('',#91571);
#9401=VERTEX_POINT('',#91573);
#9402=VERTEX_POINT('',#91576);
#9403=VERTEX_POINT('',#91585);
#9404=VERTEX_POINT('',#91597);
#9405=VERTEX_POINT('',#91606);
#9406=VERTEX_POINT('',#91616);
#9407=VERTEX_POINT('',#91618);
#9408=VERTEX_POINT('',#91622);
#9409=VERTEX_POINT('',#91625);
#9410=VERTEX_POINT('',#91627);
#9411=VERTEX_POINT('',#91631);
#9412=VERTEX_POINT('',#91632);
#9413=VERTEX_POINT('',#91764);
#9414=VERTEX_POINT('',#91790);
#9415=VERTEX_POINT('',#91792);
#9416=VERTEX_POINT('',#91811);
#9417=VERTEX_POINT('',#91815);
#9418=VERTEX_POINT('',#91817);
#9419=VERTEX_POINT('',#91822);
#9420=VERTEX_POINT('',#91833);
#9421=VERTEX_POINT('',#91837);
#9422=VERTEX_POINT('',#91838);
#9423=VERTEX_POINT('',#91840);
#9424=VERTEX_POINT('',#91842);
#9425=VERTEX_POINT('',#91846);
#9426=VERTEX_POINT('',#91849);
#9427=VERTEX_POINT('',#91862);
#9428=VERTEX_POINT('',#91864);
#9429=VERTEX_POINT('',#91866);
#9430=VERTEX_POINT('',#91884);
#9431=VERTEX_POINT('',#91888);
#9432=VERTEX_POINT('',#91894);
#9433=VERTEX_POINT('',#91898);
#9434=VERTEX_POINT('',#91901);
#9435=VERTEX_POINT('',#91903);
#9436=VERTEX_POINT('',#91906);
#9437=VERTEX_POINT('',#91917);
#9438=VERTEX_POINT('',#91919);
#9439=VERTEX_POINT('',#91922);
#9440=VERTEX_POINT('',#91924);
#9441=VERTEX_POINT('',#91928);
#9442=VERTEX_POINT('',#91929);
#9443=VERTEX_POINT('',#91932);
#9444=VERTEX_POINT('',#91934);
#9445=VERTEX_POINT('',#91953);
#9446=VERTEX_POINT('',#91955);
#9447=VERTEX_POINT('',#91979);
#9448=VERTEX_POINT('',#91981);
#9449=VERTEX_POINT('',#91983);
#9450=VERTEX_POINT('',#91986);
#9451=VERTEX_POINT('',#91990);
#9452=VERTEX_POINT('',#91992);
#9453=VERTEX_POINT('',#91996);
#9454=VERTEX_POINT('',#91998);
#9455=VERTEX_POINT('',#92004);
#9456=VERTEX_POINT('',#92006);
#9457=VERTEX_POINT('',#92015);
#9458=VERTEX_POINT('',#92017);
#9459=VERTEX_POINT('',#92019);
#9460=VERTEX_POINT('',#92021);
#9461=VERTEX_POINT('',#92023);
#9462=VERTEX_POINT('',#92025);
#9463=VERTEX_POINT('',#92027);
#9464=VERTEX_POINT('',#92030);
#9465=VERTEX_POINT('',#92033);
#9466=VERTEX_POINT('',#92034);
#9467=VERTEX_POINT('',#92036);
#9468=VERTEX_POINT('',#92038);
#9469=VERTEX_POINT('',#92041);
#9470=VERTEX_POINT('',#92058);
#9471=VERTEX_POINT('',#92060);
#9472=VERTEX_POINT('',#92062);
#9473=VERTEX_POINT('',#92064);
#9474=VERTEX_POINT('',#92068);
#9475=VERTEX_POINT('',#92072);
#9476=VERTEX_POINT('',#92074);
#9477=VERTEX_POINT('',#92076);
#9478=VERTEX_POINT('',#92080);
#9479=VERTEX_POINT('',#92105);
#9480=VERTEX_POINT('',#92107);
#9481=VERTEX_POINT('',#92111);
#9482=VERTEX_POINT('',#92113);
#9483=VERTEX_POINT('',#92121);
#9484=VERTEX_POINT('',#92123);
#9485=VERTEX_POINT('',#92125);
#9486=VERTEX_POINT('',#92144);
#9487=VERTEX_POINT('',#92147);
#9488=VERTEX_POINT('',#92150);
#9489=VERTEX_POINT('',#92152);
#9490=VERTEX_POINT('',#92154);
#9491=VERTEX_POINT('',#92156);
#9492=VERTEX_POINT('',#92158);
#9493=VERTEX_POINT('',#92160);
#9494=VERTEX_POINT('',#92162);
#9495=VERTEX_POINT('',#92164);
#9496=VERTEX_POINT('',#92166);
#9497=VERTEX_POINT('',#92168);
#9498=VERTEX_POINT('',#92170);
#9499=VERTEX_POINT('',#92173);
#9500=VERTEX_POINT('',#92175);
#9501=VERTEX_POINT('',#92178);
#9502=VERTEX_POINT('',#92181);
#9503=VERTEX_POINT('',#92182);
#9504=VERTEX_POINT('',#92184);
#9505=VERTEX_POINT('',#92186);
#9506=VERTEX_POINT('',#92189);
#9507=VERTEX_POINT('',#92190);
#9508=VERTEX_POINT('',#92192);
#9509=VERTEX_POINT('',#92194);
#9510=VERTEX_POINT('',#92196);
#9511=VERTEX_POINT('',#92198);
#9512=VERTEX_POINT('',#92201);
#9513=VERTEX_POINT('',#92203);
#9514=VERTEX_POINT('',#92206);
#9515=VERTEX_POINT('',#92212);
#9516=VERTEX_POINT('',#92213);
#9517=VERTEX_POINT('',#92216);
#9518=VERTEX_POINT('',#92233);
#9519=VERTEX_POINT('',#92238);
#9520=VERTEX_POINT('',#92240);
#9521=VERTEX_POINT('',#92244);
#9522=VERTEX_POINT('',#92248);
#9523=VERTEX_POINT('',#92252);
#9524=VERTEX_POINT('',#92256);
#9525=VERTEX_POINT('',#92261);
#9526=VERTEX_POINT('',#92279);
#9527=VERTEX_POINT('',#92283);
#9528=VERTEX_POINT('',#92285);
#9529=VERTEX_POINT('',#92287);
#9530=VERTEX_POINT('',#92289);
#9531=VERTEX_POINT('',#92291);
#9532=VERTEX_POINT('',#92295);
#9533=VERTEX_POINT('',#92299);
#9534=VERTEX_POINT('',#92301);
#9535=VERTEX_POINT('',#92305);
#9536=VERTEX_POINT('',#92306);
#9537=VERTEX_POINT('',#92311);
#9538=VERTEX_POINT('',#92312);
#9539=VERTEX_POINT('',#92314);
#9540=VERTEX_POINT('',#92316);
#9541=VERTEX_POINT('',#92318);
#9542=VERTEX_POINT('',#92320);
#9543=VERTEX_POINT('',#92322);
#9544=VERTEX_POINT('',#92326);
#9545=VERTEX_POINT('',#92347);
#9546=VERTEX_POINT('',#92348);
#9547=VERTEX_POINT('',#92354);
#9548=VERTEX_POINT('',#92362);
#9549=VERTEX_POINT('',#92368);
#9550=VERTEX_POINT('',#92370);
#9551=VERTEX_POINT('',#92378);
#9552=VERTEX_POINT('',#92382);
#9553=VERTEX_POINT('',#92384);
#9554=VERTEX_POINT('',#92388);
#9555=VERTEX_POINT('',#92392);
#9556=VERTEX_POINT('',#92396);
#9557=VERTEX_POINT('',#92398);
#9558=VERTEX_POINT('',#92402);
#9559=VERTEX_POINT('',#92404);
#9560=VERTEX_POINT('',#92406);
#9561=VERTEX_POINT('',#92408);
#9562=VERTEX_POINT('',#92412);
#9563=VERTEX_POINT('',#92414);
#9564=VERTEX_POINT('',#92418);
#9565=VERTEX_POINT('',#92420);
#9566=VERTEX_POINT('',#92422);
#9567=VERTEX_POINT('',#92424);
#9568=VERTEX_POINT('',#92428);
#9569=VERTEX_POINT('',#92430);
#9570=VERTEX_POINT('',#92434);
#9571=VERTEX_POINT('',#92436);
#9572=VERTEX_POINT('',#92438);
#9573=VERTEX_POINT('',#92440);
#9574=VERTEX_POINT('',#92444);
#9575=VERTEX_POINT('',#92461);
#9576=VERTEX_POINT('',#92463);
#9577=VERTEX_POINT('',#92467);
#9578=VERTEX_POINT('',#92469);
#9579=VERTEX_POINT('',#92471);
#9580=VERTEX_POINT('',#92473);
#9581=VERTEX_POINT('',#92477);
#9582=VERTEX_POINT('',#92479);
#9583=VERTEX_POINT('',#92499);
#9584=VERTEX_POINT('',#92501);
#9585=VERTEX_POINT('',#92505);
#9586=VERTEX_POINT('',#92509);
#9587=VERTEX_POINT('',#92511);
#9588=VERTEX_POINT('',#92515);
#9589=VERTEX_POINT('',#92519);
#9590=VERTEX_POINT('',#92523);
#9591=VERTEX_POINT('',#92527);
#9592=VERTEX_POINT('',#92528);
#9593=VERTEX_POINT('',#92531);
#9594=VERTEX_POINT('',#92549);
#9595=VERTEX_POINT('',#92553);
#9596=VERTEX_POINT('',#92559);
#9597=VERTEX_POINT('',#92573);
#9598=VERTEX_POINT('',#92575);
#9599=VERTEX_POINT('',#92583);
#9600=VERTEX_POINT('',#92585);
#9601=VERTEX_POINT('',#92587);
#9602=VERTEX_POINT('',#92589);
#9603=VERTEX_POINT('',#92591);
#9604=VERTEX_POINT('',#92593);
#9605=VERTEX_POINT('',#92595);
#9606=VERTEX_POINT('',#92597);
#9607=VERTEX_POINT('',#92599);
#9608=VERTEX_POINT('',#92605);
#9609=VERTEX_POINT('',#92606);
#9610=VERTEX_POINT('',#92612);
#9611=VERTEX_POINT('',#92623);
#9612=VERTEX_POINT('',#92625);
#9613=VERTEX_POINT('',#92636);
#9614=VERTEX_POINT('',#92638);
#9615=VERTEX_POINT('',#92640);
#9616=VERTEX_POINT('',#92644);
#9617=VERTEX_POINT('',#92646);
#9618=VERTEX_POINT('',#92653);
#9619=VERTEX_POINT('',#92655);
#9620=VERTEX_POINT('',#92657);
#9621=VERTEX_POINT('',#92659);
#9622=VERTEX_POINT('',#92661);
#9623=VERTEX_POINT('',#92663);
#9624=VERTEX_POINT('',#92713);
#9625=VERTEX_POINT('',#92715);
#9626=VERTEX_POINT('',#92717);
#9627=VERTEX_POINT('',#92719);
#9628=VERTEX_POINT('',#92730);
#9629=VERTEX_POINT('',#92743);
#9630=VERTEX_POINT('',#92745);
#9631=VERTEX_POINT('',#92747);
#9632=VERTEX_POINT('',#92762);
#9633=VERTEX_POINT('',#92767);
#9634=VERTEX_POINT('',#92768);
#9635=VERTEX_POINT('',#92771);
#9636=VERTEX_POINT('',#92775);
#9637=VERTEX_POINT('',#92779);
#9638=VERTEX_POINT('',#92782);
#9639=VERTEX_POINT('',#92786);
#9640=VERTEX_POINT('',#92787);
#9641=VERTEX_POINT('',#92789);
#9642=VERTEX_POINT('',#92791);
#9643=VERTEX_POINT('',#92795);
#9644=VERTEX_POINT('',#92796);
#9645=VERTEX_POINT('',#92798);
#9646=VERTEX_POINT('',#92800);
#9647=VERTEX_POINT('',#92802);
#9648=VERTEX_POINT('',#92804);
#9649=VERTEX_POINT('',#92808);
#9650=VERTEX_POINT('',#92810);
#9651=VERTEX_POINT('',#92814);
#9652=VERTEX_POINT('',#92816);
#9653=VERTEX_POINT('',#92818);
#9654=VERTEX_POINT('',#92820);
#9655=VERTEX_POINT('',#92822);
#9656=VERTEX_POINT('',#92824);
#9657=VERTEX_POINT('',#92828);
#9658=VERTEX_POINT('',#92832);
#9659=VERTEX_POINT('',#92833);
#9660=VERTEX_POINT('',#92835);
#9661=VERTEX_POINT('',#92837);
#9662=VERTEX_POINT('',#92841);
#9663=VERTEX_POINT('',#92843);
#9664=VERTEX_POINT('',#92845);
#9665=VERTEX_POINT('',#92849);
#9666=VERTEX_POINT('',#92850);
#9667=VERTEX_POINT('',#92852);
#9668=VERTEX_POINT('',#92855);
#9669=VERTEX_POINT('',#92872);
#9670=VERTEX_POINT('',#92874);
#9671=VERTEX_POINT('',#92879);
#9672=VERTEX_POINT('',#92882);
#9673=VERTEX_POINT('',#92887);
#9674=VERTEX_POINT('',#92893);
#9675=VERTEX_POINT('',#92895);
#9676=VERTEX_POINT('',#92897);
#9677=VERTEX_POINT('',#92899);
#9678=VERTEX_POINT('',#92903);
#9679=VERTEX_POINT('',#92907);
#9680=VERTEX_POINT('',#92909);
#9681=VERTEX_POINT('',#92911);
#9682=VERTEX_POINT('',#92913);
#9683=VERTEX_POINT('',#92915);
#9684=VERTEX_POINT('',#92932);
#9685=VERTEX_POINT('',#92962);
#9686=VERTEX_POINT('',#92973);
#9687=VERTEX_POINT('',#92987);
#9688=VERTEX_POINT('',#93007);
#9689=VERTEX_POINT('',#93009);
#9690=VERTEX_POINT('',#93011);
#9691=VERTEX_POINT('',#93013);
#9692=VERTEX_POINT('',#93028);
#9693=VERTEX_POINT('',#93030);
#9694=VERTEX_POINT('',#93040);
#9695=VERTEX_POINT('',#93042);
#9696=VERTEX_POINT('',#93048);
#9697=VERTEX_POINT('',#93050);
#9698=VERTEX_POINT('',#93054);
#9699=VERTEX_POINT('',#93056);
#9700=VERTEX_POINT('',#93115);
#9701=VERTEX_POINT('',#93134);
#9702=VERTEX_POINT('',#93144);
#9703=VERTEX_POINT('',#93154);
#9704=VERTEX_POINT('',#93161);
#11843=EDGE_CURVE('',#9276,#9277,#7928,.T.);
#11844=EDGE_CURVE('',#9276,#9278,#802,.T.);
#11845=EDGE_CURVE('',#9278,#9279,#7929,.F.);
#11846=EDGE_CURVE('',#9279,#9277,#803,.T.);
#11847=EDGE_CURVE('',#9277,#9279,#2786,.T.);
#11848=EDGE_CURVE('',#9280,#9281,#7930,.T.);
#11849=EDGE_CURVE('',#9280,#9282,#804,.T.);
#11850=EDGE_CURVE('',#9282,#9283,#7931,.F.);
#11851=EDGE_CURVE('',#9283,#9284,#7932,.F.);
#11852=EDGE_CURVE('',#9284,#9281,#805,.T.);
#11853=EDGE_CURVE('',#9284,#9285,#2787,.T.);
#11854=EDGE_CURVE('',#9285,#9281,#2788,.T.);
#11855=EDGE_CURVE('',#9286,#9287,#806,.T.);
#11856=EDGE_CURVE('',#9288,#9287,#7933,.T.);
#11857=EDGE_CURVE('',#9289,#9288,#7934,.T.);
#11858=EDGE_CURVE('',#9289,#9290,#807,.T.);
#11859=EDGE_CURVE('',#9290,#9286,#7935,.T.);
#11860=EDGE_CURVE('',#9291,#9286,#2789,.T.);
#11861=EDGE_CURVE('',#9290,#9292,#2790,.T.);
#11862=EDGE_CURVE('',#9292,#9291,#7936,.T.);
#11863=EDGE_CURVE('',#9292,#9293,#808,.T.);
#11864=EDGE_CURVE('',#9293,#9294,#7937,.F.);
#11865=EDGE_CURVE('',#9294,#9295,#7938,.F.);
#11866=EDGE_CURVE('',#9295,#9291,#809,.T.);
#11867=EDGE_CURVE('',#9295,#9287,#2791,.T.);
#11868=EDGE_CURVE('',#9296,#9297,#7939,.T.);
#11869=EDGE_CURVE('',#9296,#9298,#810,.T.);
#11870=EDGE_CURVE('',#9298,#9299,#7940,.F.);
#11871=EDGE_CURVE('',#9299,#9300,#811,.T.);
#11872=EDGE_CURVE('',#9297,#9300,#7941,.T.);
#11873=EDGE_CURVE('',#9301,#9299,#2792,.T.);
#11874=EDGE_CURVE('',#9301,#9300,#2793,.T.);
#11875=EDGE_CURVE('',#9302,#9303,#812,.F.);
#11876=EDGE_CURVE('',#9303,#9304,#2794,.T.);
#11877=EDGE_CURVE('',#9304,#9305,#813,.F.);
#11878=EDGE_CURVE('',#9305,#9302,#2795,.T.);
#11879=EDGE_CURVE('',#9306,#9303,#2796,.T.);
#11880=EDGE_CURVE('',#9307,#9306,#2797,.T.);
#11881=EDGE_CURVE('',#9304,#9307,#2798,.T.);
#11882=EDGE_CURVE('',#9306,#9308,#1901,.F.);
#11883=EDGE_CURVE('',#9308,#9309,#2799,.T.);
#11884=EDGE_CURVE('',#9309,#9307,#814,.F.);
#11885=EDGE_CURVE('',#9310,#9308,#2800,.T.);
#11886=EDGE_CURVE('',#9311,#9310,#815,.F.);
#11887=EDGE_CURVE('',#9311,#9312,#2801,.T.);
#11888=EDGE_CURVE('',#9313,#9312,#816,.F.);
#11889=EDGE_CURVE('',#9314,#9313,#2802,.T.);
#11890=EDGE_CURVE('',#9315,#9314,#817,.T.);
#11891=EDGE_CURVE('',#9316,#9315,#2803,.T.);
#11892=EDGE_CURVE('',#9316,#9317,#818,.T.);
#11893=EDGE_CURVE('',#9317,#9318,#2804,.T.);
#11894=EDGE_CURVE('',#9319,#9318,#819,.F.);
#11895=EDGE_CURVE('',#9320,#9319,#2805,.T.);
#11896=EDGE_CURVE('',#9321,#9320,#2806,.T.);
#11897=EDGE_CURVE('',#9321,#9322,#2807,.T.);
#11898=EDGE_CURVE('',#9288,#9322,#2808,.T.);
#11899=EDGE_CURVE('',#9323,#9294,#2809,.T.);
#11900=EDGE_CURVE('',#9309,#9323,#2810,.T.);
#11901=EDGE_CURVE('',#9319,#9324,#7942,.F.);
#11902=EDGE_CURVE('',#9324,#9325,#820,.F.);
#11903=EDGE_CURVE('',#9325,#9326,#2811,.T.);
#11904=EDGE_CURVE('',#9326,#9320,#1902,.T.);
#11905=EDGE_CURVE('',#9326,#9327,#2812,.T.);
#11906=EDGE_CURVE('',#9327,#9321,#821,.F.);
#11907=EDGE_CURVE('',#9328,#9329,#2813,.T.);
#11908=EDGE_CURVE('',#9329,#9330,#1903,.T.);
#11909=EDGE_CURVE('',#9330,#9331,#7943,.T.);
#11910=EDGE_CURVE('',#9332,#9331,#1904,.T.);
#11911=EDGE_CURVE('',#9332,#9333,#2814,.T.);
#11912=EDGE_CURVE('',#9334,#9333,#7944,.T.);
#11913=EDGE_CURVE('',#9334,#9335,#2815,.T.);
#11914=EDGE_CURVE('',#9335,#9336,#1905,.F.);
#11915=EDGE_CURVE('',#9336,#9337,#1906,.T.);
#11916=EDGE_CURVE('',#9337,#9338,#2816,.T.);
#11917=EDGE_CURVE('',#9338,#9339,#1907,.T.);
#11918=EDGE_CURVE('',#9339,#9340,#2817,.T.);
#11919=EDGE_CURVE('',#9340,#9341,#1908,.T.);
#11920=EDGE_CURVE('',#9341,#9342,#2818,.T.);
#11921=EDGE_CURVE('',#9342,#9328,#1909,.T.);
#11922=EDGE_CURVE('',#9332,#9343,#2819,.T.);
#11923=EDGE_CURVE('',#9343,#9344,#2820,.T.);
#11924=EDGE_CURVE('',#9333,#9344,#2821,.T.);
#11925=EDGE_CURVE('',#9345,#9334,#1910,.F.);
#11926=EDGE_CURVE('',#9345,#9346,#2822,.T.);
#11927=EDGE_CURVE('',#9335,#9346,#2823,.T.);
#11928=EDGE_CURVE('',#9347,#9341,#2824,.T.);
#11929=EDGE_CURVE('',#9347,#9348,#822,.T.);
#11930=EDGE_CURVE('',#9348,#9342,#2825,.T.);
#11931=EDGE_CURVE('',#9349,#9337,#2826,.T.);
#11932=EDGE_CURVE('',#9350,#9349,#2827,.T.);
#11933=EDGE_CURVE('',#9351,#9350,#2828,.T.);
#11934=EDGE_CURVE('',#9351,#9352,#823,.T.);
#11935=EDGE_CURVE('',#9352,#9353,#2829,.T.);
#11936=EDGE_CURVE('',#9353,#9354,#2830,.T.);
#11937=EDGE_CURVE('',#9354,#9355,#824,.T.);
#11938=EDGE_CURVE('',#9355,#9338,#2831,.T.);
#11939=EDGE_CURVE('',#9356,#9357,#2832,.T.);
#11940=EDGE_CURVE('',#9358,#9357,#2833,.T.);
#11941=EDGE_CURVE('',#9359,#9358,#2834,.T.);
#11942=EDGE_CURVE('',#9360,#9359,#2835,.T.);
#11943=EDGE_CURVE('',#9356,#9360,#2836,.T.);
#11944=EDGE_CURVE('',#9361,#9362,#2837,.T.);
#11945=EDGE_CURVE('',#9363,#9362,#825,.T.);
#11946=EDGE_CURVE('',#9363,#9364,#2838,.T.);
#11947=EDGE_CURVE('',#9364,#9359,#826,.T.);
#11948=EDGE_CURVE('',#9358,#9361,#1911,.T.);
#11949=EDGE_CURVE('',#9331,#9362,#7945,.T.);
#11950=EDGE_CURVE('',#9365,#9330,#827,.T.);
#11951=EDGE_CURVE('',#9363,#9365,#828,.T.);
#11952=EDGE_CURVE('',#9329,#9366,#1912,.T.);
#11953=EDGE_CURVE('',#9366,#9367,#2839,.T.);
#11954=EDGE_CURVE('',#9367,#9350,#1913,.T.);
#11955=EDGE_CURVE('',#9368,#9349,#829,.T.);
#11956=EDGE_CURVE('',#9368,#9365,#2840,.T.);
#11957=EDGE_CURVE('',#9369,#9370,#830,.T.);
#11958=EDGE_CURVE('',#9370,#9324,#2841,.T.);
#11959=EDGE_CURVE('',#9318,#9369,#2842,.T.);
#11960=EDGE_CURVE('',#9371,#9369,#831,.T.);
#11961=EDGE_CURVE('',#9369,#9372,#2843,.T.);
#11962=EDGE_CURVE('',#9372,#9373,#832,.T.);
#11963=EDGE_CURVE('',#9373,#9371,#2844,.T.);
#11964=EDGE_CURVE('',#9374,#9316,#7946,.T.);
#11965=EDGE_CURVE('',#9374,#9375,#2845,.T.);
#11966=EDGE_CURVE('',#9375,#9372,#833,.T.);
#11967=EDGE_CURVE('',#9372,#9317,#2846,.T.);
#11968=EDGE_CURVE('',#9375,#9373,#834,.T.);
#11969=EDGE_CURVE('',#9371,#9370,#835,.T.);
#11970=EDGE_CURVE('',#9376,#9370,#2847,.T.);
#11971=EDGE_CURVE('',#9376,#9377,#2848,.T.);
#11972=EDGE_CURVE('',#9378,#9377,#2849,.T.);
#11973=EDGE_CURVE('',#9325,#9378,#2850,.T.);
#11974=EDGE_CURVE('',#9371,#9379,#2851,.T.);
#11975=EDGE_CURVE('',#9379,#9376,#1914,.F.);
#11976=EDGE_CURVE('',#9364,#9373,#2852,.T.);
#11977=EDGE_CURVE('',#9380,#9363,#2853,.T.);
#11978=EDGE_CURVE('',#9381,#9380,#2854,.T.);
#11979=EDGE_CURVE('',#9382,#9381,#2855,.T.);
#11980=EDGE_CURVE('',#9383,#9382,#2856,.T.);
#11981=EDGE_CURVE('',#9384,#9383,#2857,.T.);
#11982=EDGE_CURVE('',#9379,#9384,#2858,.T.);
#11983=EDGE_CURVE('',#9375,#9385,#2859,.T.);
#11984=EDGE_CURVE('',#9385,#9364,#836,.T.);
#11985=EDGE_CURVE('',#9386,#9374,#837,.F.);
#11986=EDGE_CURVE('',#9387,#9386,#2860,.T.);
#11987=EDGE_CURVE('',#9388,#9387,#2861,.T.);
#11988=EDGE_CURVE('',#9385,#9388,#2862,.T.);
#11989=EDGE_CURVE('',#9389,#9315,#838,.T.);
#11990=EDGE_CURVE('',#9314,#9390,#839,.T.);
#11991=EDGE_CURVE('',#9390,#9389,#840,.T.);
#11992=EDGE_CURVE('',#9391,#9392,#841,.F.);
#11993=EDGE_CURVE('',#9392,#9390,#2863,.T.);
#11994=EDGE_CURVE('',#9313,#9391,#7947,.F.);
#11995=EDGE_CURVE('',#9389,#9386,#2864,.T.);
#11996=EDGE_CURVE('',#9392,#9393,#2865,.T.);
#11997=EDGE_CURVE('',#9394,#9393,#842,.F.);
#11998=EDGE_CURVE('',#9395,#9394,#2866,.T.);
#11999=EDGE_CURVE('',#9390,#9395,#2867,.T.);
#12000=EDGE_CURVE('',#9396,#9397,#843,.T.);
#12001=EDGE_CURVE('',#9397,#9398,#7948,.T.);
#12002=EDGE_CURVE('',#9398,#9399,#844,.T.);
#12003=EDGE_CURVE('',#9396,#9399,#7949,.T.);
#12004=EDGE_CURVE('',#9399,#9398,#2868,.T.);
#12005=EDGE_CURVE('',#9397,#9396,#2869,.T.);
#12006=EDGE_CURVE('',#9400,#9276,#2870,.T.);
#12007=EDGE_CURVE('',#9401,#9400,#845,.T.);
#12008=EDGE_CURVE('',#9298,#9401,#2871,.T.);
#12009=EDGE_CURVE('',#9402,#9296,#7950,.F.);
#12010=EDGE_CURVE('',#9402,#9403,#846,.T.);
#12011=EDGE_CURVE('',#9293,#9403,#7951,.F.);
#12012=EDGE_CURVE('',#9292,#9399,#2872,.T.);
#12013=EDGE_CURVE('',#9398,#9290,#2873,.T.);
#12014=EDGE_CURVE('',#9404,#9289,#7952,.F.);
#12015=EDGE_CURVE('',#9404,#9405,#847,.T.);
#12016=EDGE_CURVE('',#9282,#9405,#7953,.F.);
#12017=EDGE_CURVE('',#9406,#9280,#2874,.T.);
#12018=EDGE_CURVE('',#9407,#9406,#848,.T.);
#12019=EDGE_CURVE('',#9278,#9407,#2875,.T.);
#12020=EDGE_CURVE('',#9408,#9408,#849,.T.);
#12021=EDGE_CURVE('',#9408,#9409,#850,.T.);
#12022=EDGE_CURVE('',#9409,#9410,#851,.T.);
#12023=EDGE_CURVE('',#9410,#9409,#852,.T.);
#12024=EDGE_CURVE('',#9411,#9412,#7954,.T.);
#12025=EDGE_CURVE('',#9412,#9411,#7955,.T.);
#12026=EDGE_CURVE('',#9412,#9410,#2876,.T.);
#12027=EDGE_CURVE('',#9413,#9411,#7956,.T.);
#12028=EDGE_CURVE('',#9413,#9413,#7957,.T.);
#12029=EDGE_CURVE('',#9414,#9395,#853,.T.);
#12030=EDGE_CURVE('',#9415,#9414,#7958,.T.);
#12031=EDGE_CURVE('',#9416,#9415,#854,.T.);
#12032=EDGE_CURVE('',#9389,#9416,#2877,.T.);
#12033=EDGE_CURVE('',#9417,#9417,#855,.T.);
#12034=EDGE_CURVE('',#9417,#9418,#856,.T.);
#12035=EDGE_CURVE('',#9418,#9418,#857,.T.);
#12036=EDGE_CURVE('',#9310,#9419,#7959,.T.);
#12037=EDGE_CURVE('',#9306,#9420,#2878,.T.);
#12038=EDGE_CURVE('',#9419,#9420,#858,.T.);
#12039=EDGE_CURVE('',#9421,#9422,#859,.T.);
#12040=EDGE_CURVE('',#9422,#9423,#2879,.T.);
#12041=EDGE_CURVE('',#9423,#9424,#860,.T.);
#12042=EDGE_CURVE('',#9424,#9421,#2880,.T.);
#12043=EDGE_CURVE('',#9425,#9423,#861,.T.);
#12044=EDGE_CURVE('',#9423,#9368,#2881,.T.);
#12045=EDGE_CURVE('',#9368,#9426,#862,.T.);
#12046=EDGE_CURVE('',#9426,#9425,#2882,.T.);
#12047=EDGE_CURVE('',#9425,#9424,#863,.T.);
#12048=EDGE_CURVE('',#9349,#9426,#864,.T.);
#12049=EDGE_CURVE('',#9365,#9422,#2883,.T.);
#12050=EDGE_CURVE('',#9422,#9380,#865,.T.);
#12051=EDGE_CURVE('',#9421,#9380,#866,.T.);
#12052=EDGE_CURVE('',#9427,#9367,#1915,.T.);
#12053=EDGE_CURVE('',#9427,#9428,#2884,.T.);
#12054=EDGE_CURVE('',#9428,#9429,#7960,.T.);
#12055=EDGE_CURVE('',#9429,#9351,#7961,.T.);
#12056=EDGE_CURVE('',#9430,#9366,#1916,.T.);
#12057=EDGE_CURVE('',#9430,#9427,#2885,.T.);
#12058=EDGE_CURVE('',#9328,#9431,#1917,.F.);
#12059=EDGE_CURVE('',#9431,#9430,#2886,.T.);
#12060=EDGE_CURVE('',#9356,#9336,#1918,.T.);
#12061=EDGE_CURVE('',#9432,#9360,#867,.T.);
#12062=EDGE_CURVE('',#9432,#9426,#2887,.T.);
#12063=EDGE_CURVE('',#9433,#9433,#868,.T.);
#12064=EDGE_CURVE('',#9433,#9429,#2888,.T.);
#12065=EDGE_CURVE('',#9428,#9434,#2889,.T.);
#12066=EDGE_CURVE('',#9434,#9435,#869,.T.);
#12067=EDGE_CURVE('',#9435,#9348,#2890,.T.);
#12068=EDGE_CURVE('',#9436,#9347,#7962,.T.);
#12069=EDGE_CURVE('',#9436,#9437,#2891,.T.);
#12070=EDGE_CURVE('',#9437,#9438,#870,.T.);
#12071=EDGE_CURVE('',#9438,#9355,#2892,.T.);
#12072=EDGE_CURVE('',#9354,#9439,#2893,.T.);
#12073=EDGE_CURVE('',#9439,#9440,#871,.T.);
#12074=EDGE_CURVE('',#9440,#9352,#2894,.T.);
#12075=EDGE_CURVE('',#9441,#9442,#1919,.T.);
#12076=EDGE_CURVE('',#9441,#9345,#2895,.T.);
#12077=EDGE_CURVE('',#9333,#9443,#2896,.T.);
#12078=EDGE_CURVE('',#9443,#9444,#7963,.T.);
#12079=EDGE_CURVE('',#9444,#9445,#2897,.T.);
#12080=EDGE_CURVE('',#9445,#9446,#7964,.F.);
#12081=EDGE_CURVE('',#9446,#9442,#7965,.F.);
#12082=EDGE_CURVE('',#9447,#9447,#872,.T.);
#12083=EDGE_CURVE('',#9447,#9448,#2898,.T.);
#12084=EDGE_CURVE('',#9449,#9448,#873,.T.);
#12085=EDGE_CURVE('',#9449,#9444,#2899,.T.);
#12086=EDGE_CURVE('',#9443,#9450,#2900,.T.);
#12087=EDGE_CURVE('',#9448,#9450,#874,.T.);
#12088=EDGE_CURVE('',#9383,#9451,#875,.T.);
#12089=EDGE_CURVE('',#9451,#9452,#2901,.T.);
#12090=EDGE_CURVE('',#9452,#9384,#876,.T.);
#12091=EDGE_CURVE('',#9453,#9383,#877,.T.);
#12092=EDGE_CURVE('',#9382,#9454,#1920,.F.);
#12093=EDGE_CURVE('',#9454,#9453,#2902,.T.);
#12094=EDGE_CURVE('',#9453,#9451,#878,.T.);
#12095=EDGE_CURVE('',#9455,#9452,#879,.T.);
#12096=EDGE_CURVE('',#9452,#9456,#2903,.T.);
#12097=EDGE_CURVE('',#9456,#9322,#1921,.F.);
#12098=EDGE_CURVE('',#9322,#9455,#2904,.T.);
#12099=EDGE_CURVE('',#9455,#9384,#880,.T.);
#12100=EDGE_CURVE('',#9455,#9376,#2905,.T.);
#12101=EDGE_CURVE('',#9327,#9457,#2906,.T.);
#12102=EDGE_CURVE('',#9458,#9457,#881,.F.);
#12103=EDGE_CURVE('',#9459,#9458,#2907,.T.);
#12104=EDGE_CURVE('',#9460,#9459,#2908,.T.);
#12105=EDGE_CURVE('',#9461,#9460,#2909,.T.);
#12106=EDGE_CURVE('',#9462,#9461,#882,.T.);
#12107=EDGE_CURVE('',#9463,#9462,#883,.T.);
#12108=EDGE_CURVE('',#9377,#9463,#2910,.T.);
#12109=EDGE_CURVE('',#9464,#9464,#884,.T.);
#12110=EDGE_CURVE('',#9465,#9466,#885,.T.);
#12111=EDGE_CURVE('',#9466,#9467,#886,.T.);
#12112=EDGE_CURVE('',#9467,#9468,#887,.T.);
#12113=EDGE_CURVE('',#9468,#9467,#888,.T.);
#12114=EDGE_CURVE('',#9466,#9469,#889,.T.);
#12115=EDGE_CURVE('',#9469,#9465,#7966,.T.);
#12116=EDGE_CURVE('',#9469,#9470,#2911,.T.);
#12117=EDGE_CURVE('',#9471,#9470,#1922,.F.);
#12118=EDGE_CURVE('',#9471,#9472,#2912,.T.);
#12119=EDGE_CURVE('',#9473,#9472,#890,.T.);
#12120=EDGE_CURVE('',#9473,#9465,#2913,.T.);
#12121=EDGE_CURVE('',#9474,#9474,#891,.T.);
#12122=EDGE_CURVE('',#9474,#9468,#2914,.T.);
#12123=EDGE_CURVE('',#9475,#9475,#892,.T.);
#12124=EDGE_CURVE('',#9475,#9476,#893,.T.);
#12125=EDGE_CURVE('',#9476,#9477,#894,.T.);
#12126=EDGE_CURVE('',#9477,#9476,#895,.T.);
#12127=EDGE_CURVE('',#9478,#9478,#896,.T.);
#12128=EDGE_CURVE('',#9478,#9477,#2915,.T.);
#12129=EDGE_CURVE('',#9470,#9454,#2916,.T.);
#12130=EDGE_CURVE('',#9453,#9473,#2917,.T.);
#12131=EDGE_CURVE('',#9464,#9478,#897,.T.);
#12132=EDGE_CURVE('',#9462,#9474,#898,.T.);
#12133=EDGE_CURVE('',#9461,#9463,#7967,.T.);
#12134=EDGE_CURVE('',#9479,#9460,#899,.T.);
#12135=EDGE_CURVE('',#9479,#9480,#2918,.T.);
#12136=EDGE_CURVE('',#9480,#9377,#1923,.F.);
#12137=EDGE_CURVE('',#9457,#9481,#2919,.T.);
#12138=EDGE_CURVE('',#9481,#9482,#900,.F.);
#12139=EDGE_CURVE('',#9482,#9458,#2920,.T.);
#12140=EDGE_CURVE('',#9481,#9326,#2921,.T.);
#12141=EDGE_CURVE('',#9456,#9404,#2922,.T.);
#12142=EDGE_CURVE('',#9483,#9451,#2923,.T.);
#12143=EDGE_CURVE('',#9484,#9483,#2924,.T.);
#12144=EDGE_CURVE('',#9485,#9484,#2925,.T.);
#12145=EDGE_CURVE('',#9405,#9485,#2926,.T.);
#12146=EDGE_CURVE('',#9485,#9459,#1924,.F.);
#12147=EDGE_CURVE('',#9459,#9283,#2927,.T.);
#12148=EDGE_CURVE('',#9285,#9482,#2928,.T.);
#12149=EDGE_CURVE('',#9484,#9460,#901,.T.);
#12150=EDGE_CURVE('',#9479,#9484,#902,.T.);
#12151=EDGE_CURVE('',#9483,#9472,#903,.T.);
#12152=EDGE_CURVE('',#9472,#9479,#2929,.T.);
#12153=EDGE_CURVE('',#9473,#9483,#904,.T.);
#12154=EDGE_CURVE('',#9486,#9432,#2930,.T.);
#12155=EDGE_CURVE('',#9486,#9416,#2931,.T.);
#12156=EDGE_CURVE('',#9487,#9415,#905,.T.);
#12157=EDGE_CURVE('',#9414,#9487,#906,.T.);
#12158=EDGE_CURVE('',#9488,#9394,#2932,.T.);
#12159=EDGE_CURVE('',#9489,#9488,#2933,.T.);
#12160=EDGE_CURVE('',#9489,#9490,#2934,.T.);
#12161=EDGE_CURVE('',#9491,#9490,#907,.T.);
#12162=EDGE_CURVE('',#9491,#9492,#2935,.T.);
#12163=EDGE_CURVE('',#9493,#9492,#2936,.T.);
#12164=EDGE_CURVE('',#9494,#9493,#2937,.T.);
#12165=EDGE_CURVE('',#9495,#9494,#2938,.T.);
#12166=EDGE_CURVE('',#9496,#9495,#2939,.T.);
#12167=EDGE_CURVE('',#9497,#9496,#2940,.T.);
#12168=EDGE_CURVE('',#9498,#9497,#2941,.T.);
#12169=EDGE_CURVE('',#9498,#9400,#2942,.T.);
#12170=EDGE_CURVE('',#9407,#9499,#2943,.T.);
#12171=EDGE_CURVE('',#9500,#9499,#2944,.T.);
#12172=EDGE_CURVE('',#9480,#9500,#2945,.T.);
#12173=EDGE_CURVE('',#9501,#9471,#2946,.T.);
#12174=EDGE_CURVE('',#9425,#9501,#2947,.T.);
#12175=EDGE_CURVE('',#9502,#9503,#2948,.T.);
#12176=EDGE_CURVE('',#9504,#9502,#2949,.T.);
#12177=EDGE_CURVE('',#9505,#9504,#2950,.T.);
#12178=EDGE_CURVE('',#9503,#9505,#2951,.T.);
#12179=EDGE_CURVE('',#9506,#9507,#2952,.T.);
#12180=EDGE_CURVE('',#9508,#9506,#2953,.T.);
#12181=EDGE_CURVE('',#9509,#9508,#908,.T.);
#12182=EDGE_CURVE('',#9510,#9509,#2954,.T.);
#12183=EDGE_CURVE('',#9511,#9510,#2955,.T.);
#12184=EDGE_CURVE('',#9507,#9511,#2956,.T.);
#12185=EDGE_CURVE('',#9512,#9512,#909,.T.);
#12186=EDGE_CURVE('',#9513,#9513,#910,.T.);
#12187=EDGE_CURVE('',#9381,#9514,#1925,.F.);
#12188=EDGE_CURVE('',#9514,#9454,#2957,.T.);
#12189=EDGE_CURVE('',#9421,#9514,#2958,.T.);
#12190=EDGE_CURVE('',#9515,#9516,#911,.T.);
#12191=EDGE_CURVE('',#9516,#9433,#912,.T.);
#12192=EDGE_CURVE('',#9516,#9517,#913,.T.);
#12193=EDGE_CURVE('',#9517,#9515,#7968,.T.);
#12194=EDGE_CURVE('',#9501,#9518,#1926,.F.);
#12195=EDGE_CURVE('',#9518,#9515,#2959,.T.);
#12196=EDGE_CURVE('',#9517,#9424,#2960,.T.);
#12197=EDGE_CURVE('',#9431,#9519,#2961,.T.);
#12198=EDGE_CURVE('',#9519,#9520,#2962,.T.);
#12199=EDGE_CURVE('',#9430,#9520,#2963,.T.);
#12200=EDGE_CURVE('',#9340,#9521,#1927,.F.);
#12201=EDGE_CURVE('',#9521,#9436,#2964,.T.);
#12202=EDGE_CURVE('',#9521,#9522,#2965,.T.);
#12203=EDGE_CURVE('',#9522,#9437,#2966,.T.);
#12204=EDGE_CURVE('',#9339,#9523,#1928,.F.);
#12205=EDGE_CURVE('',#9523,#9521,#2967,.T.);
#12206=EDGE_CURVE('',#9523,#9524,#2968,.T.);
#12207=EDGE_CURVE('',#9524,#9522,#2969,.T.);
#12208=EDGE_CURVE('',#9335,#9442,#2970,.T.);
#12209=EDGE_CURVE('',#9446,#9525,#1929,.F.);
#12210=EDGE_CURVE('',#9525,#9357,#1930,.T.);
#12211=EDGE_CURVE('',#9346,#9441,#2971,.T.);
#12212=EDGE_CURVE('',#9385,#9359,#914,.T.);
#12213=EDGE_CURVE('',#9361,#9525,#1931,.F.);
#12214=EDGE_CURVE('',#9445,#9332,#2972,.T.);
#12215=EDGE_CURVE('',#9388,#9360,#915,.T.);
#12216=EDGE_CURVE('',#9432,#9388,#916,.T.);
#12217=EDGE_CURVE('',#9387,#9486,#917,.F.);
#12218=EDGE_CURVE('',#9403,#9526,#2973,.T.);
#12219=EDGE_CURVE('',#9526,#9323,#1932,.F.);
#12220=EDGE_CURVE('',#9526,#9527,#2974,.T.);
#12221=EDGE_CURVE('',#9528,#9402,#2975,.T.);
#12222=EDGE_CURVE('',#9529,#9528,#2976,.T.);
#12223=EDGE_CURVE('',#9530,#9529,#2977,.T.);
#12224=EDGE_CURVE('',#9531,#9530,#2978,.T.);
#12225=EDGE_CURVE('',#9527,#9531,#2979,.T.);
#12226=EDGE_CURVE('',#9532,#9528,#1933,.F.);
#12227=EDGE_CURVE('',#9297,#9532,#2980,.T.);
#12228=EDGE_CURVE('',#9533,#9533,#918,.T.);
#12229=EDGE_CURVE('',#9533,#9534,#919,.T.);
#12230=EDGE_CURVE('',#9534,#9534,#920,.T.);
#12231=EDGE_CURVE('',#9535,#9536,#921,.T.);
#12232=EDGE_CURVE('',#9536,#9535,#922,.T.);
#12233=EDGE_CURVE('',#9536,#9534,#2981,.T.);
#12234=EDGE_CURVE('',#9537,#9538,#923,.T.);
#12235=EDGE_CURVE('',#9539,#9537,#2982,.T.);
#12236=EDGE_CURVE('',#9540,#9539,#2983,.T.);
#12237=EDGE_CURVE('',#9541,#9540,#2984,.T.);
#12238=EDGE_CURVE('',#9542,#9541,#2985,.T.);
#12239=EDGE_CURVE('',#9543,#9542,#2986,.T.);
#12240=EDGE_CURVE('',#9538,#9543,#924,.T.);
#12241=EDGE_CURVE('',#9538,#9544,#925,.T.);
#12242=EDGE_CURVE('',#9544,#9544,#926,.T.);
#12243=EDGE_CURVE('',#9543,#9537,#7969,.T.);
#12244=EDGE_CURVE('',#9542,#9494,#927,.T.);
#12245=EDGE_CURVE('',#9539,#9493,#1934,.F.);
#12246=EDGE_CURVE('',#9545,#9546,#928,.T.);
#12247=EDGE_CURVE('',#9546,#9545,#929,.T.);
#12248=EDGE_CURVE('',#9546,#9544,#2987,.T.);
#12249=EDGE_CURVE('',#9514,#9518,#2988,.T.);
#12250=EDGE_CURVE('',#9547,#9547,#930,.T.);
#12251=EDGE_CURVE('',#9470,#9518,#2989,.T.);
#12252=EDGE_CURVE('',#9500,#9378,#1935,.F.);
#12253=EDGE_CURVE('',#9499,#9548,#931,.T.);
#12254=EDGE_CURVE('',#9548,#9378,#2990,.T.);
#12255=EDGE_CURVE('',#9406,#9548,#2991,.T.);
#12256=EDGE_CURVE('',#9549,#9498,#932,.T.);
#12257=EDGE_CURVE('',#9497,#9550,#1936,.F.);
#12258=EDGE_CURVE('',#9550,#9549,#2992,.T.);
#12259=EDGE_CURVE('',#9302,#9301,#2993,.T.);
#12260=EDGE_CURVE('',#9401,#9549,#2994,.T.);
#12261=EDGE_CURVE('',#9550,#9420,#2995,.T.);
#12262=EDGE_CURVE('',#9496,#9551,#1937,.F.);
#12263=EDGE_CURVE('',#9551,#9550,#2996,.T.);
#12264=EDGE_CURVE('',#9551,#9552,#2997,.T.);
#12265=EDGE_CURVE('',#9553,#9552,#2998,.T.);
#12266=EDGE_CURVE('',#9419,#9553,#2999,.T.);
#12267=EDGE_CURVE('',#9492,#9554,#933,.F.);
#12268=EDGE_CURVE('',#9554,#9539,#3000,.T.);
#12269=EDGE_CURVE('',#9554,#9555,#3001,.T.);
#12270=EDGE_CURVE('',#9540,#9555,#3002,.T.);
#12271=EDGE_CURVE('',#9505,#9556,#1938,.F.);
#12272=EDGE_CURVE('',#9556,#9557,#3003,.T.);
#12273=EDGE_CURVE('',#9557,#9503,#1939,.F.);
#12274=EDGE_CURVE('',#9556,#9558,#3004,.T.);
#12275=EDGE_CURVE('',#9558,#9559,#3005,.T.);
#12276=EDGE_CURVE('',#9559,#9560,#934,.T.);
#12277=EDGE_CURVE('',#9560,#9561,#3006,.T.);
#12278=EDGE_CURVE('',#9557,#9561,#3007,.T.);
#12279=EDGE_CURVE('',#9502,#9562,#1940,.F.);
#12280=EDGE_CURVE('',#9562,#9563,#3008,.T.);
#12281=EDGE_CURVE('',#9563,#9504,#1941,.F.);
#12282=EDGE_CURVE('',#9562,#9564,#3009,.T.);
#12283=EDGE_CURVE('',#9564,#9565,#3010,.T.);
#12284=EDGE_CURVE('',#9565,#9566,#935,.T.);
#12285=EDGE_CURVE('',#9566,#9567,#3011,.T.);
#12286=EDGE_CURVE('',#9563,#9567,#3012,.T.);
#12287=EDGE_CURVE('',#9511,#9568,#1942,.F.);
#12288=EDGE_CURVE('',#9568,#9569,#3013,.T.);
#12289=EDGE_CURVE('',#9569,#9507,#1943,.F.);
#12290=EDGE_CURVE('',#9568,#9570,#3014,.T.);
#12291=EDGE_CURVE('',#9570,#9571,#3015,.T.);
#12292=EDGE_CURVE('',#9571,#9572,#936,.T.);
#12293=EDGE_CURVE('',#9572,#9573,#3016,.T.);
#12294=EDGE_CURVE('',#9569,#9573,#3017,.T.);
#12295=EDGE_CURVE('',#9509,#9574,#7970,.T.);
#12296=EDGE_CURVE('',#9574,#9508,#7971,.T.);
#12297=EDGE_CURVE('',#9506,#9575,#1944,.F.);
#12298=EDGE_CURVE('',#9575,#9576,#3018,.T.);
#12299=EDGE_CURVE('',#9576,#9510,#1945,.F.);
#12300=EDGE_CURVE('',#9575,#9577,#3019,.T.);
#12301=EDGE_CURVE('',#9577,#9578,#3020,.T.);
#12302=EDGE_CURVE('',#9578,#9579,#937,.T.);
#12303=EDGE_CURVE('',#9579,#9580,#3021,.T.);
#12304=EDGE_CURVE('',#9576,#9580,#3022,.T.);
#12305=EDGE_CURVE('',#9574,#9581,#938,.T.);
#12306=EDGE_CURVE('',#9581,#9582,#939,.T.);
#12307=EDGE_CURVE('',#9582,#9581,#940,.T.);
#12308=EDGE_CURVE('',#9569,#9575,#3023,.T.);
#12309=EDGE_CURVE('',#9573,#9577,#3024,.T.);
#12310=EDGE_CURVE('',#9576,#9568,#3025,.T.);
#12311=EDGE_CURVE('',#9580,#9570,#3026,.T.);
#12312=EDGE_CURVE('',#9557,#9562,#3027,.T.);
#12313=EDGE_CURVE('',#9561,#9564,#3028,.T.);
#12314=EDGE_CURVE('',#9563,#9556,#3029,.T.);
#12315=EDGE_CURVE('',#9567,#9558,#3030,.T.);
#12316=EDGE_CURVE('',#9513,#9583,#941,.T.);
#12317=EDGE_CURVE('',#9583,#9584,#942,.T.);
#12318=EDGE_CURVE('',#9584,#9583,#943,.T.);
#12319=EDGE_CURVE('',#9584,#9585,#3031,.T.);
#12320=EDGE_CURVE('',#9585,#9585,#944,.T.);
#12321=EDGE_CURVE('',#9512,#9586,#945,.T.);
#12322=EDGE_CURVE('',#9586,#9587,#946,.T.);
#12323=EDGE_CURVE('',#9587,#9586,#947,.T.);
#12324=EDGE_CURVE('',#9587,#9588,#3032,.T.);
#12325=EDGE_CURVE('',#9588,#9588,#948,.T.);
#12326=EDGE_CURVE('',#9582,#9589,#3033,.T.);
#12327=EDGE_CURVE('',#9589,#9589,#949,.T.);
#12328=EDGE_CURVE('',#9590,#9590,#950,.T.);
#12329=EDGE_CURVE('',#9590,#9487,#951,.T.);
#12330=EDGE_CURVE('',#9591,#9592,#952,.T.);
#12331=EDGE_CURVE('',#9592,#9545,#953,.T.);
#12332=EDGE_CURVE('',#9592,#9593,#954,.T.);
#12333=EDGE_CURVE('',#9593,#9591,#7972,.T.);
#12334=EDGE_CURVE('',#9593,#9551,#3034,.T.);
#12335=EDGE_CURVE('',#9594,#9495,#955,.T.);
#12336=EDGE_CURVE('',#9594,#9591,#3035,.T.);
#12337=EDGE_CURVE('',#9595,#9595,#956,.T.);
#12338=EDGE_CURVE('',#9595,#9535,#957,.T.);
#12339=EDGE_CURVE('',#9532,#9594,#3036,.T.);
#12340=EDGE_CURVE('',#9532,#9305,#3037,.T.);
#12341=EDGE_CURVE('',#9596,#9323,#3038,.T.);
#12342=EDGE_CURVE('',#9552,#9596,#3039,.T.);
#12343=EDGE_CURVE('',#9494,#9530,#958,.T.);
#12344=EDGE_CURVE('',#9529,#9495,#959,.T.);
#12345=EDGE_CURVE('',#9594,#9529,#960,.T.);
#12346=EDGE_CURVE('',#9542,#9530,#961,.T.);
#12347=EDGE_CURVE('',#9541,#9531,#962,.T.);
#12348=EDGE_CURVE('',#9596,#9597,#963,.T.);
#12349=EDGE_CURVE('',#9597,#9598,#3040,.T.);
#12350=EDGE_CURVE('',#9598,#9552,#1946,.F.);
#12351=EDGE_CURVE('',#9527,#9596,#964,.T.);
#12352=EDGE_CURVE('',#9527,#9597,#965,.T.);
#12353=EDGE_CURVE('',#9598,#9599,#3041,.T.);
#12354=EDGE_CURVE('',#9600,#9597,#3042,.T.);
#12355=EDGE_CURVE('',#9601,#9600,#3043,.T.);
#12356=EDGE_CURVE('',#9602,#9601,#3044,.T.);
#12357=EDGE_CURVE('',#9602,#9603,#3045,.T.);
#12358=EDGE_CURVE('',#9604,#9603,#966,.T.);
#12359=EDGE_CURVE('',#9604,#9605,#3046,.T.);
#12360=EDGE_CURVE('',#9606,#9605,#3047,.T.);
#12361=EDGE_CURVE('',#9607,#9606,#3048,.T.);
#12362=EDGE_CURVE('',#9599,#9607,#3049,.T.);
#12363=EDGE_CURVE('',#9600,#9531,#967,.T.);
#12364=EDGE_CURVE('',#9608,#9609,#968,.T.);
#12365=EDGE_CURVE('',#9609,#9391,#3050,.T.);
#12366=EDGE_CURVE('',#9312,#9608,#3051,.T.);
#12367=EDGE_CURVE('',#9607,#9608,#969,.T.);
#12368=EDGE_CURVE('',#9608,#9610,#3052,.T.);
#12369=EDGE_CURVE('',#9610,#9599,#970,.T.);
#12370=EDGE_CURVE('',#9553,#9610,#971,.T.);
#12371=EDGE_CURVE('',#9610,#9311,#3053,.T.);
#12372=EDGE_CURVE('',#9553,#9599,#972,.T.);
#12373=EDGE_CURVE('',#9607,#9609,#973,.T.);
#12374=EDGE_CURVE('',#9611,#9609,#3054,.T.);
#12375=EDGE_CURVE('',#9612,#9611,#3055,.T.);
#12376=EDGE_CURVE('',#9393,#9612,#3056,.T.);
#12377=EDGE_CURVE('',#9606,#9611,#974,.T.);
#12378=EDGE_CURVE('',#9600,#9541,#975,.T.);
#12379=EDGE_CURVE('',#9540,#9601,#1947,.F.);
#12380=EDGE_CURVE('',#9613,#9613,#976,.T.);
#12381=EDGE_CURVE('',#9613,#9614,#977,.T.);
#12382=EDGE_CURVE('',#9614,#9615,#978,.T.);
#12383=EDGE_CURVE('',#9615,#9614,#979,.T.);
#12384=EDGE_CURVE('',#9615,#9616,#3057,.T.);
#12385=EDGE_CURVE('',#9617,#9616,#7973,.T.);
#12386=EDGE_CURVE('',#9618,#9617,#980,.T.);
#12387=EDGE_CURVE('',#9618,#9619,#3058,.T.);
#12388=EDGE_CURVE('',#9619,#9620,#981,.T.);
#12389=EDGE_CURVE('',#9620,#9621,#3059,.T.);
#12390=EDGE_CURVE('',#9622,#9621,#982,.T.);
#12391=EDGE_CURVE('',#9623,#9622,#7974,.T.);
#12392=EDGE_CURVE('',#9623,#9624,#3060,.T.);
#12393=EDGE_CURVE('',#9624,#9625,#983,.T.);
#12394=EDGE_CURVE('',#9625,#9626,#3061,.T.);
#12395=EDGE_CURVE('',#9627,#9626,#7975,.T.);
#12396=EDGE_CURVE('',#9628,#9627,#7976,.T.);
#12397=EDGE_CURVE('',#9628,#9629,#3062,.T.);
#12398=EDGE_CURVE('',#9629,#9630,#984,.T.);
#12399=EDGE_CURVE('',#9630,#9631,#3063,.T.);
#12400=EDGE_CURVE('',#9616,#9631,#7977,.T.);
#12401=EDGE_CURVE('',#9603,#9491,#3064,.T.);
#12402=EDGE_CURVE('',#9555,#9602,#985,.F.);
#12403=EDGE_CURVE('',#9632,#9632,#986,.T.);
#12404=EDGE_CURVE('',#9633,#9634,#1948,.T.);
#12405=EDGE_CURVE('',#9634,#9617,#3065,.T.);
#12406=EDGE_CURVE('',#9631,#9635,#3066,.T.);
#12407=EDGE_CURVE('',#9635,#9633,#1949,.F.);
#12408=EDGE_CURVE('',#9630,#9636,#3067,.T.);
#12409=EDGE_CURVE('',#9635,#9636,#3068,.T.);
#12410=EDGE_CURVE('',#9637,#9634,#3069,.T.);
#12411=EDGE_CURVE('',#9622,#9637,#987,.T.);
#12412=EDGE_CURVE('',#9621,#9638,#3070,.T.);
#12413=EDGE_CURVE('',#9638,#9618,#3071,.T.);
#12414=EDGE_CURVE('',#9639,#9640,#3072,.T.);
#12415=EDGE_CURVE('',#9641,#9640,#3073,.T.);
#12416=EDGE_CURVE('',#9641,#9642,#3074,.T.);
#12417=EDGE_CURVE('',#9639,#9642,#3075,.T.);
#12418=EDGE_CURVE('',#9643,#9644,#1950,.T.);
#12419=EDGE_CURVE('',#9644,#9645,#3076,.T.);
#12420=EDGE_CURVE('',#9645,#9646,#1951,.T.);
#12421=EDGE_CURVE('',#9647,#9646,#1952,.T.);
#12422=EDGE_CURVE('',#9647,#9648,#3077,.T.);
#12423=EDGE_CURVE('',#9648,#9643,#1953,.F.);
#12424=EDGE_CURVE('',#9646,#9649,#1954,.T.);
#12425=EDGE_CURVE('',#9645,#9650,#3078,.T.);
#12426=EDGE_CURVE('',#9606,#9650,#988,.T.);
#12427=EDGE_CURVE('',#9605,#9641,#989,.T.);
#12428=EDGE_CURVE('',#9640,#9651,#1955,.T.);
#12429=EDGE_CURVE('',#9651,#9652,#1956,.T.);
#12430=EDGE_CURVE('',#9652,#9653,#3079,.T.);
#12431=EDGE_CURVE('',#9653,#9654,#1957,.T.);
#12432=EDGE_CURVE('',#9654,#9655,#3080,.T.);
#12433=EDGE_CURVE('',#9655,#9656,#1958,.T.);
#12434=EDGE_CURVE('',#9656,#9649,#3081,.T.);
#12435=EDGE_CURVE('',#9657,#9644,#3082,.T.);
#12436=EDGE_CURVE('',#9650,#9657,#3083,.T.);
#12437=EDGE_CURVE('',#9658,#9659,#3084,.T.);
#12438=EDGE_CURVE('',#9660,#9659,#3085,.T.);
#12439=EDGE_CURVE('',#9660,#9661,#3086,.T.);
#12440=EDGE_CURVE('',#9658,#9661,#3087,.T.);
#12441=EDGE_CURVE('',#9662,#9649,#3088,.T.);
#12442=EDGE_CURVE('',#9656,#9663,#3089,.T.);
#12443=EDGE_CURVE('',#9663,#9664,#990,.T.);
#12444=EDGE_CURVE('',#9662,#9664,#991,.T.);
#12445=EDGE_CURVE('',#9665,#9666,#1959,.T.);
#12446=EDGE_CURVE('',#9667,#9666,#1960,.T.);
#12447=EDGE_CURVE('',#9667,#9647,#3090,.T.);
#12448=EDGE_CURVE('',#9662,#9668,#7978,.T.);
#12449=EDGE_CURVE('',#9668,#9669,#3091,.T.);
#12450=EDGE_CURVE('',#9669,#9670,#1961,.T.);
#12451=EDGE_CURVE('',#9670,#9665,#3092,.T.);
#12452=EDGE_CURVE('',#9666,#9659,#1962,.T.);
#12453=EDGE_CURVE('',#9666,#9671,#1963,.F.);
#12454=EDGE_CURVE('',#9671,#9628,#3093,.T.);
#12455=EDGE_CURVE('',#9627,#9672,#3094,.T.);
#12456=EDGE_CURVE('',#9672,#9660,#1964,.T.);
#12457=EDGE_CURVE('',#9665,#9652,#3095,.T.);
#12458=EDGE_CURVE('',#9651,#9673,#1965,.F.);
#12459=EDGE_CURVE('',#9673,#9671,#3096,.T.);
#12460=EDGE_CURVE('',#9670,#9653,#3097,.T.);
#12461=EDGE_CURVE('',#9674,#9669,#1966,.F.);
#12462=EDGE_CURVE('',#9674,#9675,#3098,.T.);
#12463=EDGE_CURVE('',#9675,#9676,#3099,.T.);
#12464=EDGE_CURVE('',#9677,#9676,#3100,.T.);
#12465=EDGE_CURVE('',#9654,#9677,#1967,.F.);
#12466=EDGE_CURVE('',#9668,#9678,#992,.T.);
#12467=EDGE_CURVE('',#9678,#9674,#3101,.T.);
#12468=EDGE_CURVE('',#9679,#9672,#1968,.F.);
#12469=EDGE_CURVE('',#9679,#9680,#3102,.T.);
#12470=EDGE_CURVE('',#9680,#9681,#3103,.T.);
#12471=EDGE_CURVE('',#9682,#9681,#3104,.T.);
#12472=EDGE_CURVE('',#9683,#9682,#1969,.F.);
#12473=EDGE_CURVE('',#9661,#9683,#1970,.T.);
#12474=EDGE_CURVE('',#9626,#9679,#3105,.T.);
#12475=EDGE_CURVE('',#9612,#9488,#993,.T.);
#12476=EDGE_CURVE('',#9611,#9650,#994,.T.);
#12477=EDGE_CURVE('',#9657,#9612,#995,.T.);
#12478=EDGE_CURVE('',#9657,#9488,#996,.T.);
#12479=EDGE_CURVE('',#9639,#9633,#1971,.T.);
#12480=EDGE_CURVE('',#9642,#9489,#997,.T.);
#12481=EDGE_CURVE('',#9658,#9643,#1972,.T.);
#12482=EDGE_CURVE('',#9683,#9684,#3106,.T.);
#12483=EDGE_CURVE('',#9684,#9637,#7979,.T.);
#12484=EDGE_CURVE('',#9490,#9604,#3107,.T.);
#12485=EDGE_CURVE('',#9547,#9447,#998,.T.);
#12486=EDGE_CURVE('',#9450,#9685,#7980,.F.);
#12487=EDGE_CURVE('',#9685,#9686,#999,.T.);
#12488=EDGE_CURVE('',#9686,#9449,#7981,.F.);
#12489=EDGE_CURVE('',#9344,#9685,#3108,.T.);
#12490=EDGE_CURVE('',#9687,#9343,#3109,.T.);
#12491=EDGE_CURVE('',#9686,#9687,#3110,.T.);
#12492=EDGE_CURVE('',#9445,#9687,#3111,.T.);
#12493=EDGE_CURVE('',#9623,#9684,#1000,.T.);
#12494=EDGE_CURVE('',#9682,#9623,#3112,.T.);
#12495=EDGE_CURVE('',#9688,#9655,#1973,.F.);
#12496=EDGE_CURVE('',#9688,#9689,#3113,.T.);
#12497=EDGE_CURVE('',#9689,#9690,#3114,.T.);
#12498=EDGE_CURVE('',#9691,#9690,#7982,.F.);
#12499=EDGE_CURVE('',#9663,#9691,#3115,.T.);
#12500=EDGE_CURVE('',#9677,#9688,#3116,.T.);
#12501=EDGE_CURVE('',#9673,#9692,#3117,.T.);
#12502=EDGE_CURVE('',#9692,#9693,#3118,.T.);
#12503=EDGE_CURVE('',#9671,#9693,#3119,.T.);
#12504=EDGE_CURVE('',#9635,#9673,#3120,.T.);
#12505=EDGE_CURVE('',#9636,#9692,#3121,.T.);
#12506=EDGE_CURVE('',#9648,#9667,#3122,.T.);
#12507=EDGE_CURVE('',#9648,#9694,#3123,.T.);
#12508=EDGE_CURVE('',#9694,#9695,#3124,.T.);
#12509=EDGE_CURVE('',#9667,#9695,#3125,.T.);
#12510=EDGE_CURVE('',#9681,#9624,#3126,.T.);
#12511=EDGE_CURVE('',#9632,#9696,#1001,.T.);
#12512=EDGE_CURVE('',#9696,#9697,#1002,.T.);
#12513=EDGE_CURVE('',#9697,#9696,#1003,.T.);
#12514=EDGE_CURVE('',#9697,#9698,#3127,.T.);
#12515=EDGE_CURVE('',#9699,#9698,#1004,.T.);
#12516=EDGE_CURVE('',#9699,#9678,#3128,.T.);
#12517=EDGE_CURVE('',#9664,#9678,#7983,.T.);
#12518=EDGE_CURVE('',#9698,#9691,#1005,.T.);
#12519=EDGE_CURVE('',#9676,#9689,#3129,.T.);
#12520=EDGE_CURVE('',#9690,#9700,#1006,.T.);
#12521=EDGE_CURVE('',#9700,#9699,#7984,.F.);
#12522=EDGE_CURVE('',#9700,#9675,#3130,.T.);
#12523=EDGE_CURVE('',#9625,#9680,#3131,.T.);
#12524=EDGE_CURVE('',#9620,#9701,#3132,.T.);
#12525=EDGE_CURVE('',#9638,#9701,#3133,.T.);
#12526=EDGE_CURVE('',#9701,#9619,#3134,.T.);
#12527=EDGE_CURVE('',#9693,#9629,#3135,.T.);
#12528=EDGE_CURVE('',#9647,#9702,#3136,.T.);
#12529=EDGE_CURVE('',#9702,#9694,#3137,.T.);
#12530=EDGE_CURVE('',#9695,#9702,#3138,.T.);
#12531=EDGE_CURVE('',#9438,#9524,#3139,.T.);
#12532=EDGE_CURVE('',#9440,#9703,#3140,.T.);
#12533=EDGE_CURVE('',#9353,#9703,#3141,.T.);
#12534=EDGE_CURVE('',#9703,#9439,#3142,.T.);
#12535=EDGE_CURVE('',#9427,#9704,#3143,.T.);
#12536=EDGE_CURVE('',#9704,#9434,#3144,.T.);
#12537=EDGE_CURVE('',#9520,#9704,#3145,.T.);
#12538=EDGE_CURVE('',#9435,#9519,#3146,.T.);
#12539=EDGE_CURVE('',#9572,#9578,#3147,.T.);
#12540=EDGE_CURVE('',#9579,#9571,#3148,.T.);
#12541=EDGE_CURVE('',#9560,#9565,#3149,.T.);
#12542=EDGE_CURVE('',#9566,#9559,#3150,.T.);
#16737=ORIENTED_EDGE('',*,*,#11843,.F.);
#16738=ORIENTED_EDGE('',*,*,#11844,.T.);
#16739=ORIENTED_EDGE('',*,*,#11845,.T.);
#16740=ORIENTED_EDGE('',*,*,#11846,.T.);
#16741=ORIENTED_EDGE('',*,*,#11846,.F.);
#16742=ORIENTED_EDGE('',*,*,#11847,.F.);
#16743=ORIENTED_EDGE('',*,*,#11848,.F.);
#16744=ORIENTED_EDGE('',*,*,#11849,.T.);
#16745=ORIENTED_EDGE('',*,*,#11850,.T.);
#16746=ORIENTED_EDGE('',*,*,#11851,.T.);
#16747=ORIENTED_EDGE('',*,*,#11852,.T.);
#16748=ORIENTED_EDGE('',*,*,#11852,.F.);
#16749=ORIENTED_EDGE('',*,*,#11853,.T.);
#16750=ORIENTED_EDGE('',*,*,#11854,.T.);
#16751=ORIENTED_EDGE('',*,*,#11855,.T.);
#16752=ORIENTED_EDGE('',*,*,#11856,.F.);
#16753=ORIENTED_EDGE('',*,*,#11857,.F.);
#16754=ORIENTED_EDGE('',*,*,#11858,.T.);
#16755=ORIENTED_EDGE('',*,*,#11859,.T.);
#16756=ORIENTED_EDGE('',*,*,#11860,.T.);
#16757=ORIENTED_EDGE('',*,*,#11859,.F.);
#16758=ORIENTED_EDGE('',*,*,#11861,.T.);
#16759=ORIENTED_EDGE('',*,*,#11862,.T.);
#16760=ORIENTED_EDGE('',*,*,#11863,.T.);
#16761=ORIENTED_EDGE('',*,*,#11864,.T.);
#16762=ORIENTED_EDGE('',*,*,#11865,.T.);
#16763=ORIENTED_EDGE('',*,*,#11866,.T.);
#16764=ORIENTED_EDGE('',*,*,#11862,.F.);
#16765=ORIENTED_EDGE('',*,*,#11855,.F.);
#16766=ORIENTED_EDGE('',*,*,#11860,.F.);
#16767=ORIENTED_EDGE('',*,*,#11866,.F.);
#16768=ORIENTED_EDGE('',*,*,#11867,.T.);
#16769=ORIENTED_EDGE('',*,*,#11868,.F.);
#16770=ORIENTED_EDGE('',*,*,#11869,.T.);
#16771=ORIENTED_EDGE('',*,*,#11870,.T.);
#16772=ORIENTED_EDGE('',*,*,#11871,.T.);
#16773=ORIENTED_EDGE('',*,*,#11872,.F.);
#16774=ORIENTED_EDGE('',*,*,#11871,.F.);
#16775=ORIENTED_EDGE('',*,*,#11873,.F.);
#16776=ORIENTED_EDGE('',*,*,#11874,.T.);
#16777=ORIENTED_EDGE('',*,*,#11875,.T.);
#16778=ORIENTED_EDGE('',*,*,#11876,.T.);
#16779=ORIENTED_EDGE('',*,*,#11877,.T.);
#16780=ORIENTED_EDGE('',*,*,#11878,.T.);
#16781=ORIENTED_EDGE('',*,*,#11876,.F.);
#16782=ORIENTED_EDGE('',*,*,#11879,.F.);
#16783=ORIENTED_EDGE('',*,*,#11880,.F.);
#16784=ORIENTED_EDGE('',*,*,#11881,.F.);
#16785=ORIENTED_EDGE('',*,*,#11882,.T.);
#16786=ORIENTED_EDGE('',*,*,#11883,.T.);
#16787=ORIENTED_EDGE('',*,*,#11884,.T.);
#16788=ORIENTED_EDGE('',*,*,#11880,.T.);
#16789=ORIENTED_EDGE('',*,*,#11883,.F.);
#16790=ORIENTED_EDGE('',*,*,#11885,.F.);
#16791=ORIENTED_EDGE('',*,*,#11886,.F.);
#16792=ORIENTED_EDGE('',*,*,#11887,.T.);
#16793=ORIENTED_EDGE('',*,*,#11888,.F.);
#16794=ORIENTED_EDGE('',*,*,#11889,.F.);
#16795=ORIENTED_EDGE('',*,*,#11890,.F.);
#16796=ORIENTED_EDGE('',*,*,#11891,.F.);
#16797=ORIENTED_EDGE('',*,*,#11892,.T.);
#16798=ORIENTED_EDGE('',*,*,#11893,.T.);
#16799=ORIENTED_EDGE('',*,*,#11894,.F.);
#16800=ORIENTED_EDGE('',*,*,#11895,.F.);
#16801=ORIENTED_EDGE('',*,*,#11896,.F.);
#16802=ORIENTED_EDGE('',*,*,#11897,.T.);
#16803=ORIENTED_EDGE('',*,*,#11898,.F.);
#16804=ORIENTED_EDGE('',*,*,#11856,.T.);
#16805=ORIENTED_EDGE('',*,*,#11867,.F.);
#16806=ORIENTED_EDGE('',*,*,#11865,.F.);
#16807=ORIENTED_EDGE('',*,*,#11899,.F.);
#16808=ORIENTED_EDGE('',*,*,#11900,.F.);
#16809=ORIENTED_EDGE('',*,*,#11895,.T.);
#16810=ORIENTED_EDGE('',*,*,#11901,.T.);
#16811=ORIENTED_EDGE('',*,*,#11902,.T.);
#16812=ORIENTED_EDGE('',*,*,#11903,.T.);
#16813=ORIENTED_EDGE('',*,*,#11904,.T.);
#16814=ORIENTED_EDGE('',*,*,#11905,.T.);
#16815=ORIENTED_EDGE('',*,*,#11906,.T.);
#16816=ORIENTED_EDGE('',*,*,#11896,.T.);
#16817=ORIENTED_EDGE('',*,*,#11904,.F.);
#16818=ORIENTED_EDGE('',*,*,#11907,.T.);
#16819=ORIENTED_EDGE('',*,*,#11908,.T.);
#16820=ORIENTED_EDGE('',*,*,#11909,.T.);
#16821=ORIENTED_EDGE('',*,*,#11910,.F.);
#16822=ORIENTED_EDGE('',*,*,#11911,.T.);
#16823=ORIENTED_EDGE('',*,*,#11912,.F.);
#16824=ORIENTED_EDGE('',*,*,#11913,.T.);
#16825=ORIENTED_EDGE('',*,*,#11914,.T.);
#16826=ORIENTED_EDGE('',*,*,#11915,.T.);
#16827=ORIENTED_EDGE('',*,*,#11916,.T.);
#16828=ORIENTED_EDGE('',*,*,#11917,.T.);
#16829=ORIENTED_EDGE('',*,*,#11918,.T.);
#16830=ORIENTED_EDGE('',*,*,#11919,.T.);
#16831=ORIENTED_EDGE('',*,*,#11920,.T.);
#16832=ORIENTED_EDGE('',*,*,#11921,.T.);
#16833=ORIENTED_EDGE('',*,*,#11911,.F.);
#16834=ORIENTED_EDGE('',*,*,#11922,.T.);
#16835=ORIENTED_EDGE('',*,*,#11923,.T.);
#16836=ORIENTED_EDGE('',*,*,#11924,.F.);
#16837=ORIENTED_EDGE('',*,*,#11913,.F.);
#16838=ORIENTED_EDGE('',*,*,#11925,.F.);
#16839=ORIENTED_EDGE('',*,*,#11926,.T.);
#16840=ORIENTED_EDGE('',*,*,#11927,.F.);
#16841=ORIENTED_EDGE('',*,*,#11920,.F.);
#16842=ORIENTED_EDGE('',*,*,#11928,.F.);
#16843=ORIENTED_EDGE('',*,*,#11929,.T.);
#16844=ORIENTED_EDGE('',*,*,#11930,.T.);
#16845=ORIENTED_EDGE('',*,*,#11916,.F.);
#16846=ORIENTED_EDGE('',*,*,#11931,.F.);
#16847=ORIENTED_EDGE('',*,*,#11932,.F.);
#16848=ORIENTED_EDGE('',*,*,#11933,.F.);
#16849=ORIENTED_EDGE('',*,*,#11934,.T.);
#16850=ORIENTED_EDGE('',*,*,#11935,.T.);
#16851=ORIENTED_EDGE('',*,*,#11936,.T.);
#16852=ORIENTED_EDGE('',*,*,#11937,.T.);
#16853=ORIENTED_EDGE('',*,*,#11938,.T.);
#16854=ORIENTED_EDGE('',*,*,#11939,.T.);
#16855=ORIENTED_EDGE('',*,*,#11940,.F.);
#16856=ORIENTED_EDGE('',*,*,#11941,.F.);
#16857=ORIENTED_EDGE('',*,*,#11942,.F.);
#16858=ORIENTED_EDGE('',*,*,#11943,.F.);
#16859=ORIENTED_EDGE('',*,*,#11944,.T.);
#16860=ORIENTED_EDGE('',*,*,#11945,.F.);
#16861=ORIENTED_EDGE('',*,*,#11946,.T.);
#16862=ORIENTED_EDGE('',*,*,#11947,.T.);
#16863=ORIENTED_EDGE('',*,*,#11941,.T.);
#16864=ORIENTED_EDGE('',*,*,#11948,.T.);
#16865=ORIENTED_EDGE('',*,*,#11949,.F.);
#16866=ORIENTED_EDGE('',*,*,#11909,.F.);
#16867=ORIENTED_EDGE('',*,*,#11950,.F.);
#16868=ORIENTED_EDGE('',*,*,#11951,.F.);
#16869=ORIENTED_EDGE('',*,*,#11945,.T.);
#16870=ORIENTED_EDGE('',*,*,#11908,.F.);
#16871=ORIENTED_EDGE('',*,*,#11952,.T.);
#16872=ORIENTED_EDGE('',*,*,#11953,.T.);
#16873=ORIENTED_EDGE('',*,*,#11954,.T.);
#16874=ORIENTED_EDGE('',*,*,#11932,.T.);
#16875=ORIENTED_EDGE('',*,*,#11955,.F.);
#16876=ORIENTED_EDGE('',*,*,#11956,.T.);
#16877=ORIENTED_EDGE('',*,*,#11950,.T.);
#16878=ORIENTED_EDGE('',*,*,#11957,.T.);
#16879=ORIENTED_EDGE('',*,*,#11958,.T.);
#16880=ORIENTED_EDGE('',*,*,#11901,.F.);
#16881=ORIENTED_EDGE('',*,*,#11894,.T.);
#16882=ORIENTED_EDGE('',*,*,#11959,.T.);
#16883=ORIENTED_EDGE('',*,*,#11960,.T.);
#16884=ORIENTED_EDGE('',*,*,#11961,.T.);
#16885=ORIENTED_EDGE('',*,*,#11962,.T.);
#16886=ORIENTED_EDGE('',*,*,#11963,.T.);
#16887=ORIENTED_EDGE('',*,*,#11964,.F.);
#16888=ORIENTED_EDGE('',*,*,#11965,.T.);
#16889=ORIENTED_EDGE('',*,*,#11966,.T.);
#16890=ORIENTED_EDGE('',*,*,#11967,.T.);
#16891=ORIENTED_EDGE('',*,*,#11892,.F.);
#16892=ORIENTED_EDGE('',*,*,#11966,.F.);
#16893=ORIENTED_EDGE('',*,*,#11968,.T.);
#16894=ORIENTED_EDGE('',*,*,#11962,.F.);
#16895=ORIENTED_EDGE('',*,*,#11960,.F.);
#16896=ORIENTED_EDGE('',*,*,#11969,.T.);
#16897=ORIENTED_EDGE('',*,*,#11957,.F.);
#16898=ORIENTED_EDGE('',*,*,#11958,.F.);
#16899=ORIENTED_EDGE('',*,*,#11970,.F.);
#16900=ORIENTED_EDGE('',*,*,#11971,.T.);
#16901=ORIENTED_EDGE('',*,*,#11972,.F.);
#16902=ORIENTED_EDGE('',*,*,#11973,.F.);
#16903=ORIENTED_EDGE('',*,*,#11902,.F.);
#16904=ORIENTED_EDGE('',*,*,#11969,.F.);
#16905=ORIENTED_EDGE('',*,*,#11974,.T.);
#16906=ORIENTED_EDGE('',*,*,#11975,.T.);
#16907=ORIENTED_EDGE('',*,*,#11970,.T.);
#16908=ORIENTED_EDGE('',*,*,#11963,.F.);
#16909=ORIENTED_EDGE('',*,*,#11976,.F.);
#16910=ORIENTED_EDGE('',*,*,#11946,.F.);
#16911=ORIENTED_EDGE('',*,*,#11977,.F.);
#16912=ORIENTED_EDGE('',*,*,#11978,.F.);
#16913=ORIENTED_EDGE('',*,*,#11979,.F.);
#16914=ORIENTED_EDGE('',*,*,#11980,.F.);
#16915=ORIENTED_EDGE('',*,*,#11981,.F.);
#16916=ORIENTED_EDGE('',*,*,#11982,.F.);
#16917=ORIENTED_EDGE('',*,*,#11974,.F.);
#16918=ORIENTED_EDGE('',*,*,#11968,.F.);
#16919=ORIENTED_EDGE('',*,*,#11983,.T.);
#16920=ORIENTED_EDGE('',*,*,#11984,.T.);
#16921=ORIENTED_EDGE('',*,*,#11976,.T.);
#16922=ORIENTED_EDGE('',*,*,#11965,.F.);
#16923=ORIENTED_EDGE('',*,*,#11985,.F.);
#16924=ORIENTED_EDGE('',*,*,#11986,.F.);
#16925=ORIENTED_EDGE('',*,*,#11987,.F.);
#16926=ORIENTED_EDGE('',*,*,#11988,.F.);
#16927=ORIENTED_EDGE('',*,*,#11983,.F.);
#16928=ORIENTED_EDGE('',*,*,#11989,.T.);
#16929=ORIENTED_EDGE('',*,*,#11890,.T.);
#16930=ORIENTED_EDGE('',*,*,#11990,.T.);
#16931=ORIENTED_EDGE('',*,*,#11991,.T.);
#16932=ORIENTED_EDGE('',*,*,#11992,.T.);
#16933=ORIENTED_EDGE('',*,*,#11993,.T.);
#16934=ORIENTED_EDGE('',*,*,#11990,.F.);
#16935=ORIENTED_EDGE('',*,*,#11889,.T.);
#16936=ORIENTED_EDGE('',*,*,#11994,.T.);
#16937=ORIENTED_EDGE('',*,*,#11985,.T.);
#16938=ORIENTED_EDGE('',*,*,#11964,.T.);
#16939=ORIENTED_EDGE('',*,*,#11891,.T.);
#16940=ORIENTED_EDGE('',*,*,#11989,.F.);
#16941=ORIENTED_EDGE('',*,*,#11995,.T.);
#16942=ORIENTED_EDGE('',*,*,#11993,.F.);
#16943=ORIENTED_EDGE('',*,*,#11996,.T.);
#16944=ORIENTED_EDGE('',*,*,#11997,.F.);
#16945=ORIENTED_EDGE('',*,*,#11998,.F.);
#16946=ORIENTED_EDGE('',*,*,#11999,.F.);
#16947=ORIENTED_EDGE('',*,*,#12000,.T.);
#16948=ORIENTED_EDGE('',*,*,#12001,.T.);
#16949=ORIENTED_EDGE('',*,*,#12002,.T.);
#16950=ORIENTED_EDGE('',*,*,#12003,.F.);
#16951=ORIENTED_EDGE('',*,*,#12004,.T.);
#16952=ORIENTED_EDGE('',*,*,#12001,.F.);
#16953=ORIENTED_EDGE('',*,*,#12005,.T.);
#16954=ORIENTED_EDGE('',*,*,#12003,.T.);
#16955=ORIENTED_EDGE('',*,*,#12006,.F.);
#16956=ORIENTED_EDGE('',*,*,#12007,.F.);
#16957=ORIENTED_EDGE('',*,*,#12008,.F.);
#16958=ORIENTED_EDGE('',*,*,#11869,.F.);
#16959=ORIENTED_EDGE('',*,*,#12009,.F.);
#16960=ORIENTED_EDGE('',*,*,#12010,.T.);
#16961=ORIENTED_EDGE('',*,*,#12011,.F.);
#16962=ORIENTED_EDGE('',*,*,#11863,.F.);
#16963=ORIENTED_EDGE('',*,*,#12012,.T.);
#16964=ORIENTED_EDGE('',*,*,#12002,.F.);
#16965=ORIENTED_EDGE('',*,*,#12013,.T.);
#16966=ORIENTED_EDGE('',*,*,#11858,.F.);
#16967=ORIENTED_EDGE('',*,*,#12014,.F.);
#16968=ORIENTED_EDGE('',*,*,#12015,.T.);
#16969=ORIENTED_EDGE('',*,*,#12016,.F.);
#16970=ORIENTED_EDGE('',*,*,#11849,.F.);
#16971=ORIENTED_EDGE('',*,*,#12017,.F.);
#16972=ORIENTED_EDGE('',*,*,#12018,.F.);
#16973=ORIENTED_EDGE('',*,*,#12019,.F.);
#16974=ORIENTED_EDGE('',*,*,#11844,.F.);
#16975=ORIENTED_EDGE('',*,*,#12000,.F.);
#16976=ORIENTED_EDGE('',*,*,#12005,.F.);
#16977=ORIENTED_EDGE('',*,*,#12020,.F.);
#16978=ORIENTED_EDGE('',*,*,#12020,.T.);
#16979=ORIENTED_EDGE('',*,*,#12021,.T.);
#16980=ORIENTED_EDGE('',*,*,#12022,.T.);
#16981=ORIENTED_EDGE('',*,*,#12023,.T.);
#16982=ORIENTED_EDGE('',*,*,#12021,.F.);
#16983=ORIENTED_EDGE('',*,*,#12024,.F.);
#16984=ORIENTED_EDGE('',*,*,#12025,.F.);
#16985=ORIENTED_EDGE('',*,*,#12026,.T.);
#16986=ORIENTED_EDGE('',*,*,#12022,.F.);
#16987=ORIENTED_EDGE('',*,*,#12023,.F.);
#16988=ORIENTED_EDGE('',*,*,#12026,.F.);
#16989=ORIENTED_EDGE('',*,*,#12027,.T.);
#16990=ORIENTED_EDGE('',*,*,#12024,.T.);
#16991=ORIENTED_EDGE('',*,*,#12025,.T.);
#16992=ORIENTED_EDGE('',*,*,#12027,.F.);
#16993=ORIENTED_EDGE('',*,*,#12028,.T.);
#16994=ORIENTED_EDGE('',*,*,#11991,.F.);
#16995=ORIENTED_EDGE('',*,*,#11999,.T.);
#16996=ORIENTED_EDGE('',*,*,#12029,.F.);
#16997=ORIENTED_EDGE('',*,*,#12030,.F.);
#16998=ORIENTED_EDGE('',*,*,#12031,.F.);
#16999=ORIENTED_EDGE('',*,*,#12032,.F.);
#17000=ORIENTED_EDGE('',*,*,#12028,.F.);
#17001=ORIENTED_EDGE('',*,*,#12033,.T.);
#17002=ORIENTED_EDGE('',*,*,#12034,.T.);
#17003=ORIENTED_EDGE('',*,*,#12035,.T.);
#17004=ORIENTED_EDGE('',*,*,#12034,.F.);
#17005=ORIENTED_EDGE('',*,*,#12033,.F.);
#17006=ORIENTED_EDGE('',*,*,#12036,.F.);
#17007=ORIENTED_EDGE('',*,*,#11885,.T.);
#17008=ORIENTED_EDGE('',*,*,#11882,.F.);
#17009=ORIENTED_EDGE('',*,*,#12037,.T.);
#17010=ORIENTED_EDGE('',*,*,#12038,.F.);
#17011=ORIENTED_EDGE('',*,*,#12039,.T.);
#17012=ORIENTED_EDGE('',*,*,#12040,.T.);
#17013=ORIENTED_EDGE('',*,*,#12041,.T.);
#17014=ORIENTED_EDGE('',*,*,#12042,.T.);
#17015=ORIENTED_EDGE('',*,*,#12043,.T.);
#17016=ORIENTED_EDGE('',*,*,#12044,.T.);
#17017=ORIENTED_EDGE('',*,*,#12045,.T.);
#17018=ORIENTED_EDGE('',*,*,#12046,.T.);
#17019=ORIENTED_EDGE('',*,*,#12043,.F.);
#17020=ORIENTED_EDGE('',*,*,#12047,.T.);
#17021=ORIENTED_EDGE('',*,*,#12041,.F.);
#17022=ORIENTED_EDGE('',*,*,#11955,.T.);
#17023=ORIENTED_EDGE('',*,*,#12048,.T.);
#17024=ORIENTED_EDGE('',*,*,#12045,.F.);
#17025=ORIENTED_EDGE('',*,*,#11951,.T.);
#17026=ORIENTED_EDGE('',*,*,#12049,.T.);
#17027=ORIENTED_EDGE('',*,*,#12050,.T.);
#17028=ORIENTED_EDGE('',*,*,#11977,.T.);
#17029=ORIENTED_EDGE('',*,*,#12039,.F.);
#17030=ORIENTED_EDGE('',*,*,#12051,.T.);
#17031=ORIENTED_EDGE('',*,*,#12050,.F.);
#17032=ORIENTED_EDGE('',*,*,#11954,.F.);
#17033=ORIENTED_EDGE('',*,*,#12052,.F.);
#17034=ORIENTED_EDGE('',*,*,#12053,.T.);
#17035=ORIENTED_EDGE('',*,*,#12054,.T.);
#17036=ORIENTED_EDGE('',*,*,#12055,.T.);
#17037=ORIENTED_EDGE('',*,*,#11933,.T.);
#17038=ORIENTED_EDGE('',*,*,#11953,.F.);
#17039=ORIENTED_EDGE('',*,*,#12056,.F.);
#17040=ORIENTED_EDGE('',*,*,#12057,.T.);
#17041=ORIENTED_EDGE('',*,*,#12052,.T.);
#17042=ORIENTED_EDGE('',*,*,#11907,.F.);
#17043=ORIENTED_EDGE('',*,*,#12058,.T.);
#17044=ORIENTED_EDGE('',*,*,#12059,.T.);
#17045=ORIENTED_EDGE('',*,*,#12056,.T.);
#17046=ORIENTED_EDGE('',*,*,#11952,.F.);
#17047=ORIENTED_EDGE('',*,*,#12040,.F.);
#17048=ORIENTED_EDGE('',*,*,#12049,.F.);
#17049=ORIENTED_EDGE('',*,*,#11956,.F.);
#17050=ORIENTED_EDGE('',*,*,#12044,.F.);
#17051=ORIENTED_EDGE('',*,*,#12060,.F.);
#17052=ORIENTED_EDGE('',*,*,#11943,.T.);
#17053=ORIENTED_EDGE('',*,*,#12061,.F.);
#17054=ORIENTED_EDGE('',*,*,#12062,.T.);
#17055=ORIENTED_EDGE('',*,*,#12048,.F.);
#17056=ORIENTED_EDGE('',*,*,#11931,.T.);
#17057=ORIENTED_EDGE('',*,*,#11915,.F.);
#17058=ORIENTED_EDGE('',*,*,#12063,.F.);
#17059=ORIENTED_EDGE('',*,*,#12064,.T.);
#17060=ORIENTED_EDGE('',*,*,#12054,.F.);
#17061=ORIENTED_EDGE('',*,*,#12065,.T.);
#17062=ORIENTED_EDGE('',*,*,#12066,.T.);
#17063=ORIENTED_EDGE('',*,*,#12067,.T.);
#17064=ORIENTED_EDGE('',*,*,#11929,.F.);
#17065=ORIENTED_EDGE('',*,*,#12068,.F.);
#17066=ORIENTED_EDGE('',*,*,#12069,.T.);
#17067=ORIENTED_EDGE('',*,*,#12070,.T.);
#17068=ORIENTED_EDGE('',*,*,#12071,.T.);
#17069=ORIENTED_EDGE('',*,*,#11937,.F.);
#17070=ORIENTED_EDGE('',*,*,#12072,.T.);
#17071=ORIENTED_EDGE('',*,*,#12073,.T.);
#17072=ORIENTED_EDGE('',*,*,#12074,.T.);
#17073=ORIENTED_EDGE('',*,*,#11934,.F.);
#17074=ORIENTED_EDGE('',*,*,#12055,.F.);
#17075=ORIENTED_EDGE('',*,*,#12064,.F.);
#17076=ORIENTED_EDGE('',*,*,#12075,.F.);
#17077=ORIENTED_EDGE('',*,*,#12076,.T.);
#17078=ORIENTED_EDGE('',*,*,#11925,.T.);
#17079=ORIENTED_EDGE('',*,*,#11912,.T.);
#17080=ORIENTED_EDGE('',*,*,#12077,.T.);
#17081=ORIENTED_EDGE('',*,*,#12078,.T.);
#17082=ORIENTED_EDGE('',*,*,#12079,.T.);
#17083=ORIENTED_EDGE('',*,*,#12080,.T.);
#17084=ORIENTED_EDGE('',*,*,#12081,.T.);
#17085=ORIENTED_EDGE('',*,*,#12082,.F.);
#17086=ORIENTED_EDGE('',*,*,#12083,.T.);
#17087=ORIENTED_EDGE('',*,*,#12084,.F.);
#17088=ORIENTED_EDGE('',*,*,#12085,.T.);
#17089=ORIENTED_EDGE('',*,*,#12078,.F.);
#17090=ORIENTED_EDGE('',*,*,#12086,.T.);
#17091=ORIENTED_EDGE('',*,*,#12087,.F.);
#17092=ORIENTED_EDGE('',*,*,#12083,.F.);
#17093=ORIENTED_EDGE('',*,*,#12088,.T.);
#17094=ORIENTED_EDGE('',*,*,#12089,.T.);
#17095=ORIENTED_EDGE('',*,*,#12090,.T.);
#17096=ORIENTED_EDGE('',*,*,#11981,.T.);
#17097=ORIENTED_EDGE('',*,*,#12091,.T.);
#17098=ORIENTED_EDGE('',*,*,#11980,.T.);
#17099=ORIENTED_EDGE('',*,*,#12092,.T.);
#17100=ORIENTED_EDGE('',*,*,#12093,.T.);
#17101=ORIENTED_EDGE('',*,*,#12091,.F.);
#17102=ORIENTED_EDGE('',*,*,#12094,.T.);
#17103=ORIENTED_EDGE('',*,*,#12088,.F.);
#17104=ORIENTED_EDGE('',*,*,#12095,.T.);
#17105=ORIENTED_EDGE('',*,*,#12096,.T.);
#17106=ORIENTED_EDGE('',*,*,#12097,.T.);
#17107=ORIENTED_EDGE('',*,*,#12098,.T.);
#17108=ORIENTED_EDGE('',*,*,#12095,.F.);
#17109=ORIENTED_EDGE('',*,*,#12099,.T.);
#17110=ORIENTED_EDGE('',*,*,#12090,.F.);
#17111=ORIENTED_EDGE('',*,*,#12099,.F.);
#17112=ORIENTED_EDGE('',*,*,#12100,.T.);
#17113=ORIENTED_EDGE('',*,*,#11975,.F.);
#17114=ORIENTED_EDGE('',*,*,#11982,.T.);
#17115=ORIENTED_EDGE('',*,*,#12098,.F.);
#17116=ORIENTED_EDGE('',*,*,#11897,.F.);
#17117=ORIENTED_EDGE('',*,*,#11906,.F.);
#17118=ORIENTED_EDGE('',*,*,#12101,.T.);
#17119=ORIENTED_EDGE('',*,*,#12102,.F.);
#17120=ORIENTED_EDGE('',*,*,#12103,.F.);
#17121=ORIENTED_EDGE('',*,*,#12104,.F.);
#17122=ORIENTED_EDGE('',*,*,#12105,.F.);
#17123=ORIENTED_EDGE('',*,*,#12106,.F.);
#17124=ORIENTED_EDGE('',*,*,#12107,.F.);
#17125=ORIENTED_EDGE('',*,*,#12108,.F.);
#17126=ORIENTED_EDGE('',*,*,#11971,.F.);
#17127=ORIENTED_EDGE('',*,*,#12100,.F.);
#17128=ORIENTED_EDGE('',*,*,#12109,.F.);
#17129=ORIENTED_EDGE('',*,*,#12110,.T.);
#17130=ORIENTED_EDGE('',*,*,#12111,.T.);
#17131=ORIENTED_EDGE('',*,*,#12112,.T.);
#17132=ORIENTED_EDGE('',*,*,#12113,.T.);
#17133=ORIENTED_EDGE('',*,*,#12111,.F.);
#17134=ORIENTED_EDGE('',*,*,#12114,.T.);
#17135=ORIENTED_EDGE('',*,*,#12115,.T.);
#17136=ORIENTED_EDGE('',*,*,#12115,.F.);
#17137=ORIENTED_EDGE('',*,*,#12116,.T.);
#17138=ORIENTED_EDGE('',*,*,#12117,.F.);
#17139=ORIENTED_EDGE('',*,*,#12118,.T.);
#17140=ORIENTED_EDGE('',*,*,#12119,.F.);
#17141=ORIENTED_EDGE('',*,*,#12120,.T.);
#17142=ORIENTED_EDGE('',*,*,#12121,.F.);
#17143=ORIENTED_EDGE('',*,*,#12122,.T.);
#17144=ORIENTED_EDGE('',*,*,#12112,.F.);
#17145=ORIENTED_EDGE('',*,*,#12113,.F.);
#17146=ORIENTED_EDGE('',*,*,#12122,.F.);
#17147=ORIENTED_EDGE('',*,*,#12123,.T.);
#17148=ORIENTED_EDGE('',*,*,#12124,.T.);
#17149=ORIENTED_EDGE('',*,*,#12125,.T.);
#17150=ORIENTED_EDGE('',*,*,#12126,.T.);
#17151=ORIENTED_EDGE('',*,*,#12124,.F.);
#17152=ORIENTED_EDGE('',*,*,#12127,.F.);
#17153=ORIENTED_EDGE('',*,*,#12128,.T.);
#17154=ORIENTED_EDGE('',*,*,#12125,.F.);
#17155=ORIENTED_EDGE('',*,*,#12126,.F.);
#17156=ORIENTED_EDGE('',*,*,#12128,.F.);
#17157=ORIENTED_EDGE('',*,*,#12093,.F.);
#17158=ORIENTED_EDGE('',*,*,#12129,.F.);
#17159=ORIENTED_EDGE('',*,*,#12116,.F.);
#17160=ORIENTED_EDGE('',*,*,#12114,.F.);
#17161=ORIENTED_EDGE('',*,*,#12110,.F.);
#17162=ORIENTED_EDGE('',*,*,#12120,.F.);
#17163=ORIENTED_EDGE('',*,*,#12130,.F.);
#17164=ORIENTED_EDGE('',*,*,#12123,.F.);
#17165=ORIENTED_EDGE('',*,*,#12109,.T.);
#17166=ORIENTED_EDGE('',*,*,#12131,.T.);
#17167=ORIENTED_EDGE('',*,*,#12127,.T.);
#17168=ORIENTED_EDGE('',*,*,#12131,.F.);
#17169=ORIENTED_EDGE('',*,*,#12107,.T.);
#17170=ORIENTED_EDGE('',*,*,#12132,.T.);
#17171=ORIENTED_EDGE('',*,*,#12121,.T.);
#17172=ORIENTED_EDGE('',*,*,#12132,.F.);
#17173=ORIENTED_EDGE('',*,*,#12106,.T.);
#17174=ORIENTED_EDGE('',*,*,#12133,.T.);
#17175=ORIENTED_EDGE('',*,*,#12133,.F.);
#17176=ORIENTED_EDGE('',*,*,#12105,.T.);
#17177=ORIENTED_EDGE('',*,*,#12134,.F.);
#17178=ORIENTED_EDGE('',*,*,#12135,.T.);
#17179=ORIENTED_EDGE('',*,*,#12136,.T.);
#17180=ORIENTED_EDGE('',*,*,#12108,.T.);
#17181=ORIENTED_EDGE('',*,*,#12102,.T.);
#17182=ORIENTED_EDGE('',*,*,#12137,.T.);
#17183=ORIENTED_EDGE('',*,*,#12138,.T.);
#17184=ORIENTED_EDGE('',*,*,#12139,.T.);
#17185=ORIENTED_EDGE('',*,*,#11905,.F.);
#17186=ORIENTED_EDGE('',*,*,#12140,.F.);
#17187=ORIENTED_EDGE('',*,*,#12137,.F.);
#17188=ORIENTED_EDGE('',*,*,#12101,.F.);
#17189=ORIENTED_EDGE('',*,*,#12141,.T.);
#17190=ORIENTED_EDGE('',*,*,#12014,.T.);
#17191=ORIENTED_EDGE('',*,*,#11857,.T.);
#17192=ORIENTED_EDGE('',*,*,#11898,.T.);
#17193=ORIENTED_EDGE('',*,*,#12097,.F.);
#17194=ORIENTED_EDGE('',*,*,#12089,.F.);
#17195=ORIENTED_EDGE('',*,*,#12142,.F.);
#17196=ORIENTED_EDGE('',*,*,#12143,.F.);
#17197=ORIENTED_EDGE('',*,*,#12144,.F.);
#17198=ORIENTED_EDGE('',*,*,#12145,.F.);
#17199=ORIENTED_EDGE('',*,*,#12015,.F.);
#17200=ORIENTED_EDGE('',*,*,#12141,.F.);
#17201=ORIENTED_EDGE('',*,*,#12096,.F.);
#17202=ORIENTED_EDGE('',*,*,#12146,.T.);
#17203=ORIENTED_EDGE('',*,*,#12147,.T.);
#17204=ORIENTED_EDGE('',*,*,#11850,.F.);
#17205=ORIENTED_EDGE('',*,*,#12016,.T.);
#17206=ORIENTED_EDGE('',*,*,#12145,.T.);
#17207=ORIENTED_EDGE('',*,*,#12139,.F.);
#17208=ORIENTED_EDGE('',*,*,#12148,.F.);
#17209=ORIENTED_EDGE('',*,*,#11853,.F.);
#17210=ORIENTED_EDGE('',*,*,#11851,.F.);
#17211=ORIENTED_EDGE('',*,*,#12147,.F.);
#17212=ORIENTED_EDGE('',*,*,#12103,.T.);
#17213=ORIENTED_EDGE('',*,*,#12149,.T.);
#17214=ORIENTED_EDGE('',*,*,#12104,.T.);
#17215=ORIENTED_EDGE('',*,*,#12146,.F.);
#17216=ORIENTED_EDGE('',*,*,#12144,.T.);
#17217=ORIENTED_EDGE('',*,*,#12150,.T.);
#17218=ORIENTED_EDGE('',*,*,#12143,.T.);
#17219=ORIENTED_EDGE('',*,*,#12151,.T.);
#17220=ORIENTED_EDGE('',*,*,#12152,.T.);
#17221=ORIENTED_EDGE('',*,*,#12150,.F.);
#17222=ORIENTED_EDGE('',*,*,#12134,.T.);
#17223=ORIENTED_EDGE('',*,*,#12149,.F.);
#17224=ORIENTED_EDGE('',*,*,#12094,.F.);
#17225=ORIENTED_EDGE('',*,*,#12130,.T.);
#17226=ORIENTED_EDGE('',*,*,#12153,.T.);
#17227=ORIENTED_EDGE('',*,*,#12142,.T.);
#17228=ORIENTED_EDGE('',*,*,#12153,.F.);
#17229=ORIENTED_EDGE('',*,*,#12119,.T.);
#17230=ORIENTED_EDGE('',*,*,#12151,.F.);
#17231=ORIENTED_EDGE('',*,*,#12046,.F.);
#17232=ORIENTED_EDGE('',*,*,#12062,.F.);
#17233=ORIENTED_EDGE('',*,*,#12154,.F.);
#17234=ORIENTED_EDGE('',*,*,#12155,.T.);
#17235=ORIENTED_EDGE('',*,*,#12031,.T.);
#17236=ORIENTED_EDGE('',*,*,#12156,.F.);
#17237=ORIENTED_EDGE('',*,*,#12157,.F.);
#17238=ORIENTED_EDGE('',*,*,#12029,.T.);
#17239=ORIENTED_EDGE('',*,*,#11998,.T.);
#17240=ORIENTED_EDGE('',*,*,#12158,.F.);
#17241=ORIENTED_EDGE('',*,*,#12159,.F.);
#17242=ORIENTED_EDGE('',*,*,#12160,.T.);
#17243=ORIENTED_EDGE('',*,*,#12161,.F.);
#17244=ORIENTED_EDGE('',*,*,#12162,.T.);
#17245=ORIENTED_EDGE('',*,*,#12163,.F.);
#17246=ORIENTED_EDGE('',*,*,#12164,.F.);
#17247=ORIENTED_EDGE('',*,*,#12165,.F.);
#17248=ORIENTED_EDGE('',*,*,#12166,.F.);
#17249=ORIENTED_EDGE('',*,*,#12167,.F.);
#17250=ORIENTED_EDGE('',*,*,#12168,.F.);
#17251=ORIENTED_EDGE('',*,*,#12169,.T.);
#17252=ORIENTED_EDGE('',*,*,#12006,.T.);
#17253=ORIENTED_EDGE('',*,*,#11843,.T.);
#17254=ORIENTED_EDGE('',*,*,#11847,.T.);
#17255=ORIENTED_EDGE('',*,*,#11845,.F.);
#17256=ORIENTED_EDGE('',*,*,#12019,.T.);
#17257=ORIENTED_EDGE('',*,*,#12170,.T.);
#17258=ORIENTED_EDGE('',*,*,#12171,.F.);
#17259=ORIENTED_EDGE('',*,*,#12172,.F.);
#17260=ORIENTED_EDGE('',*,*,#12135,.F.);
#17261=ORIENTED_EDGE('',*,*,#12152,.F.);
#17262=ORIENTED_EDGE('',*,*,#12118,.F.);
#17263=ORIENTED_EDGE('',*,*,#12173,.F.);
#17264=ORIENTED_EDGE('',*,*,#12174,.F.);
#17265=ORIENTED_EDGE('',*,*,#12175,.F.);
#17266=ORIENTED_EDGE('',*,*,#12176,.F.);
#17267=ORIENTED_EDGE('',*,*,#12177,.F.);
#17268=ORIENTED_EDGE('',*,*,#12178,.F.);
#17269=ORIENTED_EDGE('',*,*,#12179,.F.);
#17270=ORIENTED_EDGE('',*,*,#12180,.F.);
#17271=ORIENTED_EDGE('',*,*,#12181,.F.);
#17272=ORIENTED_EDGE('',*,*,#12182,.F.);
#17273=ORIENTED_EDGE('',*,*,#12183,.F.);
#17274=ORIENTED_EDGE('',*,*,#12184,.F.);
#17275=ORIENTED_EDGE('',*,*,#12185,.F.);
#17276=ORIENTED_EDGE('',*,*,#12186,.F.);
#17277=ORIENTED_EDGE('',*,*,#11979,.T.);
#17278=ORIENTED_EDGE('',*,*,#12187,.T.);
#17279=ORIENTED_EDGE('',*,*,#12188,.T.);
#17280=ORIENTED_EDGE('',*,*,#12092,.F.);
#17281=ORIENTED_EDGE('',*,*,#12051,.F.);
#17282=ORIENTED_EDGE('',*,*,#12189,.T.);
#17283=ORIENTED_EDGE('',*,*,#12187,.F.);
#17284=ORIENTED_EDGE('',*,*,#11978,.T.);
#17285=ORIENTED_EDGE('',*,*,#12190,.T.);
#17286=ORIENTED_EDGE('',*,*,#12191,.T.);
#17287=ORIENTED_EDGE('',*,*,#12063,.T.);
#17288=ORIENTED_EDGE('',*,*,#12191,.F.);
#17289=ORIENTED_EDGE('',*,*,#12192,.T.);
#17290=ORIENTED_EDGE('',*,*,#12193,.T.);
#17291=ORIENTED_EDGE('',*,*,#12047,.F.);
#17292=ORIENTED_EDGE('',*,*,#12174,.T.);
#17293=ORIENTED_EDGE('',*,*,#12194,.T.);
#17294=ORIENTED_EDGE('',*,*,#12195,.T.);
#17295=ORIENTED_EDGE('',*,*,#12193,.F.);
#17296=ORIENTED_EDGE('',*,*,#12196,.T.);
#17297=ORIENTED_EDGE('',*,*,#12059,.F.);
#17298=ORIENTED_EDGE('',*,*,#12197,.T.);
#17299=ORIENTED_EDGE('',*,*,#12198,.T.);
#17300=ORIENTED_EDGE('',*,*,#12199,.F.);
#17301=ORIENTED_EDGE('',*,*,#11919,.F.);
#17302=ORIENTED_EDGE('',*,*,#12200,.T.);
#17303=ORIENTED_EDGE('',*,*,#12201,.T.);
#17304=ORIENTED_EDGE('',*,*,#12068,.T.);
#17305=ORIENTED_EDGE('',*,*,#11928,.T.);
#17306=ORIENTED_EDGE('',*,*,#12201,.F.);
#17307=ORIENTED_EDGE('',*,*,#12202,.T.);
#17308=ORIENTED_EDGE('',*,*,#12203,.T.);
#17309=ORIENTED_EDGE('',*,*,#12069,.F.);
#17310=ORIENTED_EDGE('',*,*,#11918,.F.);
#17311=ORIENTED_EDGE('',*,*,#12204,.T.);
#17312=ORIENTED_EDGE('',*,*,#12205,.T.);
#17313=ORIENTED_EDGE('',*,*,#12200,.F.);
#17314=ORIENTED_EDGE('',*,*,#12205,.F.);
#17315=ORIENTED_EDGE('',*,*,#12206,.T.);
#17316=ORIENTED_EDGE('',*,*,#12207,.T.);
#17317=ORIENTED_EDGE('',*,*,#12202,.F.);
#17318=ORIENTED_EDGE('',*,*,#12208,.T.);
#17319=ORIENTED_EDGE('',*,*,#12081,.F.);
#17320=ORIENTED_EDGE('',*,*,#12209,.T.);
#17321=ORIENTED_EDGE('',*,*,#12210,.T.);
#17322=ORIENTED_EDGE('',*,*,#11939,.F.);
#17323=ORIENTED_EDGE('',*,*,#12060,.T.);
#17324=ORIENTED_EDGE('',*,*,#11914,.F.);
#17325=ORIENTED_EDGE('',*,*,#12208,.F.);
#17326=ORIENTED_EDGE('',*,*,#11927,.T.);
#17327=ORIENTED_EDGE('',*,*,#12211,.T.);
#17328=ORIENTED_EDGE('',*,*,#12075,.T.);
#17329=ORIENTED_EDGE('',*,*,#11984,.F.);
#17330=ORIENTED_EDGE('',*,*,#12212,.T.);
#17331=ORIENTED_EDGE('',*,*,#11947,.F.);
#17332=ORIENTED_EDGE('',*,*,#11944,.F.);
#17333=ORIENTED_EDGE('',*,*,#12213,.T.);
#17334=ORIENTED_EDGE('',*,*,#12209,.F.);
#17335=ORIENTED_EDGE('',*,*,#12080,.F.);
#17336=ORIENTED_EDGE('',*,*,#12214,.T.);
#17337=ORIENTED_EDGE('',*,*,#11910,.T.);
#17338=ORIENTED_EDGE('',*,*,#11949,.T.);
#17339=ORIENTED_EDGE('',*,*,#12210,.F.);
#17340=ORIENTED_EDGE('',*,*,#12213,.F.);
#17341=ORIENTED_EDGE('',*,*,#11948,.F.);
#17342=ORIENTED_EDGE('',*,*,#11940,.T.);
#17343=ORIENTED_EDGE('',*,*,#12212,.F.);
#17344=ORIENTED_EDGE('',*,*,#11988,.T.);
#17345=ORIENTED_EDGE('',*,*,#12215,.T.);
#17346=ORIENTED_EDGE('',*,*,#11942,.T.);
#17347=ORIENTED_EDGE('',*,*,#12216,.T.);
#17348=ORIENTED_EDGE('',*,*,#11987,.T.);
#17349=ORIENTED_EDGE('',*,*,#12217,.T.);
#17350=ORIENTED_EDGE('',*,*,#12154,.T.);
#17351=ORIENTED_EDGE('',*,*,#12216,.F.);
#17352=ORIENTED_EDGE('',*,*,#12061,.T.);
#17353=ORIENTED_EDGE('',*,*,#12215,.F.);
#17354=ORIENTED_EDGE('',*,*,#12011,.T.);
#17355=ORIENTED_EDGE('',*,*,#12218,.T.);
#17356=ORIENTED_EDGE('',*,*,#12219,.T.);
#17357=ORIENTED_EDGE('',*,*,#11899,.T.);
#17358=ORIENTED_EDGE('',*,*,#11864,.F.);
#17359=ORIENTED_EDGE('',*,*,#12220,.F.);
#17360=ORIENTED_EDGE('',*,*,#12218,.F.);
#17361=ORIENTED_EDGE('',*,*,#12010,.F.);
#17362=ORIENTED_EDGE('',*,*,#12221,.F.);
#17363=ORIENTED_EDGE('',*,*,#12222,.F.);
#17364=ORIENTED_EDGE('',*,*,#12223,.F.);
#17365=ORIENTED_EDGE('',*,*,#12224,.F.);
#17366=ORIENTED_EDGE('',*,*,#12225,.F.);
#17367=ORIENTED_EDGE('',*,*,#12226,.T.);
#17368=ORIENTED_EDGE('',*,*,#12221,.T.);
#17369=ORIENTED_EDGE('',*,*,#12009,.T.);
#17370=ORIENTED_EDGE('',*,*,#11868,.T.);
#17371=ORIENTED_EDGE('',*,*,#12227,.T.);
#17372=ORIENTED_EDGE('',*,*,#12228,.T.);
#17373=ORIENTED_EDGE('',*,*,#12229,.T.);
#17374=ORIENTED_EDGE('',*,*,#12230,.T.);
#17375=ORIENTED_EDGE('',*,*,#12229,.F.);
#17376=ORIENTED_EDGE('',*,*,#12231,.F.);
#17377=ORIENTED_EDGE('',*,*,#12232,.F.);
#17378=ORIENTED_EDGE('',*,*,#12233,.T.);
#17379=ORIENTED_EDGE('',*,*,#12230,.F.);
#17380=ORIENTED_EDGE('',*,*,#12233,.F.);
#17381=ORIENTED_EDGE('',*,*,#12234,.F.);
#17382=ORIENTED_EDGE('',*,*,#12235,.F.);
#17383=ORIENTED_EDGE('',*,*,#12236,.F.);
#17384=ORIENTED_EDGE('',*,*,#12237,.F.);
#17385=ORIENTED_EDGE('',*,*,#12238,.F.);
#17386=ORIENTED_EDGE('',*,*,#12239,.F.);
#17387=ORIENTED_EDGE('',*,*,#12240,.F.);
#17388=ORIENTED_EDGE('',*,*,#12228,.F.);
#17389=ORIENTED_EDGE('',*,*,#12234,.T.);
#17390=ORIENTED_EDGE('',*,*,#12241,.T.);
#17391=ORIENTED_EDGE('',*,*,#12242,.T.);
#17392=ORIENTED_EDGE('',*,*,#12241,.F.);
#17393=ORIENTED_EDGE('',*,*,#12240,.T.);
#17394=ORIENTED_EDGE('',*,*,#12243,.T.);
#17395=ORIENTED_EDGE('',*,*,#12243,.F.);
#17396=ORIENTED_EDGE('',*,*,#12239,.T.);
#17397=ORIENTED_EDGE('',*,*,#12244,.T.);
#17398=ORIENTED_EDGE('',*,*,#12164,.T.);
#17399=ORIENTED_EDGE('',*,*,#12245,.F.);
#17400=ORIENTED_EDGE('',*,*,#12235,.T.);
#17401=ORIENTED_EDGE('',*,*,#12246,.F.);
#17402=ORIENTED_EDGE('',*,*,#12247,.F.);
#17403=ORIENTED_EDGE('',*,*,#12248,.T.);
#17404=ORIENTED_EDGE('',*,*,#12242,.F.);
#17405=ORIENTED_EDGE('',*,*,#12248,.F.);
#17406=ORIENTED_EDGE('',*,*,#12042,.F.);
#17407=ORIENTED_EDGE('',*,*,#12196,.F.);
#17408=ORIENTED_EDGE('',*,*,#12192,.F.);
#17409=ORIENTED_EDGE('',*,*,#12190,.F.);
#17410=ORIENTED_EDGE('',*,*,#12195,.F.);
#17411=ORIENTED_EDGE('',*,*,#12249,.F.);
#17412=ORIENTED_EDGE('',*,*,#12189,.F.);
#17413=ORIENTED_EDGE('',*,*,#12250,.F.);
#17414=ORIENTED_EDGE('',*,*,#12117,.T.);
#17415=ORIENTED_EDGE('',*,*,#12251,.T.);
#17416=ORIENTED_EDGE('',*,*,#12194,.F.);
#17417=ORIENTED_EDGE('',*,*,#12173,.T.);
#17418=ORIENTED_EDGE('',*,*,#12188,.F.);
#17419=ORIENTED_EDGE('',*,*,#12249,.T.);
#17420=ORIENTED_EDGE('',*,*,#12251,.F.);
#17421=ORIENTED_EDGE('',*,*,#12129,.T.);
#17422=ORIENTED_EDGE('',*,*,#12252,.T.);
#17423=ORIENTED_EDGE('',*,*,#11972,.T.);
#17424=ORIENTED_EDGE('',*,*,#12136,.F.);
#17425=ORIENTED_EDGE('',*,*,#12172,.T.);
#17426=ORIENTED_EDGE('',*,*,#12253,.T.);
#17427=ORIENTED_EDGE('',*,*,#12254,.T.);
#17428=ORIENTED_EDGE('',*,*,#12252,.F.);
#17429=ORIENTED_EDGE('',*,*,#12171,.T.);
#17430=ORIENTED_EDGE('',*,*,#12253,.F.);
#17431=ORIENTED_EDGE('',*,*,#12170,.F.);
#17432=ORIENTED_EDGE('',*,*,#12018,.T.);
#17433=ORIENTED_EDGE('',*,*,#12255,.T.);
#17434=ORIENTED_EDGE('',*,*,#12256,.T.);
#17435=ORIENTED_EDGE('',*,*,#12168,.T.);
#17436=ORIENTED_EDGE('',*,*,#12257,.T.);
#17437=ORIENTED_EDGE('',*,*,#12258,.T.);
#17438=ORIENTED_EDGE('',*,*,#12037,.F.);
#17439=ORIENTED_EDGE('',*,*,#11879,.T.);
#17440=ORIENTED_EDGE('',*,*,#11875,.F.);
#17441=ORIENTED_EDGE('',*,*,#12259,.T.);
#17442=ORIENTED_EDGE('',*,*,#11873,.T.);
#17443=ORIENTED_EDGE('',*,*,#11870,.F.);
#17444=ORIENTED_EDGE('',*,*,#12008,.T.);
#17445=ORIENTED_EDGE('',*,*,#12260,.T.);
#17446=ORIENTED_EDGE('',*,*,#12258,.F.);
#17447=ORIENTED_EDGE('',*,*,#12261,.T.);
#17448=ORIENTED_EDGE('',*,*,#12262,.T.);
#17449=ORIENTED_EDGE('',*,*,#12263,.T.);
#17450=ORIENTED_EDGE('',*,*,#12257,.F.);
#17451=ORIENTED_EDGE('',*,*,#12167,.T.);
#17452=ORIENTED_EDGE('',*,*,#12263,.F.);
#17453=ORIENTED_EDGE('',*,*,#12264,.T.);
#17454=ORIENTED_EDGE('',*,*,#12265,.F.);
#17455=ORIENTED_EDGE('',*,*,#12266,.F.);
#17456=ORIENTED_EDGE('',*,*,#12038,.T.);
#17457=ORIENTED_EDGE('',*,*,#12261,.F.);
#17458=ORIENTED_EDGE('',*,*,#12267,.T.);
#17459=ORIENTED_EDGE('',*,*,#12268,.T.);
#17460=ORIENTED_EDGE('',*,*,#12245,.T.);
#17461=ORIENTED_EDGE('',*,*,#12163,.T.);
#17462=ORIENTED_EDGE('',*,*,#12268,.F.);
#17463=ORIENTED_EDGE('',*,*,#12269,.T.);
#17464=ORIENTED_EDGE('',*,*,#12270,.F.);
#17465=ORIENTED_EDGE('',*,*,#12236,.T.);
#17466=ORIENTED_EDGE('',*,*,#12271,.T.);
#17467=ORIENTED_EDGE('',*,*,#12272,.T.);
#17468=ORIENTED_EDGE('',*,*,#12273,.T.);
#17469=ORIENTED_EDGE('',*,*,#12178,.T.);
#17470=ORIENTED_EDGE('',*,*,#12272,.F.);
#17471=ORIENTED_EDGE('',*,*,#12274,.T.);
#17472=ORIENTED_EDGE('',*,*,#12275,.T.);
#17473=ORIENTED_EDGE('',*,*,#12276,.T.);
#17474=ORIENTED_EDGE('',*,*,#12277,.T.);
#17475=ORIENTED_EDGE('',*,*,#12278,.F.);
#17476=ORIENTED_EDGE('',*,*,#12279,.T.);
#17477=ORIENTED_EDGE('',*,*,#12280,.T.);
#17478=ORIENTED_EDGE('',*,*,#12281,.T.);
#17479=ORIENTED_EDGE('',*,*,#12176,.T.);
#17480=ORIENTED_EDGE('',*,*,#12280,.F.);
#17481=ORIENTED_EDGE('',*,*,#12282,.T.);
#17482=ORIENTED_EDGE('',*,*,#12283,.T.);
#17483=ORIENTED_EDGE('',*,*,#12284,.T.);
#17484=ORIENTED_EDGE('',*,*,#12285,.T.);
#17485=ORIENTED_EDGE('',*,*,#12286,.F.);
#17486=ORIENTED_EDGE('',*,*,#12287,.T.);
#17487=ORIENTED_EDGE('',*,*,#12288,.T.);
#17488=ORIENTED_EDGE('',*,*,#12289,.T.);
#17489=ORIENTED_EDGE('',*,*,#12184,.T.);
#17490=ORIENTED_EDGE('',*,*,#12288,.F.);
#17491=ORIENTED_EDGE('',*,*,#12290,.T.);
#17492=ORIENTED_EDGE('',*,*,#12291,.T.);
#17493=ORIENTED_EDGE('',*,*,#12292,.T.);
#17494=ORIENTED_EDGE('',*,*,#12293,.T.);
#17495=ORIENTED_EDGE('',*,*,#12294,.F.);
#17496=ORIENTED_EDGE('',*,*,#12295,.T.);
#17497=ORIENTED_EDGE('',*,*,#12296,.T.);
#17498=ORIENTED_EDGE('',*,*,#12180,.T.);
#17499=ORIENTED_EDGE('',*,*,#12297,.T.);
#17500=ORIENTED_EDGE('',*,*,#12298,.T.);
#17501=ORIENTED_EDGE('',*,*,#12299,.T.);
#17502=ORIENTED_EDGE('',*,*,#12182,.T.);
#17503=ORIENTED_EDGE('',*,*,#12298,.F.);
#17504=ORIENTED_EDGE('',*,*,#12300,.T.);
#17505=ORIENTED_EDGE('',*,*,#12301,.T.);
#17506=ORIENTED_EDGE('',*,*,#12302,.T.);
#17507=ORIENTED_EDGE('',*,*,#12303,.T.);
#17508=ORIENTED_EDGE('',*,*,#12304,.F.);
#17509=ORIENTED_EDGE('',*,*,#12295,.F.);
#17510=ORIENTED_EDGE('',*,*,#12181,.T.);
#17511=ORIENTED_EDGE('',*,*,#12296,.F.);
#17512=ORIENTED_EDGE('',*,*,#12305,.T.);
#17513=ORIENTED_EDGE('',*,*,#12306,.T.);
#17514=ORIENTED_EDGE('',*,*,#12307,.T.);
#17515=ORIENTED_EDGE('',*,*,#12305,.F.);
#17516=ORIENTED_EDGE('',*,*,#12308,.T.);
#17517=ORIENTED_EDGE('',*,*,#12297,.F.);
#17518=ORIENTED_EDGE('',*,*,#12179,.T.);
#17519=ORIENTED_EDGE('',*,*,#12289,.F.);
#17520=ORIENTED_EDGE('',*,*,#12308,.F.);
#17521=ORIENTED_EDGE('',*,*,#12294,.T.);
#17522=ORIENTED_EDGE('',*,*,#12309,.T.);
#17523=ORIENTED_EDGE('',*,*,#12300,.F.);
#17524=ORIENTED_EDGE('',*,*,#12310,.T.);
#17525=ORIENTED_EDGE('',*,*,#12287,.F.);
#17526=ORIENTED_EDGE('',*,*,#12183,.T.);
#17527=ORIENTED_EDGE('',*,*,#12299,.F.);
#17528=ORIENTED_EDGE('',*,*,#12310,.F.);
#17529=ORIENTED_EDGE('',*,*,#12304,.T.);
#17530=ORIENTED_EDGE('',*,*,#12311,.T.);
#17531=ORIENTED_EDGE('',*,*,#12290,.F.);
#17532=ORIENTED_EDGE('',*,*,#12312,.T.);
#17533=ORIENTED_EDGE('',*,*,#12279,.F.);
#17534=ORIENTED_EDGE('',*,*,#12175,.T.);
#17535=ORIENTED_EDGE('',*,*,#12273,.F.);
#17536=ORIENTED_EDGE('',*,*,#12312,.F.);
#17537=ORIENTED_EDGE('',*,*,#12278,.T.);
#17538=ORIENTED_EDGE('',*,*,#12313,.T.);
#17539=ORIENTED_EDGE('',*,*,#12282,.F.);
#17540=ORIENTED_EDGE('',*,*,#12314,.T.);
#17541=ORIENTED_EDGE('',*,*,#12271,.F.);
#17542=ORIENTED_EDGE('',*,*,#12177,.T.);
#17543=ORIENTED_EDGE('',*,*,#12281,.F.);
#17544=ORIENTED_EDGE('',*,*,#12314,.F.);
#17545=ORIENTED_EDGE('',*,*,#12286,.T.);
#17546=ORIENTED_EDGE('',*,*,#12315,.T.);
#17547=ORIENTED_EDGE('',*,*,#12274,.F.);
#17548=ORIENTED_EDGE('',*,*,#12186,.T.);
#17549=ORIENTED_EDGE('',*,*,#12316,.T.);
#17550=ORIENTED_EDGE('',*,*,#12317,.T.);
#17551=ORIENTED_EDGE('',*,*,#12318,.T.);
#17552=ORIENTED_EDGE('',*,*,#12316,.F.);
#17553=ORIENTED_EDGE('',*,*,#12318,.F.);
#17554=ORIENTED_EDGE('',*,*,#12319,.T.);
#17555=ORIENTED_EDGE('',*,*,#12320,.T.);
#17556=ORIENTED_EDGE('',*,*,#12319,.F.);
#17557=ORIENTED_EDGE('',*,*,#12317,.F.);
#17558=ORIENTED_EDGE('',*,*,#12185,.T.);
#17559=ORIENTED_EDGE('',*,*,#12321,.T.);
#17560=ORIENTED_EDGE('',*,*,#12322,.T.);
#17561=ORIENTED_EDGE('',*,*,#12323,.T.);
#17562=ORIENTED_EDGE('',*,*,#12321,.F.);
#17563=ORIENTED_EDGE('',*,*,#12323,.F.);
#17564=ORIENTED_EDGE('',*,*,#12324,.T.);
#17565=ORIENTED_EDGE('',*,*,#12325,.T.);
#17566=ORIENTED_EDGE('',*,*,#12324,.F.);
#17567=ORIENTED_EDGE('',*,*,#12322,.F.);
#17568=ORIENTED_EDGE('',*,*,#12307,.F.);
#17569=ORIENTED_EDGE('',*,*,#12326,.T.);
#17570=ORIENTED_EDGE('',*,*,#12327,.T.);
#17571=ORIENTED_EDGE('',*,*,#12326,.F.);
#17572=ORIENTED_EDGE('',*,*,#12306,.F.);
#17573=ORIENTED_EDGE('',*,*,#12328,.T.);
#17574=ORIENTED_EDGE('',*,*,#12329,.T.);
#17575=ORIENTED_EDGE('',*,*,#12156,.T.);
#17576=ORIENTED_EDGE('',*,*,#12030,.T.);
#17577=ORIENTED_EDGE('',*,*,#12157,.T.);
#17578=ORIENTED_EDGE('',*,*,#12329,.F.);
#17579=ORIENTED_EDGE('',*,*,#12330,.T.);
#17580=ORIENTED_EDGE('',*,*,#12331,.T.);
#17581=ORIENTED_EDGE('',*,*,#12246,.T.);
#17582=ORIENTED_EDGE('',*,*,#12247,.T.);
#17583=ORIENTED_EDGE('',*,*,#12331,.F.);
#17584=ORIENTED_EDGE('',*,*,#12332,.T.);
#17585=ORIENTED_EDGE('',*,*,#12333,.T.);
#17586=ORIENTED_EDGE('',*,*,#12333,.F.);
#17587=ORIENTED_EDGE('',*,*,#12334,.T.);
#17588=ORIENTED_EDGE('',*,*,#12262,.F.);
#17589=ORIENTED_EDGE('',*,*,#12166,.T.);
#17590=ORIENTED_EDGE('',*,*,#12335,.F.);
#17591=ORIENTED_EDGE('',*,*,#12336,.T.);
#17592=ORIENTED_EDGE('',*,*,#12337,.T.);
#17593=ORIENTED_EDGE('',*,*,#12338,.T.);
#17594=ORIENTED_EDGE('',*,*,#12231,.T.);
#17595=ORIENTED_EDGE('',*,*,#12232,.T.);
#17596=ORIENTED_EDGE('',*,*,#12338,.F.);
#17597=ORIENTED_EDGE('',*,*,#12330,.F.);
#17598=ORIENTED_EDGE('',*,*,#12336,.F.);
#17599=ORIENTED_EDGE('',*,*,#12339,.F.);
#17600=ORIENTED_EDGE('',*,*,#12340,.T.);
#17601=ORIENTED_EDGE('',*,*,#11877,.F.);
#17602=ORIENTED_EDGE('',*,*,#11881,.T.);
#17603=ORIENTED_EDGE('',*,*,#11884,.F.);
#17604=ORIENTED_EDGE('',*,*,#11900,.T.);
#17605=ORIENTED_EDGE('',*,*,#12341,.F.);
#17606=ORIENTED_EDGE('',*,*,#12342,.F.);
#17607=ORIENTED_EDGE('',*,*,#12264,.F.);
#17608=ORIENTED_EDGE('',*,*,#12334,.F.);
#17609=ORIENTED_EDGE('',*,*,#12332,.F.);
#17610=ORIENTED_EDGE('',*,*,#12337,.F.);
#17611=ORIENTED_EDGE('',*,*,#12343,.T.);
#17612=ORIENTED_EDGE('',*,*,#12223,.T.);
#17613=ORIENTED_EDGE('',*,*,#12344,.T.);
#17614=ORIENTED_EDGE('',*,*,#12165,.T.);
#17615=ORIENTED_EDGE('',*,*,#12345,.T.);
#17616=ORIENTED_EDGE('',*,*,#12222,.T.);
#17617=ORIENTED_EDGE('',*,*,#12226,.F.);
#17618=ORIENTED_EDGE('',*,*,#12339,.T.);
#17619=ORIENTED_EDGE('',*,*,#12345,.F.);
#17620=ORIENTED_EDGE('',*,*,#12335,.T.);
#17621=ORIENTED_EDGE('',*,*,#12344,.F.);
#17622=ORIENTED_EDGE('',*,*,#12244,.F.);
#17623=ORIENTED_EDGE('',*,*,#12346,.T.);
#17624=ORIENTED_EDGE('',*,*,#12343,.F.);
#17625=ORIENTED_EDGE('',*,*,#12346,.F.);
#17626=ORIENTED_EDGE('',*,*,#12238,.T.);
#17627=ORIENTED_EDGE('',*,*,#12347,.T.);
#17628=ORIENTED_EDGE('',*,*,#12224,.T.);
#17629=ORIENTED_EDGE('',*,*,#12348,.T.);
#17630=ORIENTED_EDGE('',*,*,#12349,.T.);
#17631=ORIENTED_EDGE('',*,*,#12350,.T.);
#17632=ORIENTED_EDGE('',*,*,#12342,.T.);
#17633=ORIENTED_EDGE('',*,*,#12351,.T.);
#17634=ORIENTED_EDGE('',*,*,#12341,.T.);
#17635=ORIENTED_EDGE('',*,*,#12219,.F.);
#17636=ORIENTED_EDGE('',*,*,#12220,.T.);
#17637=ORIENTED_EDGE('',*,*,#12351,.F.);
#17638=ORIENTED_EDGE('',*,*,#12352,.T.);
#17639=ORIENTED_EDGE('',*,*,#12348,.F.);
#17640=ORIENTED_EDGE('',*,*,#12353,.F.);
#17641=ORIENTED_EDGE('',*,*,#12349,.F.);
#17642=ORIENTED_EDGE('',*,*,#12354,.F.);
#17643=ORIENTED_EDGE('',*,*,#12355,.F.);
#17644=ORIENTED_EDGE('',*,*,#12356,.F.);
#17645=ORIENTED_EDGE('',*,*,#12357,.T.);
#17646=ORIENTED_EDGE('',*,*,#12358,.F.);
#17647=ORIENTED_EDGE('',*,*,#12359,.T.);
#17648=ORIENTED_EDGE('',*,*,#12360,.F.);
#17649=ORIENTED_EDGE('',*,*,#12361,.F.);
#17650=ORIENTED_EDGE('',*,*,#12362,.F.);
#17651=ORIENTED_EDGE('',*,*,#12352,.F.);
#17652=ORIENTED_EDGE('',*,*,#12225,.T.);
#17653=ORIENTED_EDGE('',*,*,#12363,.F.);
#17654=ORIENTED_EDGE('',*,*,#12354,.T.);
#17655=ORIENTED_EDGE('',*,*,#12364,.T.);
#17656=ORIENTED_EDGE('',*,*,#12365,.T.);
#17657=ORIENTED_EDGE('',*,*,#11994,.F.);
#17658=ORIENTED_EDGE('',*,*,#11888,.T.);
#17659=ORIENTED_EDGE('',*,*,#12366,.T.);
#17660=ORIENTED_EDGE('',*,*,#12367,.T.);
#17661=ORIENTED_EDGE('',*,*,#12368,.T.);
#17662=ORIENTED_EDGE('',*,*,#12369,.T.);
#17663=ORIENTED_EDGE('',*,*,#12362,.T.);
#17664=ORIENTED_EDGE('',*,*,#12370,.T.);
#17665=ORIENTED_EDGE('',*,*,#12371,.T.);
#17666=ORIENTED_EDGE('',*,*,#11886,.T.);
#17667=ORIENTED_EDGE('',*,*,#12036,.T.);
#17668=ORIENTED_EDGE('',*,*,#12266,.T.);
#17669=ORIENTED_EDGE('',*,*,#12370,.F.);
#17670=ORIENTED_EDGE('',*,*,#12372,.T.);
#17671=ORIENTED_EDGE('',*,*,#12369,.F.);
#17672=ORIENTED_EDGE('',*,*,#12367,.F.);
#17673=ORIENTED_EDGE('',*,*,#12373,.T.);
#17674=ORIENTED_EDGE('',*,*,#12364,.F.);
#17675=ORIENTED_EDGE('',*,*,#12365,.F.);
#17676=ORIENTED_EDGE('',*,*,#12374,.F.);
#17677=ORIENTED_EDGE('',*,*,#12375,.F.);
#17678=ORIENTED_EDGE('',*,*,#12376,.F.);
#17679=ORIENTED_EDGE('',*,*,#11996,.F.);
#17680=ORIENTED_EDGE('',*,*,#11992,.F.);
#17681=ORIENTED_EDGE('',*,*,#12373,.F.);
#17682=ORIENTED_EDGE('',*,*,#12361,.T.);
#17683=ORIENTED_EDGE('',*,*,#12377,.T.);
#17684=ORIENTED_EDGE('',*,*,#12374,.T.);
#17685=ORIENTED_EDGE('',*,*,#12372,.F.);
#17686=ORIENTED_EDGE('',*,*,#12265,.T.);
#17687=ORIENTED_EDGE('',*,*,#12350,.F.);
#17688=ORIENTED_EDGE('',*,*,#12353,.T.);
#17689=ORIENTED_EDGE('',*,*,#12378,.T.);
#17690=ORIENTED_EDGE('',*,*,#12237,.T.);
#17691=ORIENTED_EDGE('',*,*,#12379,.T.);
#17692=ORIENTED_EDGE('',*,*,#12355,.T.);
#17693=ORIENTED_EDGE('',*,*,#12378,.F.);
#17694=ORIENTED_EDGE('',*,*,#12363,.T.);
#17695=ORIENTED_EDGE('',*,*,#12347,.F.);
#17696=ORIENTED_EDGE('',*,*,#12380,.T.);
#17697=ORIENTED_EDGE('',*,*,#12381,.T.);
#17698=ORIENTED_EDGE('',*,*,#12382,.T.);
#17699=ORIENTED_EDGE('',*,*,#12383,.T.);
#17700=ORIENTED_EDGE('',*,*,#12381,.F.);
#17701=ORIENTED_EDGE('',*,*,#12383,.F.);
#17702=ORIENTED_EDGE('',*,*,#12384,.T.);
#17703=ORIENTED_EDGE('',*,*,#12385,.F.);
#17704=ORIENTED_EDGE('',*,*,#12386,.F.);
#17705=ORIENTED_EDGE('',*,*,#12387,.T.);
#17706=ORIENTED_EDGE('',*,*,#12388,.T.);
#17707=ORIENTED_EDGE('',*,*,#12389,.T.);
#17708=ORIENTED_EDGE('',*,*,#12390,.F.);
#17709=ORIENTED_EDGE('',*,*,#12391,.F.);
#17710=ORIENTED_EDGE('',*,*,#12392,.T.);
#17711=ORIENTED_EDGE('',*,*,#12393,.T.);
#17712=ORIENTED_EDGE('',*,*,#12394,.T.);
#17713=ORIENTED_EDGE('',*,*,#12395,.F.);
#17714=ORIENTED_EDGE('',*,*,#12396,.F.);
#17715=ORIENTED_EDGE('',*,*,#12397,.T.);
#17716=ORIENTED_EDGE('',*,*,#12398,.T.);
#17717=ORIENTED_EDGE('',*,*,#12399,.T.);
#17718=ORIENTED_EDGE('',*,*,#12400,.F.);
#17719=ORIENTED_EDGE('',*,*,#12384,.F.);
#17720=ORIENTED_EDGE('',*,*,#12382,.F.);
#17721=ORIENTED_EDGE('',*,*,#12401,.F.);
#17722=ORIENTED_EDGE('',*,*,#12357,.F.);
#17723=ORIENTED_EDGE('',*,*,#12402,.F.);
#17724=ORIENTED_EDGE('',*,*,#12269,.F.);
#17725=ORIENTED_EDGE('',*,*,#12267,.F.);
#17726=ORIENTED_EDGE('',*,*,#12162,.F.);
#17727=ORIENTED_EDGE('',*,*,#12403,.F.);
#17728=ORIENTED_EDGE('',*,*,#12380,.F.);
#17729=ORIENTED_EDGE('',*,*,#12402,.T.);
#17730=ORIENTED_EDGE('',*,*,#12356,.T.);
#17731=ORIENTED_EDGE('',*,*,#12379,.F.);
#17732=ORIENTED_EDGE('',*,*,#12270,.T.);
#17733=ORIENTED_EDGE('',*,*,#12366,.F.);
#17734=ORIENTED_EDGE('',*,*,#11887,.F.);
#17735=ORIENTED_EDGE('',*,*,#12371,.F.);
#17736=ORIENTED_EDGE('',*,*,#12368,.F.);
#17737=ORIENTED_EDGE('',*,*,#12404,.T.);
#17738=ORIENTED_EDGE('',*,*,#12405,.T.);
#17739=ORIENTED_EDGE('',*,*,#12385,.T.);
#17740=ORIENTED_EDGE('',*,*,#12400,.T.);
#17741=ORIENTED_EDGE('',*,*,#12406,.T.);
#17742=ORIENTED_EDGE('',*,*,#12407,.T.);
#17743=ORIENTED_EDGE('',*,*,#12406,.F.);
#17744=ORIENTED_EDGE('',*,*,#12399,.F.);
#17745=ORIENTED_EDGE('',*,*,#12408,.T.);
#17746=ORIENTED_EDGE('',*,*,#12409,.F.);
#17747=ORIENTED_EDGE('',*,*,#12405,.F.);
#17748=ORIENTED_EDGE('',*,*,#12410,.F.);
#17749=ORIENTED_EDGE('',*,*,#12411,.F.);
#17750=ORIENTED_EDGE('',*,*,#12390,.T.);
#17751=ORIENTED_EDGE('',*,*,#12412,.T.);
#17752=ORIENTED_EDGE('',*,*,#12413,.T.);
#17753=ORIENTED_EDGE('',*,*,#12386,.T.);
#17754=ORIENTED_EDGE('',*,*,#12414,.T.);
#17755=ORIENTED_EDGE('',*,*,#12415,.F.);
#17756=ORIENTED_EDGE('',*,*,#12416,.T.);
#17757=ORIENTED_EDGE('',*,*,#12417,.F.);
#17758=ORIENTED_EDGE('',*,*,#12418,.T.);
#17759=ORIENTED_EDGE('',*,*,#12419,.T.);
#17760=ORIENTED_EDGE('',*,*,#12420,.T.);
#17761=ORIENTED_EDGE('',*,*,#12421,.F.);
#17762=ORIENTED_EDGE('',*,*,#12422,.T.);
#17763=ORIENTED_EDGE('',*,*,#12423,.T.);
#17764=ORIENTED_EDGE('',*,*,#12424,.F.);
#17765=ORIENTED_EDGE('',*,*,#12420,.F.);
#17766=ORIENTED_EDGE('',*,*,#12425,.T.);
#17767=ORIENTED_EDGE('',*,*,#12426,.F.);
#17768=ORIENTED_EDGE('',*,*,#12360,.T.);
#17769=ORIENTED_EDGE('',*,*,#12427,.T.);
#17770=ORIENTED_EDGE('',*,*,#12415,.T.);
#17771=ORIENTED_EDGE('',*,*,#12428,.T.);
#17772=ORIENTED_EDGE('',*,*,#12429,.T.);
#17773=ORIENTED_EDGE('',*,*,#12430,.T.);
#17774=ORIENTED_EDGE('',*,*,#12431,.T.);
#17775=ORIENTED_EDGE('',*,*,#12432,.T.);
#17776=ORIENTED_EDGE('',*,*,#12433,.T.);
#17777=ORIENTED_EDGE('',*,*,#12434,.T.);
#17778=ORIENTED_EDGE('',*,*,#12419,.F.);
#17779=ORIENTED_EDGE('',*,*,#12435,.F.);
#17780=ORIENTED_EDGE('',*,*,#12436,.F.);
#17781=ORIENTED_EDGE('',*,*,#12425,.F.);
#17782=ORIENTED_EDGE('',*,*,#12437,.T.);
#17783=ORIENTED_EDGE('',*,*,#12438,.F.);
#17784=ORIENTED_EDGE('',*,*,#12439,.T.);
#17785=ORIENTED_EDGE('',*,*,#12440,.F.);
#17786=ORIENTED_EDGE('',*,*,#12441,.T.);
#17787=ORIENTED_EDGE('',*,*,#12434,.F.);
#17788=ORIENTED_EDGE('',*,*,#12442,.T.);
#17789=ORIENTED_EDGE('',*,*,#12443,.T.);
#17790=ORIENTED_EDGE('',*,*,#12444,.F.);
#17791=ORIENTED_EDGE('',*,*,#12445,.T.);
#17792=ORIENTED_EDGE('',*,*,#12446,.F.);
#17793=ORIENTED_EDGE('',*,*,#12447,.T.);
#17794=ORIENTED_EDGE('',*,*,#12421,.T.);
#17795=ORIENTED_EDGE('',*,*,#12424,.T.);
#17796=ORIENTED_EDGE('',*,*,#12441,.F.);
#17797=ORIENTED_EDGE('',*,*,#12448,.T.);
#17798=ORIENTED_EDGE('',*,*,#12449,.T.);
#17799=ORIENTED_EDGE('',*,*,#12450,.T.);
#17800=ORIENTED_EDGE('',*,*,#12451,.T.);
#17801=ORIENTED_EDGE('',*,*,#12452,.F.);
#17802=ORIENTED_EDGE('',*,*,#12453,.T.);
#17803=ORIENTED_EDGE('',*,*,#12454,.T.);
#17804=ORIENTED_EDGE('',*,*,#12396,.T.);
#17805=ORIENTED_EDGE('',*,*,#12455,.T.);
#17806=ORIENTED_EDGE('',*,*,#12456,.T.);
#17807=ORIENTED_EDGE('',*,*,#12438,.T.);
#17808=ORIENTED_EDGE('',*,*,#12445,.F.);
#17809=ORIENTED_EDGE('',*,*,#12457,.T.);
#17810=ORIENTED_EDGE('',*,*,#12429,.F.);
#17811=ORIENTED_EDGE('',*,*,#12458,.T.);
#17812=ORIENTED_EDGE('',*,*,#12459,.T.);
#17813=ORIENTED_EDGE('',*,*,#12453,.F.);
#17814=ORIENTED_EDGE('',*,*,#12451,.F.);
#17815=ORIENTED_EDGE('',*,*,#12460,.T.);
#17816=ORIENTED_EDGE('',*,*,#12430,.F.);
#17817=ORIENTED_EDGE('',*,*,#12457,.F.);
#17818=ORIENTED_EDGE('',*,*,#12450,.F.);
#17819=ORIENTED_EDGE('',*,*,#12461,.F.);
#17820=ORIENTED_EDGE('',*,*,#12462,.T.);
#17821=ORIENTED_EDGE('',*,*,#12463,.T.);
#17822=ORIENTED_EDGE('',*,*,#12464,.F.);
#17823=ORIENTED_EDGE('',*,*,#12465,.F.);
#17824=ORIENTED_EDGE('',*,*,#12431,.F.);
#17825=ORIENTED_EDGE('',*,*,#12460,.F.);
#17826=ORIENTED_EDGE('',*,*,#12449,.F.);
#17827=ORIENTED_EDGE('',*,*,#12466,.T.);
#17828=ORIENTED_EDGE('',*,*,#12467,.T.);
#17829=ORIENTED_EDGE('',*,*,#12461,.T.);
#17830=ORIENTED_EDGE('',*,*,#12456,.F.);
#17831=ORIENTED_EDGE('',*,*,#12468,.F.);
#17832=ORIENTED_EDGE('',*,*,#12469,.T.);
#17833=ORIENTED_EDGE('',*,*,#12470,.T.);
#17834=ORIENTED_EDGE('',*,*,#12471,.F.);
#17835=ORIENTED_EDGE('',*,*,#12472,.F.);
#17836=ORIENTED_EDGE('',*,*,#12473,.F.);
#17837=ORIENTED_EDGE('',*,*,#12439,.F.);
#17838=ORIENTED_EDGE('',*,*,#12455,.F.);
#17839=ORIENTED_EDGE('',*,*,#12395,.T.);
#17840=ORIENTED_EDGE('',*,*,#12474,.T.);
#17841=ORIENTED_EDGE('',*,*,#12468,.T.);
#17842=ORIENTED_EDGE('',*,*,#12475,.T.);
#17843=ORIENTED_EDGE('',*,*,#12158,.T.);
#17844=ORIENTED_EDGE('',*,*,#11997,.T.);
#17845=ORIENTED_EDGE('',*,*,#12376,.T.);
#17846=ORIENTED_EDGE('',*,*,#12476,.T.);
#17847=ORIENTED_EDGE('',*,*,#12436,.T.);
#17848=ORIENTED_EDGE('',*,*,#12477,.T.);
#17849=ORIENTED_EDGE('',*,*,#12375,.T.);
#17850=ORIENTED_EDGE('',*,*,#12477,.F.);
#17851=ORIENTED_EDGE('',*,*,#12478,.T.);
#17852=ORIENTED_EDGE('',*,*,#12475,.F.);
#17853=ORIENTED_EDGE('',*,*,#12377,.F.);
#17854=ORIENTED_EDGE('',*,*,#12426,.T.);
#17855=ORIENTED_EDGE('',*,*,#12476,.F.);
#17856=ORIENTED_EDGE('',*,*,#12479,.F.);
#17857=ORIENTED_EDGE('',*,*,#12417,.T.);
#17858=ORIENTED_EDGE('',*,*,#12480,.T.);
#17859=ORIENTED_EDGE('',*,*,#12159,.T.);
#17860=ORIENTED_EDGE('',*,*,#12478,.F.);
#17861=ORIENTED_EDGE('',*,*,#12435,.T.);
#17862=ORIENTED_EDGE('',*,*,#12418,.F.);
#17863=ORIENTED_EDGE('',*,*,#12481,.F.);
#17864=ORIENTED_EDGE('',*,*,#12440,.T.);
#17865=ORIENTED_EDGE('',*,*,#12473,.T.);
#17866=ORIENTED_EDGE('',*,*,#12482,.T.);
#17867=ORIENTED_EDGE('',*,*,#12483,.T.);
#17868=ORIENTED_EDGE('',*,*,#12410,.T.);
#17869=ORIENTED_EDGE('',*,*,#12404,.F.);
#17870=ORIENTED_EDGE('',*,*,#12161,.T.);
#17871=ORIENTED_EDGE('',*,*,#12484,.T.);
#17872=ORIENTED_EDGE('',*,*,#12358,.T.);
#17873=ORIENTED_EDGE('',*,*,#12401,.T.);
#17874=ORIENTED_EDGE('',*,*,#12484,.F.);
#17875=ORIENTED_EDGE('',*,*,#12160,.F.);
#17876=ORIENTED_EDGE('',*,*,#12480,.F.);
#17877=ORIENTED_EDGE('',*,*,#12416,.F.);
#17878=ORIENTED_EDGE('',*,*,#12427,.F.);
#17879=ORIENTED_EDGE('',*,*,#12359,.F.);
#17880=ORIENTED_EDGE('',*,*,#12250,.T.);
#17881=ORIENTED_EDGE('',*,*,#12485,.T.);
#17882=ORIENTED_EDGE('',*,*,#12082,.T.);
#17883=ORIENTED_EDGE('',*,*,#12485,.F.);
#17884=ORIENTED_EDGE('',*,*,#12486,.T.);
#17885=ORIENTED_EDGE('',*,*,#12487,.T.);
#17886=ORIENTED_EDGE('',*,*,#12488,.T.);
#17887=ORIENTED_EDGE('',*,*,#12084,.T.);
#17888=ORIENTED_EDGE('',*,*,#12087,.T.);
#17889=ORIENTED_EDGE('',*,*,#12487,.F.);
#17890=ORIENTED_EDGE('',*,*,#12489,.F.);
#17891=ORIENTED_EDGE('',*,*,#11923,.F.);
#17892=ORIENTED_EDGE('',*,*,#12490,.F.);
#17893=ORIENTED_EDGE('',*,*,#12491,.F.);
#17894=ORIENTED_EDGE('',*,*,#12214,.F.);
#17895=ORIENTED_EDGE('',*,*,#12492,.T.);
#17896=ORIENTED_EDGE('',*,*,#12490,.T.);
#17897=ORIENTED_EDGE('',*,*,#11922,.F.);
#17898=ORIENTED_EDGE('',*,*,#12079,.F.);
#17899=ORIENTED_EDGE('',*,*,#12085,.F.);
#17900=ORIENTED_EDGE('',*,*,#12488,.F.);
#17901=ORIENTED_EDGE('',*,*,#12491,.T.);
#17902=ORIENTED_EDGE('',*,*,#12492,.F.);
#17903=ORIENTED_EDGE('',*,*,#12077,.F.);
#17904=ORIENTED_EDGE('',*,*,#11924,.T.);
#17905=ORIENTED_EDGE('',*,*,#12489,.T.);
#17906=ORIENTED_EDGE('',*,*,#12486,.F.);
#17907=ORIENTED_EDGE('',*,*,#12086,.F.);
#17908=ORIENTED_EDGE('',*,*,#12483,.F.);
#17909=ORIENTED_EDGE('',*,*,#12493,.F.);
#17910=ORIENTED_EDGE('',*,*,#12391,.T.);
#17911=ORIENTED_EDGE('',*,*,#12411,.T.);
#17912=ORIENTED_EDGE('',*,*,#12482,.F.);
#17913=ORIENTED_EDGE('',*,*,#12472,.T.);
#17914=ORIENTED_EDGE('',*,*,#12494,.T.);
#17915=ORIENTED_EDGE('',*,*,#12493,.T.);
#17916=ORIENTED_EDGE('',*,*,#12433,.F.);
#17917=ORIENTED_EDGE('',*,*,#12495,.F.);
#17918=ORIENTED_EDGE('',*,*,#12496,.T.);
#17919=ORIENTED_EDGE('',*,*,#12497,.T.);
#17920=ORIENTED_EDGE('',*,*,#12498,.F.);
#17921=ORIENTED_EDGE('',*,*,#12499,.F.);
#17922=ORIENTED_EDGE('',*,*,#12442,.F.);
#17923=ORIENTED_EDGE('',*,*,#12432,.F.);
#17924=ORIENTED_EDGE('',*,*,#12465,.T.);
#17925=ORIENTED_EDGE('',*,*,#12500,.T.);
#17926=ORIENTED_EDGE('',*,*,#12495,.T.);
#17927=ORIENTED_EDGE('',*,*,#12459,.F.);
#17928=ORIENTED_EDGE('',*,*,#12501,.T.);
#17929=ORIENTED_EDGE('',*,*,#12502,.T.);
#17930=ORIENTED_EDGE('',*,*,#12503,.F.);
#17931=ORIENTED_EDGE('',*,*,#12428,.F.);
#17932=ORIENTED_EDGE('',*,*,#12414,.F.);
#17933=ORIENTED_EDGE('',*,*,#12479,.T.);
#17934=ORIENTED_EDGE('',*,*,#12407,.F.);
#17935=ORIENTED_EDGE('',*,*,#12504,.T.);
#17936=ORIENTED_EDGE('',*,*,#12458,.F.);
#17937=ORIENTED_EDGE('',*,*,#12504,.F.);
#17938=ORIENTED_EDGE('',*,*,#12409,.T.);
#17939=ORIENTED_EDGE('',*,*,#12505,.T.);
#17940=ORIENTED_EDGE('',*,*,#12501,.F.);
#17941=ORIENTED_EDGE('',*,*,#12506,.T.);
#17942=ORIENTED_EDGE('',*,*,#12446,.T.);
#17943=ORIENTED_EDGE('',*,*,#12452,.T.);
#17944=ORIENTED_EDGE('',*,*,#12437,.F.);
#17945=ORIENTED_EDGE('',*,*,#12481,.T.);
#17946=ORIENTED_EDGE('',*,*,#12423,.F.);
#17947=ORIENTED_EDGE('',*,*,#12506,.F.);
#17948=ORIENTED_EDGE('',*,*,#12507,.T.);
#17949=ORIENTED_EDGE('',*,*,#12508,.T.);
#17950=ORIENTED_EDGE('',*,*,#12509,.F.);
#17951=ORIENTED_EDGE('',*,*,#12494,.F.);
#17952=ORIENTED_EDGE('',*,*,#12471,.T.);
#17953=ORIENTED_EDGE('',*,*,#12510,.T.);
#17954=ORIENTED_EDGE('',*,*,#12392,.F.);
#17955=ORIENTED_EDGE('',*,*,#12403,.T.);
#17956=ORIENTED_EDGE('',*,*,#12511,.T.);
#17957=ORIENTED_EDGE('',*,*,#12512,.T.);
#17958=ORIENTED_EDGE('',*,*,#12513,.T.);
#17959=ORIENTED_EDGE('',*,*,#12511,.F.);
#17960=ORIENTED_EDGE('',*,*,#12513,.F.);
#17961=ORIENTED_EDGE('',*,*,#12514,.T.);
#17962=ORIENTED_EDGE('',*,*,#12515,.F.);
#17963=ORIENTED_EDGE('',*,*,#12516,.T.);
#17964=ORIENTED_EDGE('',*,*,#12517,.F.);
#17965=ORIENTED_EDGE('',*,*,#12443,.F.);
#17966=ORIENTED_EDGE('',*,*,#12499,.T.);
#17967=ORIENTED_EDGE('',*,*,#12518,.F.);
#17968=ORIENTED_EDGE('',*,*,#12514,.F.);
#17969=ORIENTED_EDGE('',*,*,#12512,.F.);
#17970=ORIENTED_EDGE('',*,*,#12500,.F.);
#17971=ORIENTED_EDGE('',*,*,#12464,.T.);
#17972=ORIENTED_EDGE('',*,*,#12519,.T.);
#17973=ORIENTED_EDGE('',*,*,#12496,.F.);
#17974=ORIENTED_EDGE('',*,*,#12448,.F.);
#17975=ORIENTED_EDGE('',*,*,#12444,.T.);
#17976=ORIENTED_EDGE('',*,*,#12517,.T.);
#17977=ORIENTED_EDGE('',*,*,#12466,.F.);
#17978=ORIENTED_EDGE('',*,*,#12498,.T.);
#17979=ORIENTED_EDGE('',*,*,#12520,.T.);
#17980=ORIENTED_EDGE('',*,*,#12521,.T.);
#17981=ORIENTED_EDGE('',*,*,#12515,.T.);
#17982=ORIENTED_EDGE('',*,*,#12518,.T.);
#17983=ORIENTED_EDGE('',*,*,#12520,.F.);
#17984=ORIENTED_EDGE('',*,*,#12497,.F.);
#17985=ORIENTED_EDGE('',*,*,#12519,.F.);
#17986=ORIENTED_EDGE('',*,*,#12463,.F.);
#17987=ORIENTED_EDGE('',*,*,#12522,.F.);
#17988=ORIENTED_EDGE('',*,*,#12467,.F.);
#17989=ORIENTED_EDGE('',*,*,#12516,.F.);
#17990=ORIENTED_EDGE('',*,*,#12521,.F.);
#17991=ORIENTED_EDGE('',*,*,#12522,.T.);
#17992=ORIENTED_EDGE('',*,*,#12462,.F.);
#17993=ORIENTED_EDGE('',*,*,#12393,.F.);
#17994=ORIENTED_EDGE('',*,*,#12510,.F.);
#17995=ORIENTED_EDGE('',*,*,#12470,.F.);
#17996=ORIENTED_EDGE('',*,*,#12523,.F.);
#17997=ORIENTED_EDGE('',*,*,#12474,.F.);
#17998=ORIENTED_EDGE('',*,*,#12394,.F.);
#17999=ORIENTED_EDGE('',*,*,#12523,.T.);
#18000=ORIENTED_EDGE('',*,*,#12469,.F.);
#18001=ORIENTED_EDGE('',*,*,#12389,.F.);
#18002=ORIENTED_EDGE('',*,*,#12524,.T.);
#18003=ORIENTED_EDGE('',*,*,#12525,.F.);
#18004=ORIENTED_EDGE('',*,*,#12412,.F.);
#18005=ORIENTED_EDGE('',*,*,#12387,.F.);
#18006=ORIENTED_EDGE('',*,*,#12413,.F.);
#18007=ORIENTED_EDGE('',*,*,#12525,.T.);
#18008=ORIENTED_EDGE('',*,*,#12526,.T.);
#18009=ORIENTED_EDGE('',*,*,#12388,.F.);
#18010=ORIENTED_EDGE('',*,*,#12526,.F.);
#18011=ORIENTED_EDGE('',*,*,#12524,.F.);
#18012=ORIENTED_EDGE('',*,*,#12454,.F.);
#18013=ORIENTED_EDGE('',*,*,#12503,.T.);
#18014=ORIENTED_EDGE('',*,*,#12527,.T.);
#18015=ORIENTED_EDGE('',*,*,#12397,.F.);
#18016=ORIENTED_EDGE('',*,*,#12398,.F.);
#18017=ORIENTED_EDGE('',*,*,#12527,.F.);
#18018=ORIENTED_EDGE('',*,*,#12502,.F.);
#18019=ORIENTED_EDGE('',*,*,#12505,.F.);
#18020=ORIENTED_EDGE('',*,*,#12408,.F.);
#18021=ORIENTED_EDGE('',*,*,#12422,.F.);
#18022=ORIENTED_EDGE('',*,*,#12528,.T.);
#18023=ORIENTED_EDGE('',*,*,#12529,.T.);
#18024=ORIENTED_EDGE('',*,*,#12507,.F.);
#18025=ORIENTED_EDGE('',*,*,#12447,.F.);
#18026=ORIENTED_EDGE('',*,*,#12509,.T.);
#18027=ORIENTED_EDGE('',*,*,#12530,.T.);
#18028=ORIENTED_EDGE('',*,*,#12528,.F.);
#18029=ORIENTED_EDGE('',*,*,#12530,.F.);
#18030=ORIENTED_EDGE('',*,*,#12508,.F.);
#18031=ORIENTED_EDGE('',*,*,#12529,.F.);
#18032=ORIENTED_EDGE('',*,*,#12070,.F.);
#18033=ORIENTED_EDGE('',*,*,#12203,.F.);
#18034=ORIENTED_EDGE('',*,*,#12207,.F.);
#18035=ORIENTED_EDGE('',*,*,#12531,.F.);
#18036=ORIENTED_EDGE('',*,*,#11917,.F.);
#18037=ORIENTED_EDGE('',*,*,#11938,.F.);
#18038=ORIENTED_EDGE('',*,*,#12071,.F.);
#18039=ORIENTED_EDGE('',*,*,#12531,.T.);
#18040=ORIENTED_EDGE('',*,*,#12206,.F.);
#18041=ORIENTED_EDGE('',*,*,#12204,.F.);
#18042=ORIENTED_EDGE('',*,*,#12074,.F.);
#18043=ORIENTED_EDGE('',*,*,#12532,.T.);
#18044=ORIENTED_EDGE('',*,*,#12533,.F.);
#18045=ORIENTED_EDGE('',*,*,#11935,.F.);
#18046=ORIENTED_EDGE('',*,*,#12072,.F.);
#18047=ORIENTED_EDGE('',*,*,#11936,.F.);
#18048=ORIENTED_EDGE('',*,*,#12533,.T.);
#18049=ORIENTED_EDGE('',*,*,#12534,.T.);
#18050=ORIENTED_EDGE('',*,*,#12073,.F.);
#18051=ORIENTED_EDGE('',*,*,#12534,.F.);
#18052=ORIENTED_EDGE('',*,*,#12532,.F.);
#18053=ORIENTED_EDGE('',*,*,#12053,.F.);
#18054=ORIENTED_EDGE('',*,*,#12535,.T.);
#18055=ORIENTED_EDGE('',*,*,#12536,.T.);
#18056=ORIENTED_EDGE('',*,*,#12065,.F.);
#18057=ORIENTED_EDGE('',*,*,#12057,.F.);
#18058=ORIENTED_EDGE('',*,*,#12199,.T.);
#18059=ORIENTED_EDGE('',*,*,#12537,.T.);
#18060=ORIENTED_EDGE('',*,*,#12535,.F.);
#18061=ORIENTED_EDGE('',*,*,#11921,.F.);
#18062=ORIENTED_EDGE('',*,*,#11930,.F.);
#18063=ORIENTED_EDGE('',*,*,#12067,.F.);
#18064=ORIENTED_EDGE('',*,*,#12538,.T.);
#18065=ORIENTED_EDGE('',*,*,#12197,.F.);
#18066=ORIENTED_EDGE('',*,*,#12058,.F.);
#18067=ORIENTED_EDGE('',*,*,#12066,.F.);
#18068=ORIENTED_EDGE('',*,*,#12536,.F.);
#18069=ORIENTED_EDGE('',*,*,#12537,.F.);
#18070=ORIENTED_EDGE('',*,*,#12198,.F.);
#18071=ORIENTED_EDGE('',*,*,#12538,.F.);
#18072=ORIENTED_EDGE('',*,*,#12076,.F.);
#18073=ORIENTED_EDGE('',*,*,#12211,.F.);
#18074=ORIENTED_EDGE('',*,*,#11926,.F.);
#18075=ORIENTED_EDGE('',*,*,#12328,.F.);
#18076=ORIENTED_EDGE('',*,*,#12035,.F.);
#18077=ORIENTED_EDGE('',*,*,#12327,.F.);
#18078=ORIENTED_EDGE('',*,*,#12325,.F.);
#18079=ORIENTED_EDGE('',*,*,#12320,.F.);
#18080=ORIENTED_EDGE('',*,*,#12302,.F.);
#18081=ORIENTED_EDGE('',*,*,#12539,.F.);
#18082=ORIENTED_EDGE('',*,*,#12292,.F.);
#18083=ORIENTED_EDGE('',*,*,#12540,.F.);
#18084=ORIENTED_EDGE('',*,*,#12284,.F.);
#18085=ORIENTED_EDGE('',*,*,#12541,.F.);
#18086=ORIENTED_EDGE('',*,*,#12276,.F.);
#18087=ORIENTED_EDGE('',*,*,#12542,.F.);
#18088=ORIENTED_EDGE('',*,*,#12541,.T.);
#18089=ORIENTED_EDGE('',*,*,#12283,.F.);
#18090=ORIENTED_EDGE('',*,*,#12313,.F.);
#18091=ORIENTED_EDGE('',*,*,#12277,.F.);
#18092=ORIENTED_EDGE('',*,*,#12539,.T.);
#18093=ORIENTED_EDGE('',*,*,#12301,.F.);
#18094=ORIENTED_EDGE('',*,*,#12309,.F.);
#18095=ORIENTED_EDGE('',*,*,#12293,.F.);
#18096=ORIENTED_EDGE('',*,*,#12542,.T.);
#18097=ORIENTED_EDGE('',*,*,#12275,.F.);
#18098=ORIENTED_EDGE('',*,*,#12315,.F.);
#18099=ORIENTED_EDGE('',*,*,#12285,.F.);
#18100=ORIENTED_EDGE('',*,*,#12540,.T.);
#18101=ORIENTED_EDGE('',*,*,#12291,.F.);
#18102=ORIENTED_EDGE('',*,*,#12311,.F.);
#18103=ORIENTED_EDGE('',*,*,#12303,.F.);
#18104=ORIENTED_EDGE('',*,*,#11878,.F.);
#18105=ORIENTED_EDGE('',*,*,#12340,.F.);
#18106=ORIENTED_EDGE('',*,*,#12227,.F.);
#18107=ORIENTED_EDGE('',*,*,#11872,.T.);
#18108=ORIENTED_EDGE('',*,*,#11874,.F.);
#18109=ORIENTED_EDGE('',*,*,#12259,.F.);
#18110=ORIENTED_EDGE('',*,*,#11959,.F.);
#18111=ORIENTED_EDGE('',*,*,#11893,.F.);
#18112=ORIENTED_EDGE('',*,*,#11967,.F.);
#18113=ORIENTED_EDGE('',*,*,#11961,.F.);
#18114=ORIENTED_EDGE('',*,*,#11903,.F.);
#18115=ORIENTED_EDGE('',*,*,#11973,.T.);
#18116=ORIENTED_EDGE('',*,*,#12254,.F.);
#18117=ORIENTED_EDGE('',*,*,#12255,.F.);
#18118=ORIENTED_EDGE('',*,*,#12017,.T.);
#18119=ORIENTED_EDGE('',*,*,#11848,.T.);
#18120=ORIENTED_EDGE('',*,*,#11854,.F.);
#18121=ORIENTED_EDGE('',*,*,#12148,.T.);
#18122=ORIENTED_EDGE('',*,*,#12138,.F.);
#18123=ORIENTED_EDGE('',*,*,#12140,.T.);
#18124=ORIENTED_EDGE('',*,*,#11861,.F.);
#18125=ORIENTED_EDGE('',*,*,#12013,.F.);
#18126=ORIENTED_EDGE('',*,*,#12004,.F.);
#18127=ORIENTED_EDGE('',*,*,#12012,.F.);
#18128=ORIENTED_EDGE('',*,*,#12256,.F.);
#18129=ORIENTED_EDGE('',*,*,#12260,.F.);
#18130=ORIENTED_EDGE('',*,*,#12007,.T.);
#18131=ORIENTED_EDGE('',*,*,#12169,.F.);
#18132=ORIENTED_EDGE('',*,*,#11995,.F.);
#18133=ORIENTED_EDGE('',*,*,#12032,.T.);
#18134=ORIENTED_EDGE('',*,*,#12155,.F.);
#18135=ORIENTED_EDGE('',*,*,#12217,.F.);
#18136=ORIENTED_EDGE('',*,*,#11986,.T.);
#18935=B_SPLINE_SURFACE_WITH_KNOTS('',3,3,((#91656,#91657,#91658,#91659,
#91660,#91661,#91662,#91663,#91664,#91665,#91666,#91667,#91668,#91669,#91670,
#91671,#91672,#91673),(#91674,#91675,#91676,#91677,#91678,#91679,#91680,
#91681,#91682,#91683,#91684,#91685,#91686,#91687,#91688,#91689,#91690,#91691),
(#91692,#91693,#91694,#91695,#91696,#91697,#91698,#91699,#91700,#91701,
#91702,#91703,#91704,#91705,#91706,#91707,#91708,#91709),(#91710,#91711,
#91712,#91713,#91714,#91715,#91716,#91717,#91718,#91719,#91720,#91721,#91722,
#91723,#91724,#91725,#91726,#91727),(#91728,#91729,#91730,#91731,#91732,
#91733,#91734,#91735,#91736,#91737,#91738,#91739,#91740,#91741,#91742,#91743,
#91744,#91745),(#91746,#91747,#91748,#91749,#91750,#91751,#91752,#91753,
#91754,#91755,#91756,#91757,#91758,#91759,#91760,#91761,#91762,#91763)),
 .UNSPECIFIED.,.F.,.T.,.F.,(4,1,1,4),(4,1,1,1,1,1,1,1,1,1,1,1,1,1,1,4),
(0.,0.285714285714286,0.571428571428571,1.),(0.,0.177176435663881,0.354352871327763,
0.531529306991644,0.708705742655525,0.885882178319406,1.06305861398329,
1.18117623775921,1.29929386153513,1.41741148531105,1.65364673286289,1.77176435663881,
1.94894079230269,2.12611722796658,2.30329366363046,2.48047009929434),
 .UNSPECIFIED.);
#19674=ADVANCED_FACE('',(#5740),#1249,.T.);
#19675=ADVANCED_FACE('',(#5741),#1529,.F.);
#19676=ADVANCED_FACE('',(#5742),#1250,.T.);
#19677=ADVANCED_FACE('',(#5743),#1530,.F.);
#19678=ADVANCED_FACE('',(#5744),#1251,.T.);
#19679=ADVANCED_FACE('',(#5745),#4862,.T.);
#19680=ADVANCED_FACE('',(#5746),#1252,.T.);
#19681=ADVANCED_FACE('',(#5747),#1531,.F.);
#19682=ADVANCED_FACE('',(#5748),#1253,.T.);
#19683=ADVANCED_FACE('',(#5749),#1532,.F.);
#19684=ADVANCED_FACE('',(#5750),#4863,.T.);
#19685=ADVANCED_FACE('',(#5751),#1533,.T.);
#19686=ADVANCED_FACE('',(#5752),#4864,.T.);
#19687=ADVANCED_FACE('',(#5753),#1534,.F.);
#19688=ADVANCED_FACE('',(#5754),#4865,.T.);
#19689=ADVANCED_FACE('',(#5755),#4866,.T.);
#19690=ADVANCED_FACE('',(#5756),#4867,.T.);
#19691=ADVANCED_FACE('',(#5757),#1535,.F.);
#19692=ADVANCED_FACE('',(#5758),#1536,.F.);
#19693=ADVANCED_FACE('',(#5759),#1537,.T.);
#19694=ADVANCED_FACE('',(#5760),#1538,.T.);
#19695=ADVANCED_FACE('',(#5761),#1539,.T.);
#19696=ADVANCED_FACE('',(#5762),#4868,.T.);
#19697=ADVANCED_FACE('',(#5763),#197,.T.);
#19698=ADVANCED_FACE('',(#5764),#4869,.T.);
#19699=ADVANCED_FACE('',(#5765),#4870,.T.);
#19700=ADVANCED_FACE('',(#5766),#4871,.T.);
#19701=ADVANCED_FACE('',(#5767),#4872,.T.);
#19702=ADVANCED_FACE('',(#5768),#198,.T.);
#19703=ADVANCED_FACE('',(#5769),#199,.T.);
#19704=ADVANCED_FACE('',(#5770),#1540,.T.);
#19705=ADVANCED_FACE('',(#5771),#4873,.T.);
#19706=ADVANCED_FACE('',(#5772),#1541,.F.);
#19707=ADVANCED_FACE('',(#5773),#4874,.T.);
#19708=ADVANCED_FACE('',(#5774),#1542,.T.);
#19709=ADVANCED_FACE('',(#5775),#1254,.T.);
#19710=ADVANCED_FACE('',(#5776),#4875,.T.);
#19711=ADVANCED_FACE('',(#5777),#4876,.T.);
#19712=ADVANCED_FACE('',(#5778),#1543,.T.);
#19713=ADVANCED_FACE('',(#5779),#1255,.T.);
#19714=ADVANCED_FACE('',(#5780),#4877,.T.);
#19715=ADVANCED_FACE('',(#5781),#4878,.T.);
#19716=ADVANCED_FACE('',(#5782,#1760),#1544,.T.);
#19717=ADVANCED_FACE('',(#5783),#1256,.T.);
#19718=ADVANCED_FACE('',(#5784),#4879,.F.);
#19719=ADVANCED_FACE('',(#5785),#18935,.F.);
#19720=ADVANCED_FACE('',(#5786,#1761),#4880,.T.);
#19721=ADVANCED_FACE('',(#5787),#1257,.T.);
#19722=ADVANCED_FACE('',(#5788),#1545,.T.);
#19723=ADVANCED_FACE('',(#5789),#4881,.T.);
#19724=ADVANCED_FACE('',(#5790),#4882,.T.);
#19725=ADVANCED_FACE('',(#5791),#4883,.T.);
#19726=ADVANCED_FACE('',(#5792),#200,.T.);
#19727=ADVANCED_FACE('',(#5793),#201,.T.);
#19728=ADVANCED_FACE('',(#5794),#4884,.T.);
#19729=ADVANCED_FACE('',(#5795),#202,.T.);
#19730=ADVANCED_FACE('',(#5796),#4885,.T.);
#19731=ADVANCED_FACE('',(#5797),#4886,.T.);
#19732=ADVANCED_FACE('',(#5798),#4887,.T.);
#19733=ADVANCED_FACE('',(#5799),#1546,.T.);
#19734=ADVANCED_FACE('',(#5800),#4888,.T.);
#19735=ADVANCED_FACE('',(#5801),#4889,.F.);
#19736=ADVANCED_FACE('',(#5802),#4890,.T.);
#19737=ADVANCED_FACE('',(#5803),#4891,.F.);
#19738=ADVANCED_FACE('',(#5804),#4892,.T.);
#19739=ADVANCED_FACE('',(#5805),#4893,.T.);
#19740=ADVANCED_FACE('',(#5806),#203,.T.);
#19741=ADVANCED_FACE('',(#5807),#4894,.T.);
#19742=ADVANCED_FACE('',(#5808),#204,.T.);
#19743=ADVANCED_FACE('',(#5809),#4895,.T.);
#19744=ADVANCED_FACE('',(#5810,#1762),#1547,.T.);
#19745=ADVANCED_FACE('',(#5811),#1258,.T.);
#19746=ADVANCED_FACE('',(#5812),#4896,.T.);
#19747=ADVANCED_FACE('',(#5813),#4897,.F.);
#19748=ADVANCED_FACE('',(#5814),#1259,.T.);
#19749=ADVANCED_FACE('',(#5815),#4898,.F.);
#19750=ADVANCED_FACE('',(#5816,#1763),#1548,.T.);
#19751=ADVANCED_FACE('',(#5817),#1260,.T.);
#19752=ADVANCED_FACE('',(#5818),#1261,.T.);
#19753=ADVANCED_FACE('',(#5819),#4899,.T.);
#19754=ADVANCED_FACE('',(#5820),#4900,.T.);
#19755=ADVANCED_FACE('',(#5821),#1549,.T.);
#19756=ADVANCED_FACE('',(#5822),#4901,.T.);
#19757=ADVANCED_FACE('',(#5823),#1550,.T.);
#19758=ADVANCED_FACE('',(#5824),#4902,.T.);
#19759=ADVANCED_FACE('',(#5825),#1551,.T.);
#19760=ADVANCED_FACE('',(#5826),#4903,.T.);
#19761=ADVANCED_FACE('',(#5827),#4904,.T.);
#19762=ADVANCED_FACE('',(#5828),#205,.T.);
#19763=ADVANCED_FACE('',(#5829),#4905,.T.);
#19764=ADVANCED_FACE('',(#5830),#206,.T.);
#19765=ADVANCED_FACE('',(#5831,#1764,#1765,#1766,#1767),#1552,.T.);
#19766=ADVANCED_FACE('',(#5832),#4906,.T.);
#19767=ADVANCED_FACE('',(#5833),#4907,.T.);
#19768=ADVANCED_FACE('',(#5834),#1262,.T.);
#19769=ADVANCED_FACE('',(#5835),#4908,.T.);
#19770=ADVANCED_FACE('',(#5836),#1553,.F.);
#19771=ADVANCED_FACE('',(#5837),#4909,.T.);
#19772=ADVANCED_FACE('',(#5838),#1554,.F.);
#19773=ADVANCED_FACE('',(#5839),#4910,.T.);
#19774=ADVANCED_FACE('',(#5840),#1555,.F.);
#19775=ADVANCED_FACE('',(#5841),#4911,.T.);
#19776=ADVANCED_FACE('',(#5842),#1556,.F.);
#19777=ADVANCED_FACE('',(#5843),#207,.T.);
#19778=ADVANCED_FACE('',(#5844),#4912,.T.);
#19779=ADVANCED_FACE('',(#5845),#4913,.T.);
#19780=ADVANCED_FACE('',(#5846),#4914,.T.);
#19781=ADVANCED_FACE('',(#5847),#4915,.T.);
#19782=ADVANCED_FACE('',(#5848),#208,.T.);
#19783=ADVANCED_FACE('',(#5849),#4916,.T.);
#19784=ADVANCED_FACE('',(#5850),#1557,.T.);
#19785=ADVANCED_FACE('',(#5851),#4917,.T.);
#19786=ADVANCED_FACE('',(#5852),#1263,.T.);
#19787=ADVANCED_FACE('',(#5853),#4918,.F.);
#19788=ADVANCED_FACE('',(#5854,#1768),#1558,.T.);
#19789=ADVANCED_FACE('',(#5855),#1264,.T.);
#19790=ADVANCED_FACE('',(#5856),#4919,.T.);
#19791=ADVANCED_FACE('',(#5857),#4920,.F.);
#19792=ADVANCED_FACE('',(#5858,#1769),#1559,.T.);
#19793=ADVANCED_FACE('',(#5859),#4921,.T.);
#19794=ADVANCED_FACE('',(#5860),#1560,.T.);
#19795=ADVANCED_FACE('',(#5861),#4922,.T.);
#19796=ADVANCED_FACE('',(#5862),#4923,.T.);
#19797=ADVANCED_FACE('',(#5863),#1561,.T.);
#19798=ADVANCED_FACE('',(#5864),#4924,.T.);
#19799=ADVANCED_FACE('',(#5865),#1562,.T.);
#19800=ADVANCED_FACE('',(#5866),#4925,.T.);
#19801=ADVANCED_FACE('',(#5867),#1563,.T.);
#19802=ADVANCED_FACE('',(#5868),#4926,.T.);
#19803=ADVANCED_FACE('',(#5869),#1564,.T.);
#19804=ADVANCED_FACE('',(#5870),#4927,.T.);
#19805=ADVANCED_FACE('',(#5871),#1565,.F.);
#19806=ADVANCED_FACE('',(#5872),#4928,.T.);
#19807=ADVANCED_FACE('',(#5873),#1566,.F.);
#19808=ADVANCED_FACE('',(#5874),#4929,.T.);
#19809=ADVANCED_FACE('',(#5875),#1567,.F.);
#19810=ADVANCED_FACE('',(#5876),#4930,.T.);
#19811=ADVANCED_FACE('',(#5877),#1568,.F.);
#19812=ADVANCED_FACE('',(#5878),#1265,.T.);
#19813=ADVANCED_FACE('',(#5879),#4931,.T.);
#19814=ADVANCED_FACE('',(#5880),#1569,.F.);
#19815=ADVANCED_FACE('',(#5881),#4932,.T.);
#19816=ADVANCED_FACE('',(#5882),#1570,.F.);
#19817=ADVANCED_FACE('',(#5883),#4933,.T.);
#19818=ADVANCED_FACE('',(#5884),#1571,.F.);
#19819=ADVANCED_FACE('',(#5885),#4934,.T.);
#19820=ADVANCED_FACE('',(#5886),#1572,.F.);
#19821=ADVANCED_FACE('',(#5887),#1266,.T.);
#19822=ADVANCED_FACE('',(#5888),#4935,.F.);
#19823=ADVANCED_FACE('',(#5889),#1267,.T.);
#19824=ADVANCED_FACE('',(#5890),#4936,.F.);
#19825=ADVANCED_FACE('',(#5891),#4937,.F.);
#19826=ADVANCED_FACE('',(#5892),#1268,.T.);
#19827=ADVANCED_FACE('',(#5893),#1269,.T.);
#19828=ADVANCED_FACE('',(#5894),#4938,.T.);
#19829=ADVANCED_FACE('',(#5895),#1270,.T.);
#19830=ADVANCED_FACE('',(#5896,#1770),#1573,.T.);
#19831=ADVANCED_FACE('',(#5897),#4939,.T.);
#19832=ADVANCED_FACE('',(#5898),#4940,.T.);
#19833=ADVANCED_FACE('',(#5899),#209,.T.);
#19834=ADVANCED_FACE('',(#5900),#210,.T.);
#19835=ADVANCED_FACE('',(#5901),#4941,.T.);
#19836=ADVANCED_FACE('',(#5902),#4942,.T.);
#19837=ADVANCED_FACE('',(#5903),#4943,.T.);
#19838=ADVANCED_FACE('',(#5904),#211,.T.);
#19839=ADVANCED_FACE('',(#5905),#1574,.F.);
#19840=ADVANCED_FACE('',(#5906),#4944,.T.);
#19841=ADVANCED_FACE('',(#5907),#4945,.T.);
#19842=ADVANCED_FACE('',(#5908),#4946,.T.);
#19843=ADVANCED_FACE('',(#5909),#4947,.T.);
#19844=ADVANCED_FACE('',(#5910),#212,.T.);
#19845=ADVANCED_FACE('',(#5911),#213,.T.);
#19846=ADVANCED_FACE('',(#5912),#1575,.T.);
#19847=ADVANCED_FACE('',(#5913),#4948,.T.);
#19848=ADVANCED_FACE('',(#5914),#4949,.T.);
#19849=ADVANCED_FACE('',(#5915),#4950,.T.);
#19850=ADVANCED_FACE('',(#5916),#214,.T.);
#19851=ADVANCED_FACE('',(#5917),#1271,.T.);
#19852=ADVANCED_FACE('',(#5918),#4951,.F.);
#19853=ADVANCED_FACE('',(#5919,#1771,#1772),#1576,.T.);
#19854=ADVANCED_FACE('',(#5920),#4952,.T.);
#19855=ADVANCED_FACE('',(#5921),#1577,.T.);
#19856=ADVANCED_FACE('',(#5922),#4953,.T.);
#19857=ADVANCED_FACE('',(#5923),#1578,.F.);
#19858=ADVANCED_FACE('',(#5924),#1579,.T.);
#19859=ADVANCED_FACE('',(#5925),#1580,.T.);
#19860=ADVANCED_FACE('',(#5926),#4954,.T.);
#19861=ADVANCED_FACE('',(#5927),#4955,.T.);
#19862=ADVANCED_FACE('',(#5928),#1581,.T.);
#19863=ADVANCED_FACE('',(#5929),#1582,.T.);
#19864=ADVANCED_FACE('',(#5930),#1583,.T.);
#19865=ADVANCED_FACE('',(#5931),#4956,.T.);
#19866=ADVANCED_FACE('',(#5932),#4957,.T.);
#19867=ADVANCED_FACE('',(#5933),#4958,.T.);
#19868=ADVANCED_FACE('',(#5934),#1584,.T.);
#19869=ADVANCED_FACE('',(#5935),#1585,.F.);
#19870=ADVANCED_FACE('',(#5936),#4959,.T.);
#19871=ADVANCED_FACE('',(#5937),#1586,.F.);
#19872=ADVANCED_FACE('',(#5938),#4960,.T.);
#19873=ADVANCED_FACE('',(#5939),#4961,.T.);
#19874=ADVANCED_FACE('',(#5940),#4962,.T.);
#19875=ADVANCED_FACE('',(#5941),#215,.T.);
#19876=ADVANCED_FACE('',(#5942),#216,.T.);
#19877=ADVANCED_FACE('',(#5943),#4963,.T.);
#19878=ADVANCED_FACE('',(#5944),#4964,.T.);
#19879=ADVANCED_FACE('',(#5945),#1587,.T.);
#19880=ADVANCED_FACE('',(#5946),#1272,.T.);
#19881=ADVANCED_FACE('',(#5947),#1273,.T.);
#19882=ADVANCED_FACE('',(#5948),#1588,.F.);
#19883=ADVANCED_FACE('',(#5949),#1589,.F.);
#19884=ADVANCED_FACE('',(#5950),#1590,.F.);
#19885=ADVANCED_FACE('',(#5951),#1591,.F.);
#19886=ADVANCED_FACE('',(#5952),#115,.F.);
#19887=ADVANCED_FACE('',(#5953),#4965,.T.);
#19888=ADVANCED_FACE('',(#5954),#1592,.F.);
#19889=ADVANCED_FACE('',(#5955),#4966,.T.);
#19890=ADVANCED_FACE('',(#5956),#1593,.F.);
#19891=ADVANCED_FACE('',(#5957),#4967,.T.);
#19892=ADVANCED_FACE('',(#5958),#1594,.F.);
#19893=ADVANCED_FACE('',(#5959),#4968,.T.);
#19894=ADVANCED_FACE('',(#5960),#1595,.F.);
#19895=ADVANCED_FACE('',(#5961),#1596,.F.);
#19896=ADVANCED_FACE('',(#5962),#1274,.T.);
#19897=ADVANCED_FACE('',(#5963),#4969,.F.);
#19898=ADVANCED_FACE('',(#5964),#1597,.F.);
#19899=ADVANCED_FACE('',(#5965),#116,.F.);
#19900=ADVANCED_FACE('',(#5966),#1275,.T.);
#19901=ADVANCED_FACE('',(#5967),#1598,.F.);
#19902=ADVANCED_FACE('',(#5968),#1599,.F.);
#19903=ADVANCED_FACE('',(#5969),#1600,.F.);
#19904=ADVANCED_FACE('',(#5970),#1601,.F.);
#19905=ADVANCED_FACE('',(#5971),#1602,.F.);
#19906=ADVANCED_FACE('',(#5972),#1603,.F.);
#19907=ADVANCED_FACE('',(#5973),#1604,.F.);
#19908=ADVANCED_FACE('',(#5974),#1605,.F.);
#19909=ADVANCED_FACE('',(#5975),#1606,.F.);
#19910=ADVANCED_FACE('',(#5976),#1607,.F.);
#19911=ADVANCED_FACE('',(#5977),#1608,.F.);
#19912=ADVANCED_FACE('',(#5978),#1609,.F.);
#19913=ADVANCED_FACE('',(#5979),#1610,.F.);
#19914=ADVANCED_FACE('',(#5980),#1611,.F.);
#19915=ADVANCED_FACE('',(#5981),#1612,.F.);
#19916=ADVANCED_FACE('',(#5982),#1613,.F.);
#19917=ADVANCED_FACE('',(#5983),#1614,.F.);
#19918=ADVANCED_FACE('',(#5984),#1615,.F.);
#19919=ADVANCED_FACE('',(#5985),#1616,.F.);
#19920=ADVANCED_FACE('',(#5986),#1617,.F.);
#19921=ADVANCED_FACE('',(#5987),#1618,.F.);
#19922=ADVANCED_FACE('',(#5988),#1619,.F.);
#19923=ADVANCED_FACE('',(#5989,#1773),#1620,.T.);
#19924=ADVANCED_FACE('',(#5990),#1621,.T.);
#19925=ADVANCED_FACE('',(#5991),#1622,.T.);
#19926=ADVANCED_FACE('',(#5992),#1623,.T.);
#19927=ADVANCED_FACE('',(#5993),#4970,.T.);
#19928=ADVANCED_FACE('',(#5994),#4971,.T.);
#19929=ADVANCED_FACE('',(#5995),#1624,.F.);
#19930=ADVANCED_FACE('',(#5996),#1625,.F.);
#19931=ADVANCED_FACE('',(#5997),#1626,.F.);
#19932=ADVANCED_FACE('',(#5998),#1627,.F.);
#19933=ADVANCED_FACE('',(#5999),#1628,.T.);
#19934=ADVANCED_FACE('',(#6000),#1629,.T.);
#19935=ADVANCED_FACE('',(#6001),#1630,.T.);
#19936=ADVANCED_FACE('',(#6002),#1631,.F.);
#19937=ADVANCED_FACE('',(#6003),#1632,.T.);
#19938=ADVANCED_FACE('',(#6004),#1633,.T.);
#20123=CLOSED_SHELL('',(#19674,#19675,#19676,#19677,#19678,#19679,#19680,
#19681,#19682,#19683,#19684,#19685,#19686,#19687,#19688,#19689,#19690,#19691,
#19692,#19693,#19694,#19695,#19696,#19697,#19698,#19699,#19700,#19701,#19702,
#19703,#19704,#19705,#19706,#19707,#19708,#19709,#19710,#19711,#19712,#19713,
#19714,#19715,#19716,#19717,#19718,#19719,#19720,#19721,#19722,#19723,#19724,
#19725,#19726,#19727,#19728,#19729,#19730,#19731,#19732,#19733,#19734,#19735,
#19736,#19737,#19738,#19739,#19740,#19741,#19742,#19743,#19744,#19745,#19746,
#19747,#19748,#19749,#19750,#19751,#19752,#19753,#19754,#19755,#19756,#19757,
#19758,#19759,#19760,#19761,#19762,#19763,#19764,#19765,#19766,#19767,#19768,
#19769,#19770,#19771,#19772,#19773,#19774,#19775,#19776,#19777,#19778,#19779,
#19780,#19781,#19782,#19783,#19784,#19785,#19786,#19787,#19788,#19789,#19790,
#19791,#19792,#19793,#19794,#19795,#19796,#19797,#19798,#19799,#19800,#19801,
#19802,#19803,#19804,#19805,#19806,#19807,#19808,#19809,#19810,#19811,#19812,
#19813,#19814,#19815,#19816,#19817,#19818,#19819,#19820,#19821,#19822,#19823,
#19824,#19825,#19826,#19827,#19828,#19829,#19830,#19831,#19832,#19833,#19834,
#19835,#19836,#19837,#19838,#19839,#19840,#19841,#19842,#19843,#19844,#19845,
#19846,#19847,#19848,#19849,#19850,#19851,#19852,#19853,#19854,#19855,#19856,
#19857,#19858,#19859,#19860,#19861,#19862,#19863,#19864,#19865,#19866,#19867,
#19868,#19869,#19870,#19871,#19872,#19873,#19874,#19875,#19876,#19877,#19878,
#19879,#19880,#19881,#19882,#19883,#19884,#19885,#19886,#19887,#19888,#19889,
#19890,#19891,#19892,#19893,#19894,#19895,#19896,#19897,#19898,#19899,#19900,
#19901,#19902,#19903,#19904,#19905,#19906,#19907,#19908,#19909,#19910,#19911,
#19912,#19913,#19914,#19915,#19916,#19917,#19918,#19919,#19920,#19921,#19922,
#19923,#19924,#19925,#19926,#19927,#19928,#19929,#19930,#19931,#19932,#19933,
#19934,#19935,#19936,#19937,#19938));
#21611=AXIS2_PLACEMENT_3D('',#90982,#25885,#25886);
#21612=AXIS2_PLACEMENT_3D('',#90983,#25887,#25888);
#21613=AXIS2_PLACEMENT_3D('',#90997,#25889,#25890);
#21614=AXIS2_PLACEMENT_3D('',#91009,#25891,#25892);
#21615=AXIS2_PLACEMENT_3D('',#91010,#25893,#25894);
#21616=AXIS2_PLACEMENT_3D('',#91012,#25896,#25897);
#21617=AXIS2_PLACEMENT_3D('',#91028,#25898,#25899);
#21618=AXIS2_PLACEMENT_3D('',#91047,#25900,#25901);
#21619=AXIS2_PLACEMENT_3D('',#91048,#25902,#25903);
#21620=AXIS2_PLACEMENT_3D('',#91052,#25906,#25907);
#21621=AXIS2_PLACEMENT_3D('',#91055,#25908,#25909);
#21622=AXIS2_PLACEMENT_3D('',#91075,#25910,#25911);
#21623=AXIS2_PLACEMENT_3D('',#91104,#25912,#25913);
#21624=AXIS2_PLACEMENT_3D('',#91137,#25916,#25917);
#21625=AXIS2_PLACEMENT_3D('',#91139,#25918,#25919);
#21626=AXIS2_PLACEMENT_3D('',#91158,#25920,#25921);
#21627=AXIS2_PLACEMENT_3D('',#91159,#25922,#25923);
#21628=AXIS2_PLACEMENT_3D('',#91161,#25925,#25926);
#21629=AXIS2_PLACEMENT_3D('',#91173,#25927,#25928);
#21630=AXIS2_PLACEMENT_3D('',#91188,#25929,#25930);
#21631=AXIS2_PLACEMENT_3D('',#91197,#25931,#25932);
#21632=AXIS2_PLACEMENT_3D('',#91201,#25935,#25936);
#21633=AXIS2_PLACEMENT_3D('',#91204,#25937,#25938);
#21634=AXIS2_PLACEMENT_3D('',#91208,#25940,#25941);
#21635=AXIS2_PLACEMENT_3D('',#91210,#25943,#25944);
#21636=AXIS2_PLACEMENT_3D('',#91216,#25948,#25949);
#21637=AXIS2_PLACEMENT_3D('',#91218,#25950,#25951);
#21638=AXIS2_PLACEMENT_3D('',#91221,#25953,#25954);
#21639=AXIS2_PLACEMENT_3D('',#91222,#25955,#25956);
#21640=AXIS2_PLACEMENT_3D('',#91226,#25958,#25959);
#21641=AXIS2_PLACEMENT_3D('',#91230,#25961,#25962);
#21642=AXIS2_PLACEMENT_3D('',#91234,#25964,#25965);
#21643=AXIS2_PLACEMENT_3D('',#91238,#25967,#25968);
#21644=AXIS2_PLACEMENT_3D('',#91242,#25970,#25971);
#21645=AXIS2_PLACEMENT_3D('',#91253,#25978,#25979);
#21646=AXIS2_PLACEMENT_3D('',#91266,#25980,#25981);
#21647=AXIS2_PLACEMENT_3D('',#91269,#25983,#25984);
#21648=AXIS2_PLACEMENT_3D('',#91270,#25985,#25986);
#21649=AXIS2_PLACEMENT_3D('',#91273,#25988,#25989);
#21650=AXIS2_PLACEMENT_3D('',#91274,#25990,#25991);
#21651=AXIS2_PLACEMENT_3D('',#91279,#25993,#25994);
#21652=AXIS2_PLACEMENT_3D('',#91288,#25995,#25996);
#21653=AXIS2_PLACEMENT_3D('',#91314,#25999,#26000);
#21654=AXIS2_PLACEMENT_3D('',#91316,#26001,#26002);
#21655=AXIS2_PLACEMENT_3D('',#91320,#26004,#26005);
#21656=AXIS2_PLACEMENT_3D('',#91324,#26007,#26008);
#21657=AXIS2_PLACEMENT_3D('',#91327,#26010,#26011);
#21658=AXIS2_PLACEMENT_3D('',#91328,#26012,#26013);
#21659=AXIS2_PLACEMENT_3D('',#91334,#26017,#26018);
#21660=AXIS2_PLACEMENT_3D('',#91336,#26019,#26020);
#21661=AXIS2_PLACEMENT_3D('',#91340,#26023,#26024);
#21662=AXIS2_PLACEMENT_3D('',#91344,#26026,#26027);
#21663=AXIS2_PLACEMENT_3D('',#91346,#26029,#26030);
#21664=AXIS2_PLACEMENT_3D('',#91354,#26034,#26035);
#21665=AXIS2_PLACEMENT_3D('',#91360,#26038,#26039);
#21666=AXIS2_PLACEMENT_3D('',#91362,#26041,#26042);
#21667=AXIS2_PLACEMENT_3D('',#91373,#26048,#26049);
#21668=AXIS2_PLACEMENT_3D('',#91378,#26051,#26052);
#21669=AXIS2_PLACEMENT_3D('',#91381,#26054,#26055);
#21670=AXIS2_PLACEMENT_3D('',#91382,#26056,#26057);
#21671=AXIS2_PLACEMENT_3D('',#91383,#26058,#26059);
#21672=AXIS2_PLACEMENT_3D('',#91391,#26060,#26061);
#21673=AXIS2_PLACEMENT_3D('',#91392,#26062,#26063);
#21674=AXIS2_PLACEMENT_3D('',#91393,#26064,#26065);
#21675=AXIS2_PLACEMENT_3D('',#91395,#26066,#26067);
#21676=AXIS2_PLACEMENT_3D('',#91398,#26069,#26070);
#21677=AXIS2_PLACEMENT_3D('',#91400,#26071,#26072);
#21678=AXIS2_PLACEMENT_3D('',#91402,#26074,#26075);
#21679=AXIS2_PLACEMENT_3D('',#91405,#26076,#26077);
#21680=AXIS2_PLACEMENT_3D('',#91408,#26080,#26081);
#21681=AXIS2_PLACEMENT_3D('',#91410,#26082,#26083);
#21682=AXIS2_PLACEMENT_3D('',#91414,#26085,#26086);
#21683=AXIS2_PLACEMENT_3D('',#91416,#26088,#26089);
#21684=AXIS2_PLACEMENT_3D('',#91430,#26091,#26092);
#21685=AXIS2_PLACEMENT_3D('',#91432,#26094,#26095);
#21686=AXIS2_PLACEMENT_3D('',#91433,#26096,#26097);
#21687=AXIS2_PLACEMENT_3D('',#91434,#26098,#26099);
#21688=AXIS2_PLACEMENT_3D('',#91435,#26100,#26101);
#21689=AXIS2_PLACEMENT_3D('',#91436,#26102,#26103);
#21690=AXIS2_PLACEMENT_3D('',#91444,#26108,#26109);
#21691=AXIS2_PLACEMENT_3D('',#91447,#26111,#26112);
#21692=AXIS2_PLACEMENT_3D('',#91448,#26113,#26114);
#21693=AXIS2_PLACEMENT_3D('',#91461,#26122,#26123);
#21694=AXIS2_PLACEMENT_3D('',#91464,#26125,#26126);
#21695=AXIS2_PLACEMENT_3D('',#91465,#26127,#26128);
#21696=AXIS2_PLACEMENT_3D('',#91467,#26129,#26130);
#21697=AXIS2_PLACEMENT_3D('',#91473,#26134,#26135);
#21698=AXIS2_PLACEMENT_3D('',#91475,#26136,#26137);
#21699=AXIS2_PLACEMENT_3D('',#91477,#26138,#26139);
#21700=AXIS2_PLACEMENT_3D('',#91478,#26140,#26141);
#21701=AXIS2_PLACEMENT_3D('',#91479,#26142,#26143);
#21702=AXIS2_PLACEMENT_3D('',#91482,#26144,#26145);
#21703=AXIS2_PLACEMENT_3D('',#91494,#26147,#26148);
#21704=AXIS2_PLACEMENT_3D('',#91496,#26150,#26151);
#21705=AXIS2_PLACEMENT_3D('',#91500,#26153,#26154);
#21706=AXIS2_PLACEMENT_3D('',#91504,#26157,#26158);
#21707=AXIS2_PLACEMENT_3D('',#91507,#26159,#26160);
#21708=AXIS2_PLACEMENT_3D('',#91538,#26161,#26162);
#21709=AXIS2_PLACEMENT_3D('',#91567,#26163,#26164);
#21710=AXIS2_PLACEMENT_3D('',#91570,#26167,#26168);
#21711=AXIS2_PLACEMENT_3D('',#91574,#26170,#26171);
#21712=AXIS2_PLACEMENT_3D('',#91586,#26173,#26174);
#21713=AXIS2_PLACEMENT_3D('',#91607,#26177,#26178);
#21714=AXIS2_PLACEMENT_3D('',#91619,#26180,#26181);
#21715=AXIS2_PLACEMENT_3D('',#91621,#26183,#26184);
#21716=AXIS2_PLACEMENT_3D('',#91623,#26185,#26186);
#21717=AXIS2_PLACEMENT_3D('',#91624,#26187,#26188);
#21718=AXIS2_PLACEMENT_3D('',#91626,#26189,#26190);
#21719=AXIS2_PLACEMENT_3D('',#91628,#26191,#26192);
#21720=AXIS2_PLACEMENT_3D('',#91629,#26193,#26194);
#21721=AXIS2_PLACEMENT_3D('',#91630,#26195,#26196);
#21722=AXIS2_PLACEMENT_3D('',#91789,#26198,#26199);
#21723=AXIS2_PLACEMENT_3D('',#91791,#26200,#26201);
#21724=AXIS2_PLACEMENT_3D('',#91812,#26202,#26203);
#21725=AXIS2_PLACEMENT_3D('',#91814,#26205,#26206);
#21726=AXIS2_PLACEMENT_3D('',#91816,#26207,#26208);
#21727=AXIS2_PLACEMENT_3D('',#91818,#26209,#26210);
#21728=AXIS2_PLACEMENT_3D('',#91819,#26211,#26212);
#21729=AXIS2_PLACEMENT_3D('',#91820,#26213,#26214);
#21730=AXIS2_PLACEMENT_3D('',#91821,#26215,#26216);
#21731=AXIS2_PLACEMENT_3D('',#91835,#26218,#26219);
#21732=AXIS2_PLACEMENT_3D('',#91836,#26220,#26221);
#21733=AXIS2_PLACEMENT_3D('',#91839,#26222,#26223);
#21734=AXIS2_PLACEMENT_3D('',#91843,#26225,#26226);
#21735=AXIS2_PLACEMENT_3D('',#91845,#26228,#26229);
#21736=AXIS2_PLACEMENT_3D('',#91847,#26230,#26231);
#21737=AXIS2_PLACEMENT_3D('',#91850,#26233,#26234);
#21738=AXIS2_PLACEMENT_3D('',#91852,#26236,#26237);
#21739=AXIS2_PLACEMENT_3D('',#91853,#26238,#26239);
#21740=AXIS2_PLACEMENT_3D('',#91854,#26240,#26241);
#21741=AXIS2_PLACEMENT_3D('',#91855,#26242,#26243);
#21742=AXIS2_PLACEMENT_3D('',#91856,#26244,#26245);
#21743=AXIS2_PLACEMENT_3D('',#91858,#26247,#26248);
#21744=AXIS2_PLACEMENT_3D('',#91859,#26249,#26250);
#21745=AXIS2_PLACEMENT_3D('',#91860,#26251,#26252);
#21746=AXIS2_PLACEMENT_3D('',#91861,#26253,#26254);
#21747=AXIS2_PLACEMENT_3D('',#91863,#26255,#26256);
#21748=AXIS2_PLACEMENT_3D('',#91883,#26258,#26259);
#21749=AXIS2_PLACEMENT_3D('',#91885,#26260,#26261);
#21750=AXIS2_PLACEMENT_3D('',#91887,#26263,#26264);
#21751=AXIS2_PLACEMENT_3D('',#91889,#26265,#26266);
#21752=AXIS2_PLACEMENT_3D('',#91891,#26268,#26269);
#21753=AXIS2_PLACEMENT_3D('',#91892,#26270,#26271);
#21754=AXIS2_PLACEMENT_3D('',#91893,#26272,#26273);
#21755=AXIS2_PLACEMENT_3D('',#91895,#26274,#26275);
#21756=AXIS2_PLACEMENT_3D('',#91897,#26277,#26278);
#21757=AXIS2_PLACEMENT_3D('',#91899,#26279,#26280);
#21758=AXIS2_PLACEMENT_3D('',#91904,#26283,#26284);
#21759=AXIS2_PLACEMENT_3D('',#91920,#26287,#26288);
#21760=AXIS2_PLACEMENT_3D('',#91925,#26291,#26292);
#21761=AXIS2_PLACEMENT_3D('',#91927,#26294,#26295);
#21762=AXIS2_PLACEMENT_3D('',#91930,#26296,#26297);
#21763=AXIS2_PLACEMENT_3D('',#91978,#26301,#26302);
#21764=AXIS2_PLACEMENT_3D('',#91980,#26303,#26304);
#21765=AXIS2_PLACEMENT_3D('',#91984,#26306,#26307);
#21766=AXIS2_PLACEMENT_3D('',#91988,#26310,#26311);
#21767=AXIS2_PLACEMENT_3D('',#91989,#26312,#26313);
#21768=AXIS2_PLACEMENT_3D('',#91991,#26314,#26315);
#21769=AXIS2_PLACEMENT_3D('',#91994,#26317,#26318);
#21770=AXIS2_PLACEMENT_3D('',#91995,#26319,#26320);
#21771=AXIS2_PLACEMENT_3D('',#91997,#26321,#26322);
#21772=AXIS2_PLACEMENT_3D('',#91999,#26323,#26324);
#21773=AXIS2_PLACEMENT_3D('',#92001,#26326,#26327);
#21774=AXIS2_PLACEMENT_3D('',#92002,#26328,#26329);
#21775=AXIS2_PLACEMENT_3D('',#92003,#26330,#26331);
#21776=AXIS2_PLACEMENT_3D('',#92005,#26332,#26333);
#21777=AXIS2_PLACEMENT_3D('',#92008,#26335,#26336);
#21778=AXIS2_PLACEMENT_3D('',#92010,#26338,#26339);
#21779=AXIS2_PLACEMENT_3D('',#92011,#26340,#26341);
#21780=AXIS2_PLACEMENT_3D('',#92012,#26342,#26343);
#21781=AXIS2_PLACEMENT_3D('',#92014,#26345,#26346);
#21782=AXIS2_PLACEMENT_3D('',#92018,#26348,#26349);
#21783=AXIS2_PLACEMENT_3D('',#92026,#26353,#26354);
#21784=AXIS2_PLACEMENT_3D('',#92028,#26355,#26356);
#21785=AXIS2_PLACEMENT_3D('',#92031,#26358,#26359);
#21786=AXIS2_PLACEMENT_3D('',#92032,#26360,#26361);
#21787=AXIS2_PLACEMENT_3D('',#92035,#26362,#26363);
#21788=AXIS2_PLACEMENT_3D('',#92037,#26364,#26365);
#21789=AXIS2_PLACEMENT_3D('',#92039,#26366,#26367);
#21790=AXIS2_PLACEMENT_3D('',#92040,#26368,#26369);
#21791=AXIS2_PLACEMENT_3D('',#92042,#26370,#26371);
#21792=AXIS2_PLACEMENT_3D('',#92057,#26372,#26373);
#21793=AXIS2_PLACEMENT_3D('',#92061,#26375,#26376);
#21794=AXIS2_PLACEMENT_3D('',#92065,#26378,#26379);
#21795=AXIS2_PLACEMENT_3D('',#92067,#26381,#26382);
#21796=AXIS2_PLACEMENT_3D('',#92069,#26383,#26384);
#21797=AXIS2_PLACEMENT_3D('',#92071,#26386,#26387);
#21798=AXIS2_PLACEMENT_3D('',#92073,#26388,#26389);
#21799=AXIS2_PLACEMENT_3D('',#92075,#26390,#26391);
#21800=AXIS2_PLACEMENT_3D('',#92077,#26392,#26393);
#21801=AXIS2_PLACEMENT_3D('',#92078,#26394,#26395);
#21802=AXIS2_PLACEMENT_3D('',#92079,#26396,#26397);
#21803=AXIS2_PLACEMENT_3D('',#92081,#26398,#26399);
#21804=AXIS2_PLACEMENT_3D('',#92083,#26401,#26402);
#21805=AXIS2_PLACEMENT_3D('',#92086,#26405,#26406);
#21806=AXIS2_PLACEMENT_3D('',#92087,#26407,#26408);
#21807=AXIS2_PLACEMENT_3D('',#92088,#26409,#26410);
#21808=AXIS2_PLACEMENT_3D('',#92089,#26411,#26412);
#21809=AXIS2_PLACEMENT_3D('',#92104,#26413,#26414);
#21810=AXIS2_PLACEMENT_3D('',#92106,#26415,#26416);
#21811=AXIS2_PLACEMENT_3D('',#92109,#26418,#26419);
#21812=AXIS2_PLACEMENT_3D('',#92110,#26420,#26421);
#21813=AXIS2_PLACEMENT_3D('',#92114,#26423,#26424);
#21814=AXIS2_PLACEMENT_3D('',#92116,#26426,#26427);
#21815=AXIS2_PLACEMENT_3D('',#92118,#26429,#26430);
#21816=AXIS2_PLACEMENT_3D('',#92120,#26432,#26433);
#21817=AXIS2_PLACEMENT_3D('',#92128,#26438,#26439);
#21818=AXIS2_PLACEMENT_3D('',#92129,#26440,#26441);
#21819=AXIS2_PLACEMENT_3D('',#92131,#26443,#26444);
#21820=AXIS2_PLACEMENT_3D('',#92133,#26446,#26447);
#21821=AXIS2_PLACEMENT_3D('',#92134,#26448,#26449);
#21822=AXIS2_PLACEMENT_3D('',#92135,#26450,#26451);
#21823=AXIS2_PLACEMENT_3D('',#92136,#26452,#26453);
#21824=AXIS2_PLACEMENT_3D('',#92137,#26454,#26455);
#21825=AXIS2_PLACEMENT_3D('',#92139,#26457,#26458);
#21826=AXIS2_PLACEMENT_3D('',#92140,#26459,#26460);
#21827=AXIS2_PLACEMENT_3D('',#92141,#26461,#26462);
#21828=AXIS2_PLACEMENT_3D('',#92142,#26463,#26464);
#21829=AXIS2_PLACEMENT_3D('',#92143,#26465,#26466);
#21830=AXIS2_PLACEMENT_3D('',#92148,#26469,#26470);
#21831=AXIS2_PLACEMENT_3D('',#92149,#26471,#26472);
#21832=AXIS2_PLACEMENT_3D('',#92157,#26476,#26477);
#21833=AXIS2_PLACEMENT_3D('',#92195,#26497,#26498);
#21834=AXIS2_PLACEMENT_3D('',#92202,#26502,#26503);
#21835=AXIS2_PLACEMENT_3D('',#92204,#26504,#26505);
#21836=AXIS2_PLACEMENT_3D('',#92205,#26506,#26507);
#21837=AXIS2_PLACEMENT_3D('',#92207,#26508,#26509);
#21838=AXIS2_PLACEMENT_3D('',#92209,#26511,#26512);
#21839=AXIS2_PLACEMENT_3D('',#92211,#26514,#26515);
#21840=AXIS2_PLACEMENT_3D('',#92214,#26516,#26517);
#21841=AXIS2_PLACEMENT_3D('',#92215,#26518,#26519);
#21842=AXIS2_PLACEMENT_3D('',#92217,#26520,#26521);
#21843=AXIS2_PLACEMENT_3D('',#92232,#26522,#26523);
#21844=AXIS2_PLACEMENT_3D('',#92234,#26524,#26525);
#21845=AXIS2_PLACEMENT_3D('',#92237,#26528,#26529);
#21846=AXIS2_PLACEMENT_3D('',#92243,#26533,#26534);
#21847=AXIS2_PLACEMENT_3D('',#92245,#26535,#26536);
#21848=AXIS2_PLACEMENT_3D('',#92247,#26538,#26539);
#21849=AXIS2_PLACEMENT_3D('',#92251,#26542,#26543);
#21850=AXIS2_PLACEMENT_3D('',#92253,#26544,#26545);
#21851=AXIS2_PLACEMENT_3D('',#92255,#26547,#26548);
#21852=AXIS2_PLACEMENT_3D('',#92259,#26551,#26552);
#21853=AXIS2_PLACEMENT_3D('',#92262,#26554,#26555);
#21854=AXIS2_PLACEMENT_3D('',#92263,#26556,#26557);
#21855=AXIS2_PLACEMENT_3D('',#92264,#26558,#26559);
#21856=AXIS2_PLACEMENT_3D('',#92266,#26561,#26562);
#21857=AXIS2_PLACEMENT_3D('',#92267,#26563,#26564);
#21858=AXIS2_PLACEMENT_3D('',#92268,#26565,#26566);
#21859=AXIS2_PLACEMENT_3D('',#92269,#26567,#26568);
#21860=AXIS2_PLACEMENT_3D('',#92271,#26570,#26571);
#21861=AXIS2_PLACEMENT_3D('',#92272,#26572,#26573);
#21862=AXIS2_PLACEMENT_3D('',#92273,#26574,#26575);
#21863=AXIS2_PLACEMENT_3D('',#92274,#26576,#26577);
#21864=AXIS2_PLACEMENT_3D('',#92275,#26578,#26579);
#21865=AXIS2_PLACEMENT_3D('',#92276,#26580,#26581);
#21866=AXIS2_PLACEMENT_3D('',#92277,#26582,#26583);
#21867=AXIS2_PLACEMENT_3D('',#92278,#26584,#26585);
#21868=AXIS2_PLACEMENT_3D('',#92281,#26587,#26588);
#21869=AXIS2_PLACEMENT_3D('',#92282,#26589,#26590);
#21870=AXIS2_PLACEMENT_3D('',#92294,#26597,#26598);
#21871=AXIS2_PLACEMENT_3D('',#92296,#26599,#26600);
#21872=AXIS2_PLACEMENT_3D('',#92298,#26602,#26603);
#21873=AXIS2_PLACEMENT_3D('',#92300,#26604,#26605);
#21874=AXIS2_PLACEMENT_3D('',#92302,#26606,#26607);
#21875=AXIS2_PLACEMENT_3D('',#92303,#26608,#26609);
#21876=AXIS2_PLACEMENT_3D('',#92304,#26610,#26611);
#21877=AXIS2_PLACEMENT_3D('',#92307,#26612,#26613);
#21878=AXIS2_PLACEMENT_3D('',#92308,#26614,#26615);
#21879=AXIS2_PLACEMENT_3D('',#92310,#26617,#26618);
#21880=AXIS2_PLACEMENT_3D('',#92313,#26619,#26620);
#21881=AXIS2_PLACEMENT_3D('',#92324,#26626,#26627);
#21882=AXIS2_PLACEMENT_3D('',#92325,#26628,#26629);
#21883=AXIS2_PLACEMENT_3D('',#92327,#26630,#26631);
#21884=AXIS2_PLACEMENT_3D('',#92328,#26632,#26633);
#21885=AXIS2_PLACEMENT_3D('',#92343,#26634,#26635);
#21886=AXIS2_PLACEMENT_3D('',#92344,#26636,#26637);
#21887=AXIS2_PLACEMENT_3D('',#92345,#26638,#26639);
#21888=AXIS2_PLACEMENT_3D('',#92346,#26640,#26641);
#21889=AXIS2_PLACEMENT_3D('',#92349,#26642,#26643);
#21890=AXIS2_PLACEMENT_3D('',#92350,#26644,#26645);
#21891=AXIS2_PLACEMENT_3D('',#92352,#26647,#26648);
#21892=AXIS2_PLACEMENT_3D('',#92355,#26650,#26651);
#21893=AXIS2_PLACEMENT_3D('',#92356,#26652,#26653);
#21894=AXIS2_PLACEMENT_3D('',#92358,#26655,#26656);
#21895=AXIS2_PLACEMENT_3D('',#92359,#26657,#26658);
#21896=AXIS2_PLACEMENT_3D('',#92360,#26659,#26660);
#21897=AXIS2_PLACEMENT_3D('',#92361,#26661,#26662);
#21898=AXIS2_PLACEMENT_3D('',#92363,#26663,#26664);
#21899=AXIS2_PLACEMENT_3D('',#92365,#26666,#26667);
#21900=AXIS2_PLACEMENT_3D('',#92367,#26669,#26670);
#21901=AXIS2_PLACEMENT_3D('',#92369,#26671,#26672);
#21902=AXIS2_PLACEMENT_3D('',#92371,#26673,#26674);
#21903=AXIS2_PLACEMENT_3D('',#92373,#26676,#26677);
#21904=AXIS2_PLACEMENT_3D('',#92377,#26681,#26682);
#21905=AXIS2_PLACEMENT_3D('',#92379,#26683,#26684);
#21906=AXIS2_PLACEMENT_3D('',#92381,#26686,#26687);
#21907=AXIS2_PLACEMENT_3D('',#92387,#26691,#26692);
#21908=AXIS2_PLACEMENT_3D('',#92389,#26693,#26694);
#21909=AXIS2_PLACEMENT_3D('',#92391,#26696,#26697);
#21910=AXIS2_PLACEMENT_3D('',#92395,#26700,#26701);
#21911=AXIS2_PLACEMENT_3D('',#92397,#26702,#26703);
#21912=AXIS2_PLACEMENT_3D('',#92400,#26705,#26706);
#21913=AXIS2_PLACEMENT_3D('',#92401,#26707,#26708);
#21914=AXIS2_PLACEMENT_3D('',#92407,#26711,#26712);
#21915=AXIS2_PLACEMENT_3D('',#92411,#26715,#26716);
#21916=AXIS2_PLACEMENT_3D('',#92413,#26717,#26718);
#21917=AXIS2_PLACEMENT_3D('',#92416,#26720,#26721);
#21918=AXIS2_PLACEMENT_3D('',#92417,#26722,#26723);
#21919=AXIS2_PLACEMENT_3D('',#92423,#26726,#26727);
#21920=AXIS2_PLACEMENT_3D('',#92427,#26730,#26731);
#21921=AXIS2_PLACEMENT_3D('',#92429,#26732,#26733);
#21922=AXIS2_PLACEMENT_3D('',#92432,#26735,#26736);
#21923=AXIS2_PLACEMENT_3D('',#92433,#26737,#26738);
#21924=AXIS2_PLACEMENT_3D('',#92439,#26741,#26742);
#21925=AXIS2_PLACEMENT_3D('',#92443,#26745,#26746);
#21926=AXIS2_PLACEMENT_3D('',#92462,#26747,#26748);
#21927=AXIS2_PLACEMENT_3D('',#92465,#26750,#26751);
#21928=AXIS2_PLACEMENT_3D('',#92466,#26752,#26753);
#21929=AXIS2_PLACEMENT_3D('',#92472,#26756,#26757);
#21930=AXIS2_PLACEMENT_3D('',#92476,#26760,#26761);
#21931=AXIS2_PLACEMENT_3D('',#92478,#26762,#26763);
#21932=AXIS2_PLACEMENT_3D('',#92480,#26764,#26765);
#21933=AXIS2_PLACEMENT_3D('',#92481,#26766,#26767);
#21934=AXIS2_PLACEMENT_3D('',#92482,#26768,#26769);
#21935=AXIS2_PLACEMENT_3D('',#92484,#26771,#26772);
#21936=AXIS2_PLACEMENT_3D('',#92486,#26774,#26775);
#21937=AXIS2_PLACEMENT_3D('',#92488,#26777,#26778);
#21938=AXIS2_PLACEMENT_3D('',#92490,#26780,#26781);
#21939=AXIS2_PLACEMENT_3D('',#92492,#26783,#26784);
#21940=AXIS2_PLACEMENT_3D('',#92494,#26786,#26787);
#21941=AXIS2_PLACEMENT_3D('',#92496,#26789,#26790);
#21942=AXIS2_PLACEMENT_3D('',#92498,#26792,#26793);
#21943=AXIS2_PLACEMENT_3D('',#92500,#26794,#26795);
#21944=AXIS2_PLACEMENT_3D('',#92502,#26796,#26797);
#21945=AXIS2_PLACEMENT_3D('',#92503,#26798,#26799);
#21946=AXIS2_PLACEMENT_3D('',#92504,#26800,#26801);
#21947=AXIS2_PLACEMENT_3D('',#92507,#26803,#26804);
#21948=AXIS2_PLACEMENT_3D('',#92508,#26805,#26806);
#21949=AXIS2_PLACEMENT_3D('',#92510,#26807,#26808);
#21950=AXIS2_PLACEMENT_3D('',#92512,#26809,#26810);
#21951=AXIS2_PLACEMENT_3D('',#92513,#26811,#26812);
#21952=AXIS2_PLACEMENT_3D('',#92514,#26813,#26814);
#21953=AXIS2_PLACEMENT_3D('',#92517,#26816,#26817);
#21954=AXIS2_PLACEMENT_3D('',#92518,#26818,#26819);
#21955=AXIS2_PLACEMENT_3D('',#92521,#26821,#26822);
#21956=AXIS2_PLACEMENT_3D('',#92522,#26823,#26824);
#21957=AXIS2_PLACEMENT_3D('',#92524,#26825,#26826);
#21958=AXIS2_PLACEMENT_3D('',#92525,#26827,#26828);
#21959=AXIS2_PLACEMENT_3D('',#92526,#26829,#26830);
#21960=AXIS2_PLACEMENT_3D('',#92529,#26831,#26832);
#21961=AXIS2_PLACEMENT_3D('',#92530,#26833,#26834);
#21962=AXIS2_PLACEMENT_3D('',#92532,#26835,#26836);
#21963=AXIS2_PLACEMENT_3D('',#92547,#26837,#26838);
#21964=AXIS2_PLACEMENT_3D('',#92550,#26840,#26841);
#21965=AXIS2_PLACEMENT_3D('',#92552,#26843,#26844);
#21966=AXIS2_PLACEMENT_3D('',#92554,#26845,#26846);
#21967=AXIS2_PLACEMENT_3D('',#92555,#26847,#26848);
#21968=AXIS2_PLACEMENT_3D('',#92556,#26849,#26850);
#21969=AXIS2_PLACEMENT_3D('',#92562,#26855,#26856);
#21970=AXIS2_PLACEMENT_3D('',#92563,#26857,#26858);
#21971=AXIS2_PLACEMENT_3D('',#92564,#26859,#26860);
#21972=AXIS2_PLACEMENT_3D('',#92565,#26861,#26862);
#21973=AXIS2_PLACEMENT_3D('',#92566,#26863,#26864);
#21974=AXIS2_PLACEMENT_3D('',#92567,#26865,#26866);
#21975=AXIS2_PLACEMENT_3D('',#92568,#26867,#26868);
#21976=AXIS2_PLACEMENT_3D('',#92569,#26869,#26870);
#21977=AXIS2_PLACEMENT_3D('',#92570,#26871,#26872);
#21978=AXIS2_PLACEMENT_3D('',#92571,#26873,#26874);
#21979=AXIS2_PLACEMENT_3D('',#92572,#26875,#26876);
#21980=AXIS2_PLACEMENT_3D('',#92574,#26877,#26878);
#21981=AXIS2_PLACEMENT_3D('',#92577,#26880,#26881);
#21982=AXIS2_PLACEMENT_3D('',#92578,#26882,#26883);
#21983=AXIS2_PLACEMENT_3D('',#92579,#26884,#26885);
#21984=AXIS2_PLACEMENT_3D('',#92580,#26886,#26887);
#21985=AXIS2_PLACEMENT_3D('',#92581,#26888,#26889);
#21986=AXIS2_PLACEMENT_3D('',#92582,#26890,#26891);
#21987=AXIS2_PLACEMENT_3D('',#92594,#26897,#26898);
#21988=AXIS2_PLACEMENT_3D('',#92602,#26903,#26904);
#21989=AXIS2_PLACEMENT_3D('',#92603,#26905,#26906);
#21990=AXIS2_PLACEMENT_3D('',#92604,#26907,#26908);
#21991=AXIS2_PLACEMENT_3D('',#92607,#26909,#26910);
#21992=AXIS2_PLACEMENT_3D('',#92610,#26913,#26914);
#21993=AXIS2_PLACEMENT_3D('',#92611,#26915,#26916);
#21994=AXIS2_PLACEMENT_3D('',#92614,#26918,#26919);
#21995=AXIS2_PLACEMENT_3D('',#92615,#26920,#26921);
#21996=AXIS2_PLACEMENT_3D('',#92616,#26922,#26923);
#21997=AXIS2_PLACEMENT_3D('',#92618,#26925,#26926);
#21998=AXIS2_PLACEMENT_3D('',#92619,#26927,#26928);
#21999=AXIS2_PLACEMENT_3D('',#92620,#26929,#26930);
#22000=AXIS2_PLACEMENT_3D('',#92621,#26931,#26932);
#22001=AXIS2_PLACEMENT_3D('',#92622,#26933,#26934);
#22002=AXIS2_PLACEMENT_3D('',#92628,#26938,#26939);
#22003=AXIS2_PLACEMENT_3D('',#92629,#26940,#26941);
#22004=AXIS2_PLACEMENT_3D('',#92630,#26942,#26943);
#22005=AXIS2_PLACEMENT_3D('',#92631,#26944,#26945);
#22006=AXIS2_PLACEMENT_3D('',#92632,#26946,#26947);
#22007=AXIS2_PLACEMENT_3D('',#92633,#26948,#26949);
#22008=AXIS2_PLACEMENT_3D('',#92634,#26950,#26951);
#22009=AXIS2_PLACEMENT_3D('',#92635,#26952,#26953);
#22010=AXIS2_PLACEMENT_3D('',#92637,#26954,#26955);
#22011=AXIS2_PLACEMENT_3D('',#92639,#26956,#26957);
#22012=AXIS2_PLACEMENT_3D('',#92641,#26958,#26959);
#22013=AXIS2_PLACEMENT_3D('',#92642,#26960,#26961);
#22014=AXIS2_PLACEMENT_3D('',#92643,#26962,#26963);
#22015=AXIS2_PLACEMENT_3D('',#92654,#26965,#26966);
#22016=AXIS2_PLACEMENT_3D('',#92658,#26968,#26969);
#22017=AXIS2_PLACEMENT_3D('',#92662,#26971,#26972);
#22018=AXIS2_PLACEMENT_3D('',#92716,#26974,#26975);
#22019=AXIS2_PLACEMENT_3D('',#92746,#26978,#26979);
#22020=AXIS2_PLACEMENT_3D('',#92759,#26981,#26982);
#22021=AXIS2_PLACEMENT_3D('',#92761,#26984,#26985);
#22022=AXIS2_PLACEMENT_3D('',#92763,#26986,#26987);
#22023=AXIS2_PLACEMENT_3D('',#92764,#26988,#26989);
#22024=AXIS2_PLACEMENT_3D('',#92765,#26990,#26991);
#22025=AXIS2_PLACEMENT_3D('',#92766,#26992,#26993);
#22026=AXIS2_PLACEMENT_3D('',#92769,#26994,#26995);
#22027=AXIS2_PLACEMENT_3D('',#92773,#26998,#26999);
#22028=AXIS2_PLACEMENT_3D('',#92774,#27000,#27001);
#22029=AXIS2_PLACEMENT_3D('',#92778,#27004,#27005);
#22030=AXIS2_PLACEMENT_3D('',#92781,#27007,#27008);
#22031=AXIS2_PLACEMENT_3D('',#92785,#27011,#27012);
#22032=AXIS2_PLACEMENT_3D('',#92794,#27017,#27018);
#22033=AXIS2_PLACEMENT_3D('',#92797,#27019,#27020);
#22034=AXIS2_PLACEMENT_3D('',#92801,#27022,#27023);
#22035=AXIS2_PLACEMENT_3D('',#92803,#27024,#27025);
#22036=AXIS2_PLACEMENT_3D('',#92806,#27027,#27028);
#22037=AXIS2_PLACEMENT_3D('',#92807,#27029,#27030);
#22038=AXIS2_PLACEMENT_3D('',#92809,#27031,#27032);
#22039=AXIS2_PLACEMENT_3D('',#92812,#27034,#27035);
#22040=AXIS2_PLACEMENT_3D('',#92813,#27036,#27037);
#22041=AXIS2_PLACEMENT_3D('',#92815,#27038,#27039);
#22042=AXIS2_PLACEMENT_3D('',#92817,#27040,#27041);
#22043=AXIS2_PLACEMENT_3D('',#92821,#27043,#27044);
#22044=AXIS2_PLACEMENT_3D('',#92825,#27046,#27047);
#22045=AXIS2_PLACEMENT_3D('',#92827,#27049,#27050);
#22046=AXIS2_PLACEMENT_3D('',#92831,#27053,#27054);
#22047=AXIS2_PLACEMENT_3D('',#92840,#27059,#27060);
#22048=AXIS2_PLACEMENT_3D('',#92846,#27063,#27064);
#22049=AXIS2_PLACEMENT_3D('',#92847,#27065,#27066);
#22050=AXIS2_PLACEMENT_3D('',#92848,#27067,#27068);
#22051=AXIS2_PLACEMENT_3D('',#92851,#27069,#27070);
#22052=AXIS2_PLACEMENT_3D('',#92853,#27071,#27072);
#22053=AXIS2_PLACEMENT_3D('',#92875,#27075,#27076);
#22054=AXIS2_PLACEMENT_3D('',#92877,#27078,#27079);
#22055=AXIS2_PLACEMENT_3D('',#92878,#27080,#27081);
#22056=AXIS2_PLACEMENT_3D('',#92880,#27082,#27083);
#22057=AXIS2_PLACEMENT_3D('',#92884,#27086,#27087);
#22058=AXIS2_PLACEMENT_3D('',#92885,#27088,#27089);
#22059=AXIS2_PLACEMENT_3D('',#92888,#27091,#27092);
#22060=AXIS2_PLACEMENT_3D('',#92890,#27094,#27095);
#22061=AXIS2_PLACEMENT_3D('',#92892,#27097,#27098);
#22062=AXIS2_PLACEMENT_3D('',#92894,#27099,#27100);
#22063=AXIS2_PLACEMENT_3D('',#92901,#27104,#27105);
#22064=AXIS2_PLACEMENT_3D('',#92902,#27106,#27107);
#22065=AXIS2_PLACEMENT_3D('',#92904,#27108,#27109);
#22066=AXIS2_PLACEMENT_3D('',#92906,#27111,#27112);
#22067=AXIS2_PLACEMENT_3D('',#92908,#27113,#27114);
#22068=AXIS2_PLACEMENT_3D('',#92916,#27118,#27119);
#22069=AXIS2_PLACEMENT_3D('',#92917,#27120,#27121);
#22070=AXIS2_PLACEMENT_3D('',#92918,#27122,#27123);
#22071=AXIS2_PLACEMENT_3D('',#92920,#27125,#27126);
#22072=AXIS2_PLACEMENT_3D('',#92921,#27127,#27128);
#22073=AXIS2_PLACEMENT_3D('',#92922,#27129,#27130);
#22074=AXIS2_PLACEMENT_3D('',#92923,#27131,#27132);
#22075=AXIS2_PLACEMENT_3D('',#92924,#27133,#27134);
#22076=AXIS2_PLACEMENT_3D('',#92925,#27135,#27136);
#22077=AXIS2_PLACEMENT_3D('',#92926,#27137,#27138);
#22078=AXIS2_PLACEMENT_3D('',#92927,#27139,#27140);
#22079=AXIS2_PLACEMENT_3D('',#92928,#27141,#27142);
#22080=AXIS2_PLACEMENT_3D('',#92929,#27143,#27144);
#22081=AXIS2_PLACEMENT_3D('',#92930,#27145,#27146);
#22082=AXIS2_PLACEMENT_3D('',#92931,#27147,#27148);
#22083=AXIS2_PLACEMENT_3D('',#92956,#27150,#27151);
#22084=AXIS2_PLACEMENT_3D('',#92958,#27153,#27154);
#22085=AXIS2_PLACEMENT_3D('',#92959,#27155,#27156);
#22086=AXIS2_PLACEMENT_3D('',#92960,#27157,#27158);
#22087=AXIS2_PLACEMENT_3D('',#92961,#27159,#27160);
#22088=AXIS2_PLACEMENT_3D('',#92974,#27161,#27162);
#22089=AXIS2_PLACEMENT_3D('',#92985,#27163,#27164);
#22090=AXIS2_PLACEMENT_3D('',#92990,#27168,#27169);
#22091=AXIS2_PLACEMENT_3D('',#92992,#27171,#27172);
#22092=AXIS2_PLACEMENT_3D('',#92993,#27173,#27174);
#22093=AXIS2_PLACEMENT_3D('',#93003,#27175,#27176);
#22094=AXIS2_PLACEMENT_3D('',#93004,#27177,#27178);
#22095=AXIS2_PLACEMENT_3D('',#93006,#27180,#27181);
#22096=AXIS2_PLACEMENT_3D('',#93008,#27182,#27183);
#22097=AXIS2_PLACEMENT_3D('',#93025,#27187,#27188);
#22098=AXIS2_PLACEMENT_3D('',#93027,#27190,#27191);
#22099=AXIS2_PLACEMENT_3D('',#93033,#27195,#27196);
#22100=AXIS2_PLACEMENT_3D('',#93035,#27198,#27199);
#22101=AXIS2_PLACEMENT_3D('',#93037,#27201,#27202);
#22102=AXIS2_PLACEMENT_3D('',#93039,#27204,#27205);
#22103=AXIS2_PLACEMENT_3D('',#93045,#27209,#27210);
#22104=AXIS2_PLACEMENT_3D('',#93047,#27212,#27213);
#22105=AXIS2_PLACEMENT_3D('',#93049,#27214,#27215);
#22106=AXIS2_PLACEMENT_3D('',#93051,#27216,#27217);
#22107=AXIS2_PLACEMENT_3D('',#93052,#27218,#27219);
#22108=AXIS2_PLACEMENT_3D('',#93053,#27220,#27221);
#22109=AXIS2_PLACEMENT_3D('',#93057,#27223,#27224);
#22110=AXIS2_PLACEMENT_3D('',#93102,#27226,#27227);
#22111=AXIS2_PLACEMENT_3D('',#93103,#27228,#27229);
#22112=AXIS2_PLACEMENT_3D('',#93114,#27231,#27232);
#22113=AXIS2_PLACEMENT_3D('',#93116,#27233,#27234);
#22114=AXIS2_PLACEMENT_3D('',#93127,#27235,#27236);
#22115=AXIS2_PLACEMENT_3D('',#93129,#27238,#27239);
#22116=AXIS2_PLACEMENT_3D('',#93130,#27240,#27241);
#22117=AXIS2_PLACEMENT_3D('',#93132,#27243,#27244);
#22118=AXIS2_PLACEMENT_3D('',#93133,#27245,#27246);
#22119=AXIS2_PLACEMENT_3D('',#93137,#27249,#27250);
#22120=AXIS2_PLACEMENT_3D('',#93139,#27252,#27253);
#22121=AXIS2_PLACEMENT_3D('',#93140,#27254,#27255);
#22122=AXIS2_PLACEMENT_3D('',#93142,#27257,#27258);
#22123=AXIS2_PLACEMENT_3D('',#93143,#27259,#27260);
#22124=AXIS2_PLACEMENT_3D('',#93147,#27263,#27264);
#22125=AXIS2_PLACEMENT_3D('',#93149,#27266,#27267);
#22126=AXIS2_PLACEMENT_3D('',#93150,#27268,#27269);
#22127=AXIS2_PLACEMENT_3D('',#93152,#27271,#27272);
#22128=AXIS2_PLACEMENT_3D('',#93153,#27273,#27274);
#22129=AXIS2_PLACEMENT_3D('',#93157,#27277,#27278);
#22130=AXIS2_PLACEMENT_3D('',#93159,#27280,#27281);
#22131=AXIS2_PLACEMENT_3D('',#93160,#27282,#27283);
#22132=AXIS2_PLACEMENT_3D('',#93164,#27286,#27287);
#22133=AXIS2_PLACEMENT_3D('',#93166,#27289,#27290);
#22134=AXIS2_PLACEMENT_3D('',#93168,#27292,#27293);
#22135=AXIS2_PLACEMENT_3D('',#93169,#27294,#27295);
#22136=AXIS2_PLACEMENT_3D('',#93170,#27296,#27297);
#22137=AXIS2_PLACEMENT_3D('',#93171,#27298,#27299);
#22138=AXIS2_PLACEMENT_3D('',#93172,#27300,#27301);
#22139=AXIS2_PLACEMENT_3D('',#93173,#27302,#27303);
#22140=AXIS2_PLACEMENT_3D('',#93174,#27304,#27305);
#22141=AXIS2_PLACEMENT_3D('',#93177,#27308,#27309);
#22142=AXIS2_PLACEMENT_3D('',#93180,#27312,#27313);
#22143=AXIS2_PLACEMENT_3D('',#93181,#27314,#27315);
#22144=AXIS2_PLACEMENT_3D('',#93182,#27316,#27317);
#22145=AXIS2_PLACEMENT_3D('',#93183,#27318,#27319);
#22146=AXIS2_PLACEMENT_3D('',#93184,#27320,#27321);
#22147=AXIS2_PLACEMENT_3D('',#93185,#27322,#27323);
#22148=AXIS2_PLACEMENT_3D('',#93186,#27324,#27325);
#22149=AXIS2_PLACEMENT_3D('',#93187,#27326,#27327);
#22150=AXIS2_PLACEMENT_3D('',#93188,#27328,#27329);
#22151=AXIS2_PLACEMENT_3D('',#93189,#27330,#27331);
#25885=DIRECTION('axis',(0.,0.,1.));
#25886=DIRECTION('refdir',(1.,0.,0.));
#25887=DIRECTION('center_axis',(0.,0.,1.));
#25888=DIRECTION('ref_axis',(1.,0.,0.));
#25889=DIRECTION('center_axis',(0.,0.,-1.));
#25890=DIRECTION('ref_axis',(6.12323399573677E-17,1.,0.));
#25891=DIRECTION('center_axis',(0.,0.,1.));
#25892=DIRECTION('ref_axis',(6.12323399573677E-17,1.,0.));
#25893=DIRECTION('center_axis',(0.,0.,1.));
#25894=DIRECTION('ref_axis',(1.,0.,0.));
#25895=DIRECTION('',(1.,0.,0.));
#25896=DIRECTION('center_axis',(0.,0.,1.));
#25897=DIRECTION('ref_axis',(1.,0.,0.));
#25898=DIRECTION('center_axis',(0.,0.,-1.));
#25899=DIRECTION('ref_axis',(0.936506715470107,0.350649642634058,0.));
#25900=DIRECTION('center_axis',(0.,0.,1.));
#25901=DIRECTION('ref_axis',(0.936506715470107,0.350649642634058,0.));
#25902=DIRECTION('center_axis',(0.,0.,1.));
#25903=DIRECTION('ref_axis',(1.,0.,0.));
#25904=DIRECTION('',(-1.,0.,0.));
#25905=DIRECTION('',(0.,1.,0.));
#25906=DIRECTION('center_axis',(0.,0.,1.));
#25907=DIRECTION('ref_axis',(1.,0.,0.));
#25908=DIRECTION('center_axis',(0.,0.,1.));
#25909=DIRECTION('ref_axis',(0.670584301865815,-0.741833333095203,0.));
#25910=DIRECTION('center_axis',(0.,0.,-1.));
#25911=DIRECTION('ref_axis',(0.670584301865815,-0.741833333095203,0.));
#25912=DIRECTION('center_axis',(-1.,0.,0.));
#25913=DIRECTION('ref_axis',(0.,-0.707106781186547,-0.707106781186547));
#25914=DIRECTION('',(1.,0.,0.));
#25915=DIRECTION('',(-1.,0.,0.));
#25916=DIRECTION('center_axis',(0.,0.,1.));
#25917=DIRECTION('ref_axis',(1.,0.,0.));
#25918=DIRECTION('center_axis',(0.,0.,-1.));
#25919=DIRECTION('ref_axis',(-0.670584301865815,-0.741833333095203,0.));
#25920=DIRECTION('center_axis',(0.,0.,1.));
#25921=DIRECTION('ref_axis',(-0.670584301865815,-0.741833333095203,0.));
#25922=DIRECTION('center_axis',(0.,0.,1.));
#25923=DIRECTION('ref_axis',(1.,0.,0.));
#25924=DIRECTION('',(1.,0.,0.));
#25925=DIRECTION('center_axis',(0.,0.,1.));
#25926=DIRECTION('ref_axis',(1.,0.,0.));
#25927=DIRECTION('center_axis',(0.,0.,-1.));
#25928=DIRECTION('ref_axis',(-0.936506715470107,0.350649642634058,0.));
#25929=DIRECTION('center_axis',(0.,0.,1.));
#25930=DIRECTION('ref_axis',(-0.936506715470107,0.350649642634058,0.));
#25931=DIRECTION('center_axis',(0.,0.,1.));
#25932=DIRECTION('ref_axis',(1.,0.,0.));
#25933=DIRECTION('',(0.,1.,0.));
#25934=DIRECTION('',(-1.,0.,0.));
#25935=DIRECTION('center_axis',(-1.,0.,0.));
#25936=DIRECTION('ref_axis',(0.,0.707106781186547,-0.707106781186547));
#25937=DIRECTION('center_axis',(1.,0.,0.));
#25938=DIRECTION('ref_axis',(0.,0.707106781186547,-0.707106781186547));
#25939=DIRECTION('',(-1.,0.,0.));
#25940=DIRECTION('center_axis',(-1.,0.,0.));
#25941=DIRECTION('ref_axis',(0.,0.707106781186547,-0.707106781186547));
#25942=DIRECTION('',(1.,0.,0.));
#25943=DIRECTION('center_axis',(0.,0.,-1.));
#25944=DIRECTION('ref_axis',(-1.,0.,0.));
#25945=DIRECTION('',(0.,1.,0.));
#25946=DIRECTION('',(1.,0.,0.));
#25947=DIRECTION('',(0.,-1.,0.));
#25948=DIRECTION('center_axis',(1.,0.,0.));
#25949=DIRECTION('ref_axis',(0.,-0.707106781186547,-0.707106781186547));
#25950=DIRECTION('center_axis',(0.707106781186549,0.,-0.707106781186546));
#25951=DIRECTION('ref_axis',(-0.707106781186546,0.,-0.707106781186549));
#25952=DIRECTION('',(-1.,0.,0.));
#25953=DIRECTION('center_axis',(-1.,0.,0.));
#25954=DIRECTION('ref_axis',(0.,-0.707106781186547,-0.707106781186547));
#25955=DIRECTION('center_axis',(0.,1.,0.));
#25956=DIRECTION('ref_axis',(1.,0.,0.));
#25957=DIRECTION('',(0.,0.,1.));
#25958=DIRECTION('center_axis',(0.,1.,0.));
#25959=DIRECTION('ref_axis',(0.707106781186547,0.,0.707106781186547));
#25960=DIRECTION('',(0.,0.,-1.));
#25961=DIRECTION('center_axis',(0.,1.,0.));
#25962=DIRECTION('ref_axis',(0.707106781186547,0.,-0.707106781186547));
#25963=DIRECTION('',(0.,0.,1.));
#25964=DIRECTION('center_axis',(0.,1.,0.));
#25965=DIRECTION('ref_axis',(-1.86143556795118E-16,0.,-1.));
#25966=DIRECTION('',(0.,0.,-1.));
#25967=DIRECTION('center_axis',(0.,1.,0.));
#25968=DIRECTION('ref_axis',(-0.707106781186547,0.,-0.707106781186547));
#25969=DIRECTION('',(0.,0.,1.));
#25970=DIRECTION('center_axis',(0.,1.,0.));
#25971=DIRECTION('ref_axis',(-0.707106781186547,0.,0.707106781186547));
#25972=DIRECTION('',(0.,0.,-1.));
#25973=DIRECTION('',(-1.,0.,0.));
#25974=DIRECTION('',(0.,0.,1.));
#25975=DIRECTION('',(1.,0.,0.));
#25976=DIRECTION('',(1.,0.,0.));
#25977=DIRECTION('',(0.,0.,1.));
#25978=DIRECTION('center_axis',(0.,0.,-1.));
#25979=DIRECTION('ref_axis',(0.707106781186547,-0.707106781186547,0.));
#25980=DIRECTION('center_axis',(0.,0.,-1.));
#25981=DIRECTION('ref_axis',(0.707106781186547,-0.707106781186547,0.));
#25982=DIRECTION('',(0.,0.,1.));
#25983=DIRECTION('center_axis',(-0.707106781186548,0.,-0.707106781186548));
#25984=DIRECTION('ref_axis',(-0.707106781186548,0.,0.707106781186548));
#25985=DIRECTION('center_axis',(1.,0.,0.));
#25986=DIRECTION('ref_axis',(0.,-0.707106781186547,-0.707106781186547));
#25987=DIRECTION('',(1.,0.,0.));
#25988=DIRECTION('center_axis',(1.,0.,0.));
#25989=DIRECTION('ref_axis',(0.,-0.707106781186547,-0.707106781186547));
#25990=DIRECTION('center_axis',(0.,0.568073288796263,-0.82297796966638));
#25991=DIRECTION('ref_axis',(0.70710678118655,-0.581933303118232,-0.40168847471878));
#25992=DIRECTION('',(0.,-0.568073288796263,0.82297796966638));
#25993=DIRECTION('center_axis',(0.,-0.464718576777245,-0.885458437419923));
#25994=DIRECTION('ref_axis',(-2.68719408286006E-17,-0.885458437419923,0.464718576777245));
#25995=DIRECTION('center_axis',(0.,-0.954719322541023,-0.297508008575921));
#25996=DIRECTION('ref_axis',(-1.72031375589252E-17,0.297508008575921,-0.954719322541023));
#25997=DIRECTION('',(0.,0.568073288796263,-0.82297796966638));
#25998=DIRECTION('',(0.,0.568073288796263,-0.82297796966638));
#25999=DIRECTION('center_axis',(0.,-0.464718576777247,-0.885458437419922));
#26000=DIRECTION('ref_axis',(-2.68719408286005E-17,-0.885458437419922,0.464718576777247));
#26001=DIRECTION('center_axis',(0.,-0.954719322541023,-0.297508008575921));
#26002=DIRECTION('ref_axis',(-1.72031375589252E-17,0.297508008575921,-0.954719322541023));
#26003=DIRECTION('',(0.,-0.568073288796263,0.82297796966638));
#26004=DIRECTION('center_axis',(0.,1.,0.));
#26005=DIRECTION('ref_axis',(9.85450070150229E-17,0.,-1.));
#26006=DIRECTION('',(0.,-0.568073288796263,0.82297796966638));
#26007=DIRECTION('center_axis',(0.,-1.,0.));
#26008=DIRECTION('ref_axis',(9.85450070150229E-17,0.,-1.));
#26009=DIRECTION('',(0.,-0.568073288796263,0.822977969666381));
#26010=DIRECTION('center_axis',(0.,0.82297796966638,-0.568073288796263));
#26011=DIRECTION('ref_axis',(1.08133826391977E-16,-0.568073288796263,-0.82297796966638));
#26012=DIRECTION('center_axis',(0.,0.82297796966638,0.568073288796263));
#26013=DIRECTION('ref_axis',(0.,0.568073288796263,-0.82297796966638));
#26014=DIRECTION('',(-1.,0.,0.));
#26015=DIRECTION('',(0.,0.568073288796263,-0.82297796966638));
#26016=DIRECTION('',(-1.,0.,0.));
#26017=DIRECTION('center_axis',(0.,0.82297796966638,0.568073288796263));
#26018=DIRECTION('ref_axis',(0.,0.568073288796263,-0.82297796966638));
#26019=DIRECTION('center_axis',(0.,0.82297796966638,0.568073288796263));
#26020=DIRECTION('ref_axis',(-3.78468392371919E-16,-0.568073288796263,0.82297796966638));
#26021=DIRECTION('',(0.,0.568073288796263,-0.82297796966638));
#26022=DIRECTION('',(-1.,0.,0.));
#26023=DIRECTION('center_axis',(1.,0.,0.));
#26024=DIRECTION('ref_axis',(0.,0.,-1.));
#26025=DIRECTION('',(0.,-0.568073288796263,-0.822977969666381));
#26026=DIRECTION('center_axis',(-1.,0.,0.));
#26027=DIRECTION('ref_axis',(0.,0.,-1.));
#26028=DIRECTION('',(0.,-0.568073288796263,-0.82297796966638));
#26029=DIRECTION('center_axis',(1.,0.,0.));
#26030=DIRECTION('ref_axis',(0.,0.,-1.));
#26031=DIRECTION('',(0.,0.,-1.));
#26032=DIRECTION('',(0.,1.,0.));
#26033=DIRECTION('',(0.,0.568073288796263,0.82297796966638));
#26034=DIRECTION('center_axis',(-1.,0.,0.));
#26035=DIRECTION('ref_axis',(0.,0.,-1.));
#26036=DIRECTION('',(0.,0.568073288796263,0.822977969666381));
#26037=DIRECTION('',(0.,0.,-1.));
#26038=DIRECTION('center_axis',(-1.,0.,0.));
#26039=DIRECTION('ref_axis',(0.,0.,-1.));
#26040=DIRECTION('',(0.,0.,-1.));
#26041=DIRECTION('center_axis',(1.,0.,0.));
#26042=DIRECTION('ref_axis',(0.,0.,-1.));
#26043=DIRECTION('',(0.,-1.,0.));
#26044=DIRECTION('',(0.,0.568073288796263,0.82297796966638));
#26045=DIRECTION('',(0.,0.,1.));
#26046=DIRECTION('',(0.,-1.,0.));
#26047=DIRECTION('',(0.,0.,-1.));
#26048=DIRECTION('center_axis',(0.,0.,1.));
#26049=DIRECTION('ref_axis',(0.707106781186545,-0.70710678118655,0.));
#26050=DIRECTION('',(0.,0.,1.));
#26051=DIRECTION('center_axis',(0.,0.,1.));
#26052=DIRECTION('ref_axis',(0.707106781186544,-0.707106781186551,0.));
#26053=DIRECTION('',(0.,0.,-1.));
#26054=DIRECTION('center_axis',(0.,0.,1.));
#26055=DIRECTION('ref_axis',(0.,-1.,0.));
#26056=DIRECTION('center_axis',(0.,-0.297508008575919,-0.954719322541024));
#26057=DIRECTION('ref_axis',(-5.52058007260196E-17,-0.954719322541023,0.297508008575919));
#26058=DIRECTION('center_axis',(-0.816496580927726,-0.408248290463864,0.408248290463863));
#26059=DIRECTION('ref_axis',(0.577350269189628,-0.577350269189625,0.577350269189625));
#26060=DIRECTION('center_axis',(0.,1.,0.));
#26061=DIRECTION('ref_axis',(0.,0.,1.));
#26062=DIRECTION('center_axis',(-1.,0.,0.));
#26063=DIRECTION('ref_axis',(0.,-1.,-1.85037170770859E-15));
#26064=DIRECTION('center_axis',(0.,1.,0.));
#26065=DIRECTION('ref_axis',(0.707106781186545,0.,0.70710678118655));
#26066=DIRECTION('center_axis',(0.,-0.885458437419923,0.464718576777245));
#26067=DIRECTION('ref_axis',(-2.04803405119211E-16,0.464718576777245,0.885458437419923));
#26068=DIRECTION('',(0.,1.,0.));
#26069=DIRECTION('center_axis',(0.,0.885458437419921,0.464718576777249));
#26070=DIRECTION('ref_axis',(-2.0480340511921E-16,-0.464718576777249,0.885458437419921));
#26071=DIRECTION('center_axis',(0.,1.,0.));
#26072=DIRECTION('ref_axis',(0.,0.,1.));
#26073=DIRECTION('',(0.,-1.,0.));
#26074=DIRECTION('center_axis',(0.,1.,0.));
#26075=DIRECTION('ref_axis',(-0.707106781186547,0.,0.707106781186547));
#26076=DIRECTION('center_axis',(0.,1.,0.));
#26077=DIRECTION('ref_axis',(-1.,0.,0.));
#26078=DIRECTION('',(0.,1.,0.));
#26079=DIRECTION('',(0.,-1.,0.));
#26080=DIRECTION('center_axis',(0.,0.,-1.));
#26081=DIRECTION('ref_axis',(-0.707106781186547,-0.707106781186547,0.));
#26082=DIRECTION('center_axis',(0.,0.,-1.));
#26083=DIRECTION('ref_axis',(0.,-1.,0.));
#26084=DIRECTION('',(0.,0.,-1.));
#26085=DIRECTION('center_axis',(0.,0.,1.));
#26086=DIRECTION('ref_axis',(-1.,0.,0.));
#26087=DIRECTION('',(0.,0.,1.));
#26088=DIRECTION('center_axis',(0.,1.,0.));
#26089=DIRECTION('ref_axis',(-0.707106781186547,0.,-0.707106781186547));
#26090=DIRECTION('',(0.,-1.,0.));
#26091=DIRECTION('center_axis',(0.,1.,0.));
#26092=DIRECTION('ref_axis',(0.,0.,-1.));
#26093=DIRECTION('',(0.,1.,0.));
#26094=DIRECTION('center_axis',(0.408248290463863,-0.816496580927727,0.408248290463863));
#26095=DIRECTION('ref_axis',(-0.577350269189626,-0.577350269189626,-0.577350269189626));
#26096=DIRECTION('center_axis',(-1.,0.,0.));
#26097=DIRECTION('ref_axis',(0.,-0.707106781186547,-0.707106781186547));
#26098=DIRECTION('center_axis',(0.408248290463863,-0.816496580927727,-0.408248290463863));
#26099=DIRECTION('ref_axis',(-0.577350269189626,-0.577350269189626,0.577350269189626));
#26100=DIRECTION('center_axis',(-1.,0.,0.));
#26101=DIRECTION('ref_axis',(0.,-0.707106781186547,0.707106781186547));
#26102=DIRECTION('center_axis',(0.,0.,1.));
#26103=DIRECTION('ref_axis',(1.,0.,0.));
#26104=DIRECTION('',(-1.,0.,0.));
#26105=DIRECTION('',(0.,1.,0.));
#26106=DIRECTION('',(1.,0.,0.));
#26107=DIRECTION('',(0.,1.,0.));
#26108=DIRECTION('center_axis',(1.,0.,0.));
#26109=DIRECTION('ref_axis',(0.,-0.707106781186547,0.707106781186547));
#26110=DIRECTION('',(1.,0.,0.));
#26111=DIRECTION('center_axis',(0.707106781186548,0.,0.707106781186548));
#26112=DIRECTION('ref_axis',(-0.707106781186548,0.,0.707106781186548));
#26113=DIRECTION('center_axis',(0.,1.,0.));
#26114=DIRECTION('ref_axis',(1.,0.,0.));
#26115=DIRECTION('',(-1.,0.,0.));
#26116=DIRECTION('',(1.,0.,0.));
#26117=DIRECTION('',(0.,0.,1.));
#26118=DIRECTION('',(1.,0.,0.));
#26119=DIRECTION('',(0.,0.,-1.));
#26120=DIRECTION('',(1.,0.,0.));
#26121=DIRECTION('',(0.,0.,1.));
#26122=DIRECTION('center_axis',(1.,0.,0.));
#26123=DIRECTION('ref_axis',(0.,-0.707106781186547,-0.707106781186547));
#26124=DIRECTION('',(1.,0.,0.));
#26125=DIRECTION('center_axis',(-1.,0.,0.));
#26126=DIRECTION('ref_axis',(0.,0.,-1.));
#26127=DIRECTION('center_axis',(0.,0.,-1.));
#26128=DIRECTION('ref_axis',(-1.,0.,0.));
#26129=DIRECTION('center_axis',(0.,0.,1.));
#26130=DIRECTION('ref_axis',(0.707106781186547,-0.707106781186547,0.));
#26131=DIRECTION('',(0.,-1.,0.));
#26132=DIRECTION('',(-1.,0.,0.));
#26133=DIRECTION('',(0.,1.,0.));
#26134=DIRECTION('center_axis',(0.,1.,0.));
#26135=DIRECTION('ref_axis',(1.22464679914735E-16,0.,-1.));
#26136=DIRECTION('center_axis',(0.,0.,-1.));
#26137=DIRECTION('ref_axis',(1.,0.,0.));
#26138=DIRECTION('center_axis',(3.70074341541718E-15,0.,-1.));
#26139=DIRECTION('ref_axis',(0.,-1.,0.));
#26140=DIRECTION('center_axis',(0.,-1.,0.));
#26141=DIRECTION('ref_axis',(-1.86143556795118E-16,0.,-1.));
#26142=DIRECTION('center_axis',(0.,0.,1.));
#26143=DIRECTION('ref_axis',(-0.707106781186547,-0.707106781186547,0.));
#26144=DIRECTION('center_axis',(0.,0.,1.));
#26145=DIRECTION('ref_axis',(-0.707106781186547,-0.707106781186547,0.));
#26146=DIRECTION('',(0.,0.,-1.));
#26147=DIRECTION('center_axis',(0.,0.,-1.));
#26148=DIRECTION('ref_axis',(0.707106781186547,-0.707106781186547,0.));
#26149=DIRECTION('',(0.,0.,1.));
#26150=DIRECTION('center_axis',(-1.,0.,0.));
#26151=DIRECTION('ref_axis',(0.,0.,1.));
#26152=DIRECTION('',(0.,1.,0.));
#26153=DIRECTION('center_axis',(1.,0.,0.));
#26154=DIRECTION('ref_axis',(0.,0.707106781186545,-0.70710678118655));
#26155=DIRECTION('',(0.,0.,1.));
#26156=DIRECTION('',(0.,1.,0.));
#26157=DIRECTION('center_axis',(0.,0.,1.));
#26158=DIRECTION('ref_axis',(-1.83697019872103E-16,1.,0.));
#26159=DIRECTION('center_axis',(0.,0.,-1.));
#26160=DIRECTION('ref_axis',(-1.83697019872103E-16,1.,0.));
#26161=DIRECTION('center_axis',(0.,0.,1.));
#26162=DIRECTION('ref_axis',(-1.83697019872103E-16,1.,0.));
#26163=DIRECTION('center_axis',(1.,0.,0.));
#26164=DIRECTION('ref_axis',(0.,-0.707106781186547,0.707106781186547));
#26165=DIRECTION('',(1.,0.,0.));
#26166=DIRECTION('',(-1.,0.,0.));
#26167=DIRECTION('center_axis',(0.,0.,1.));
#26168=DIRECTION('ref_axis',(6.12323399573677E-17,1.,0.));
#26169=DIRECTION('',(0.,0.,1.));
#26170=DIRECTION('center_axis',(0.,0.,-1.));
#26171=DIRECTION('ref_axis',(1.,0.,0.));
#26172=DIRECTION('',(0.,0.,-1.));
#26173=DIRECTION('center_axis',(0.,0.,1.));
#26174=DIRECTION('ref_axis',(1.,0.,0.));
#26175=DIRECTION('',(0.,0.,1.));
#26176=DIRECTION('',(0.,0.,-1.));
#26177=DIRECTION('center_axis',(0.,0.,1.));
#26178=DIRECTION('ref_axis',(1.,0.,0.));
#26179=DIRECTION('',(0.,0.,1.));
#26180=DIRECTION('center_axis',(0.,0.,-1.));
#26181=DIRECTION('ref_axis',(1.,0.,0.));
#26182=DIRECTION('',(0.,0.,-1.));
#26183=DIRECTION('center_axis',(0.,0.,1.));
#26184=DIRECTION('ref_axis',(1.,0.,0.));
#26185=DIRECTION('center_axis',(0.,0.,1.));
#26186=DIRECTION('ref_axis',(1.,0.,0.));
#26187=DIRECTION('center_axis',(0.,0.,-1.));
#26188=DIRECTION('ref_axis',(-1.,0.,0.));
#26189=DIRECTION('center_axis',(0.,-1.,0.));
#26190=DIRECTION('ref_axis',(1.,0.,0.));
#26191=DIRECTION('center_axis',(0.,0.,-1.));
#26192=DIRECTION('ref_axis',(1.,0.,0.));
#26193=DIRECTION('center_axis',(0.,0.,-1.));
#26194=DIRECTION('ref_axis',(1.,0.,0.));
#26195=DIRECTION('center_axis',(0.,0.,1.));
#26196=DIRECTION('ref_axis',(1.,0.,0.));
#26197=DIRECTION('',(0.,0.,1.));
#26198=DIRECTION('center_axis',(0.,1.,0.));
#26199=DIRECTION('ref_axis',(1.,0.,-2.47375896752486E-16));
#26200=DIRECTION('center_axis',(0.,1.,0.));
#26201=DIRECTION('ref_axis',(1.,0.,-2.47375896752486E-16));
#26202=DIRECTION('center_axis',(0.,1.,0.));
#26203=DIRECTION('ref_axis',(1.,0.,-2.47375896752486E-16));
#26204=DIRECTION('',(0.,1.,0.));
#26205=DIRECTION('center_axis',(0.,1.,0.));
#26206=DIRECTION('ref_axis',(-1.,0.,0.));
#26207=DIRECTION('center_axis',(0.,-1.,0.));
#26208=DIRECTION('ref_axis',(-1.,0.,0.));
#26209=DIRECTION('center_axis',(0.,0.,-1.));
#26210=DIRECTION('ref_axis',(1.,0.,0.));
#26211=DIRECTION('center_axis',(0.,1.,0.));
#26212=DIRECTION('ref_axis',(1.,0.,0.));
#26213=DIRECTION('center_axis',(0.,1.,0.));
#26214=DIRECTION('ref_axis',(1.,0.,0.));
#26215=DIRECTION('center_axis',(0.,0.,1.));
#26216=DIRECTION('ref_axis',(-0.707106781186547,-0.707106781186547,0.));
#26217=DIRECTION('',(0.,0.,-1.));
#26218=DIRECTION('center_axis',(0.,0.,-1.));
#26219=DIRECTION('ref_axis',(-0.707106781186547,-0.707106781186547,0.));
#26220=DIRECTION('center_axis',(0.,1.,0.));
#26221=DIRECTION('ref_axis',(-0.70710678118655,0.,0.707106781186545));
#26222=DIRECTION('center_axis',(0.,1.,0.));
#26223=DIRECTION('ref_axis',(-1.,0.,0.));
#26224=DIRECTION('',(0.,1.,0.));
#26225=DIRECTION('center_axis',(0.,-1.,0.));
#26226=DIRECTION('ref_axis',(0.,0.,1.));
#26227=DIRECTION('',(0.,-1.,0.));
#26228=DIRECTION('center_axis',(1.,0.,0.));
#26229=DIRECTION('ref_axis',(0.,0.707106781186545,0.70710678118655));
#26230=DIRECTION('center_axis',(1.,0.,0.));
#26231=DIRECTION('ref_axis',(0.,1.,0.));
#26232=DIRECTION('',(1.,0.,0.));
#26233=DIRECTION('center_axis',(-1.,0.,0.));
#26234=DIRECTION('ref_axis',(0.,0.,1.));
#26235=DIRECTION('',(-1.,0.,0.));
#26236=DIRECTION('center_axis',(-0.816496580927725,-0.408248290463866,-0.408248290463863));
#26237=DIRECTION('ref_axis',(-0.577350269189628,0.577350269189628,0.577350269189622));
#26238=DIRECTION('center_axis',(0.,0.,1.));
#26239=DIRECTION('ref_axis',(-0.707106781186551,0.707106781186544,0.));
#26240=DIRECTION('center_axis',(-0.816496580927725,0.408248290463866,0.408248290463863));
#26241=DIRECTION('ref_axis',(0.577350269189628,0.577350269189628,0.577350269189622));
#26242=DIRECTION('center_axis',(0.,0.,1.));
#26243=DIRECTION('ref_axis',(0.707106781186547,0.707106781186547,0.));
#26244=DIRECTION('center_axis',(-1.,0.,0.));
#26245=DIRECTION('ref_axis',(0.,-0.707106781186549,0.707106781186546));
#26246=DIRECTION('',(-1.,0.,0.));
#26247=DIRECTION('center_axis',(1.,0.,0.));
#26248=DIRECTION('ref_axis',(0.,0.,1.));
#26249=DIRECTION('center_axis',(-0.816496580927726,0.408248290463864,-0.408248290463863));
#26250=DIRECTION('ref_axis',(-0.577350269189628,-0.577350269189625,0.577350269189625));
#26251=DIRECTION('center_axis',(0.,0.,1.));
#26252=DIRECTION('ref_axis',(-0.70710678118655,-0.707106781186545,0.));
#26253=DIRECTION('center_axis',(0.,-0.568073288796263,-0.82297796966638));
#26254=DIRECTION('ref_axis',(0.707106781186551,-0.581933303118231,0.40168847471878));
#26255=DIRECTION('center_axis',(0.,-0.464718576777247,0.885458437419922));
#26256=DIRECTION('ref_axis',(-5.3743881657201E-17,-0.885458437419922,-0.464718576777247));
#26257=DIRECTION('',(0.,-0.568073288796263,-0.82297796966638));
#26258=DIRECTION('center_axis',(0.,1.,0.));
#26259=DIRECTION('ref_axis',(0.70710678118655,0.,-0.707106781186545));
#26260=DIRECTION('center_axis',(0.,-0.464718576777246,-0.885458437419922));
#26261=DIRECTION('ref_axis',(0.,0.885458437419922,-0.464718576777246));
#26262=DIRECTION('',(0.,1.,0.));
#26263=DIRECTION('center_axis',(0.,-0.568073288796263,0.822977969666381));
#26264=DIRECTION('ref_axis',(0.707106781186551,0.581933303118232,0.401688474718779));
#26265=DIRECTION('center_axis',(0.,0.82297796966638,-0.568073288796263));
#26266=DIRECTION('ref_axis',(-8.11003697939828E-16,0.568073288796263,0.82297796966638));
#26267=DIRECTION('',(0.,-0.568073288796263,0.822977969666381));
#26268=DIRECTION('center_axis',(0.,0.,1.));
#26269=DIRECTION('ref_axis',(1.,0.,0.));
#26270=DIRECTION('center_axis',(0.,0.,-1.));
#26271=DIRECTION('ref_axis',(0.707106781186547,0.707106781186547,0.));
#26272=DIRECTION('center_axis',(0.,-0.707106781186548,0.707106781186548));
#26273=DIRECTION('ref_axis',(0.,0.707106781186548,0.707106781186548));
#26274=DIRECTION('center_axis',(0.,0.,-1.));
#26275=DIRECTION('ref_axis',(0.707106781186547,0.707106781186547,0.));
#26276=DIRECTION('',(0.,0.,1.));
#26277=DIRECTION('center_axis',(1.,0.,0.));
#26278=DIRECTION('ref_axis',(0.,0.,-1.));
#26279=DIRECTION('center_axis',(1.,0.,0.));
#26280=DIRECTION('ref_axis',(0.,0.,-1.));
#26281=DIRECTION('',(1.,0.,0.));
#26282=DIRECTION('',(-1.,0.,0.));
#26283=DIRECTION('center_axis',(1.,0.,0.));
#26284=DIRECTION('ref_axis',(0.,0.,-1.));
#26285=DIRECTION('',(1.,0.,0.));
#26286=DIRECTION('',(-1.,0.,0.));
#26287=DIRECTION('center_axis',(1.,0.,0.));
#26288=DIRECTION('ref_axis',(0.,0.,-1.));
#26289=DIRECTION('',(1.,0.,0.));
#26290=DIRECTION('',(-1.,0.,0.));
#26291=DIRECTION('center_axis',(1.,0.,0.));
#26292=DIRECTION('ref_axis',(0.,0.,-1.));
#26293=DIRECTION('',(1.,0.,0.));
#26294=DIRECTION('center_axis',(1.41247214930022E-16,0.568073288796262,
0.822977969666381));
#26295=DIRECTION('ref_axis',(0.423270070760653,-0.745620968714058,0.514676420882269));
#26296=DIRECTION('center_axis',(0.,0.,-1.));
#26297=DIRECTION('ref_axis',(-5.71055681676799E-16,-1.,0.));
#26298=DIRECTION('',(0.,0.568073288796263,0.822977969666381));
#26299=DIRECTION('',(0.,-0.568073288796263,-0.822977969666381));
#26300=DIRECTION('',(0.,-0.568073288796263,-0.822977969666381));
#26301=DIRECTION('center_axis',(1.,0.,0.));
#26302=DIRECTION('ref_axis',(0.,0.,-1.));
#26303=DIRECTION('center_axis',(1.,0.,0.));
#26304=DIRECTION('ref_axis',(0.,0.,-1.));
#26305=DIRECTION('',(1.,0.,0.));
#26306=DIRECTION('center_axis',(-1.,0.,0.));
#26307=DIRECTION('ref_axis',(0.,-0.822977969666381,0.568073288796262));
#26308=DIRECTION('',(1.,0.,0.));
#26309=DIRECTION('',(-1.,0.,0.));
#26310=DIRECTION('center_axis',(-1.,0.,0.));
#26311=DIRECTION('ref_axis',(0.,-0.822977969666381,0.568073288796262));
#26312=DIRECTION('center_axis',(-1.,0.,0.));
#26313=DIRECTION('ref_axis',(0.,-0.707106781186549,0.707106781186546));
#26314=DIRECTION('center_axis',(-1.,0.,0.));
#26315=DIRECTION('ref_axis',(0.,-1.,0.));
#26316=DIRECTION('',(-1.,0.,0.));
#26317=DIRECTION('center_axis',(1.,0.,0.));
#26318=DIRECTION('ref_axis',(0.,0.,1.));
#26319=DIRECTION('center_axis',(0.,0.,1.));
#26320=DIRECTION('ref_axis',(0.707106781186547,-0.707106781186547,0.));
#26321=DIRECTION('center_axis',(1.85037170770859E-15,0.,-1.));
#26322=DIRECTION('ref_axis',(1.,0.,1.85037170770859E-15));
#26323=DIRECTION('center_axis',(0.707106781186548,0.,-0.707106781186548));
#26324=DIRECTION('ref_axis',(0.707106781186548,0.,0.707106781186548));
#26325=DIRECTION('',(0.,0.,1.));
#26326=DIRECTION('center_axis',(-0.408248290463863,-0.816496580927727,-0.408248290463863));
#26327=DIRECTION('ref_axis',(0.577350269189626,-0.577350269189626,0.577350269189626));
#26328=DIRECTION('center_axis',(0.,-1.,0.));
#26329=DIRECTION('ref_axis',(0.707106781186547,0.,0.707106781186547));
#26330=DIRECTION('center_axis',(0.,1.,0.));
#26331=DIRECTION('ref_axis',(-0.707106781186547,0.,0.707106781186547));
#26332=DIRECTION('center_axis',(0.,1.,0.));
#26333=DIRECTION('ref_axis',(-1.,0.,0.));
#26334=DIRECTION('',(0.,1.,0.));
#26335=DIRECTION('center_axis',(-0.707106781186548,0.707106781186548,0.));
#26336=DIRECTION('ref_axis',(-0.707106781186548,-0.707106781186548,0.));
#26337=DIRECTION('',(0.,-1.,0.));
#26338=DIRECTION('center_axis',(-0.816496580927726,0.408248290463864,-0.408248290463863));
#26339=DIRECTION('ref_axis',(-0.577350269189626,-0.577350269189626,0.577350269189626));
#26340=DIRECTION('center_axis',(0.,0.,1.));
#26341=DIRECTION('ref_axis',(-0.707106781186547,-0.707106781186547,0.));
#26342=DIRECTION('center_axis',(0.,0.,-1.));
#26343=DIRECTION('ref_axis',(-0.707106781186547,-0.707106781186547,0.));
#26344=DIRECTION('',(0.,0.,-1.));
#26345=DIRECTION('center_axis',(-1.,0.,0.));
#26346=DIRECTION('ref_axis',(0.,0.,1.));
#26347=DIRECTION('',(0.,1.,0.));
#26348=DIRECTION('center_axis',(1.,0.,0.));
#26349=DIRECTION('ref_axis',(0.,0.707106781186547,-0.707106781186547));
#26350=DIRECTION('',(0.,0.,-1.));
#26351=DIRECTION('',(0.,-1.,0.));
#26352=DIRECTION('',(0.,0.,1.));
#26353=DIRECTION('center_axis',(-1.,0.,0.));
#26354=DIRECTION('ref_axis',(0.,0.,-1.));
#26355=DIRECTION('center_axis',(-1.,0.,0.));
#26356=DIRECTION('ref_axis',(0.,0.,-1.));
#26357=DIRECTION('',(0.,0.,1.));
#26358=DIRECTION('center_axis',(-1.,0.,0.));
#26359=DIRECTION('ref_axis',(0.,0.,-1.));
#26360=DIRECTION('center_axis',(-1.,0.,0.));
#26361=DIRECTION('ref_axis',(0.,0.,1.));
#26362=DIRECTION('center_axis',(1.,0.,0.));
#26363=DIRECTION('ref_axis',(0.,0.,-1.));
#26364=DIRECTION('center_axis',(0.,-1.,0.));
#26365=DIRECTION('ref_axis',(0.,0.,-1.));
#26366=DIRECTION('center_axis',(-1.,0.,0.));
#26367=DIRECTION('ref_axis',(0.,0.,-1.));
#26368=DIRECTION('center_axis',(-1.,0.,0.));
#26369=DIRECTION('ref_axis',(0.,0.,-1.));
#26370=DIRECTION('center_axis',(1.,0.,0.));
#26371=DIRECTION('ref_axis',(0.,0.,-1.));
#26372=DIRECTION('center_axis',(0.,0.,-1.));
#26373=DIRECTION('ref_axis',(0.70710678118655,0.707106781186545,0.));
#26374=DIRECTION('',(0.,0.,-1.));
#26375=DIRECTION('center_axis',(-0.707106781186548,0.,0.707106781186548));
#26376=DIRECTION('ref_axis',(0.707106781186548,4.088782444489E-17,0.707106781186548));
#26377=DIRECTION('',(0.,0.,1.));
#26378=DIRECTION('center_axis',(0.,0.,1.));
#26379=DIRECTION('ref_axis',(0.707106781186551,0.707106781186544,0.));
#26380=DIRECTION('',(0.,0.,-1.));
#26381=DIRECTION('center_axis',(1.,0.,0.));
#26382=DIRECTION('ref_axis',(0.,0.,-1.));
#26383=DIRECTION('center_axis',(1.,0.,0.));
#26384=DIRECTION('ref_axis',(0.,0.,-1.));
#26385=DIRECTION('',(1.,0.,0.));
#26386=DIRECTION('center_axis',(-1.,0.,0.));
#26387=DIRECTION('ref_axis',(0.,0.,1.));
#26388=DIRECTION('center_axis',(1.,0.,0.));
#26389=DIRECTION('ref_axis',(0.,0.,-1.));
#26390=DIRECTION('center_axis',(0.,-1.,0.));
#26391=DIRECTION('ref_axis',(0.,0.,-1.));
#26392=DIRECTION('center_axis',(-1.,0.,0.));
#26393=DIRECTION('ref_axis',(0.,0.,-1.));
#26394=DIRECTION('center_axis',(-1.,0.,0.));
#26395=DIRECTION('ref_axis',(0.,0.,-1.));
#26396=DIRECTION('center_axis',(1.,0.,0.));
#26397=DIRECTION('ref_axis',(0.,0.,-1.));
#26398=DIRECTION('center_axis',(1.,0.,0.));
#26399=DIRECTION('ref_axis',(0.,0.,-1.));
#26400=DIRECTION('',(1.,0.,0.));
#26401=DIRECTION('center_axis',(1.,0.,0.));
#26402=DIRECTION('ref_axis',(0.,0.,-1.));
#26403=DIRECTION('',(0.,-1.,0.));
#26404=DIRECTION('',(0.,1.,0.));
#26405=DIRECTION('center_axis',(1.,0.,0.));
#26406=DIRECTION('ref_axis',(0.,0.,-1.));
#26407=DIRECTION('center_axis',(0.,-1.,0.));
#26408=DIRECTION('ref_axis',(0.,0.,1.));
#26409=DIRECTION('center_axis',(1.,0.,0.));
#26410=DIRECTION('ref_axis',(0.,0.,-1.));
#26411=DIRECTION('center_axis',(0.,-1.,0.));
#26412=DIRECTION('ref_axis',(0.,0.,1.));
#26413=DIRECTION('center_axis',(0.,0.,1.));
#26414=DIRECTION('ref_axis',(-0.70710678118655,0.707106781186545,0.));
#26415=DIRECTION('center_axis',(0.,0.,1.));
#26416=DIRECTION('ref_axis',(-0.707106781186551,0.707106781186544,0.));
#26417=DIRECTION('',(0.,0.,-1.));
#26418=DIRECTION('center_axis',(-0.707106781186548,0.,-0.707106781186548));
#26419=DIRECTION('ref_axis',(-0.707106781186548,4.088782444489E-17,0.707106781186548));
#26420=DIRECTION('center_axis',(-1.,0.,0.));
#26421=DIRECTION('ref_axis',(0.,0.707106781186547,-0.707106781186547));
#26422=DIRECTION('',(-1.,0.,0.));
#26423=DIRECTION('center_axis',(-1.,0.,0.));
#26424=DIRECTION('ref_axis',(0.,0.707106781186547,-0.707106781186547));
#26425=DIRECTION('',(1.,0.,0.));
#26426=DIRECTION('center_axis',(0.,0.,-1.));
#26427=DIRECTION('ref_axis',(-1.,0.,0.));
#26428=DIRECTION('',(0.,-1.,0.));
#26429=DIRECTION('center_axis',(-1.,0.,0.));
#26430=DIRECTION('ref_axis',(0.,-0.707106781186547,0.707106781186547));
#26431=DIRECTION('',(-1.,0.,0.));
#26432=DIRECTION('center_axis',(0.,0.,1.));
#26433=DIRECTION('ref_axis',(1.,0.,0.));
#26434=DIRECTION('',(0.,-1.,0.));
#26435=DIRECTION('',(1.,0.,0.));
#26436=DIRECTION('',(0.,1.,0.));
#26437=DIRECTION('',(1.,0.,0.));
#26438=DIRECTION('center_axis',(1.,0.,0.));
#26439=DIRECTION('ref_axis',(0.,0.707106781186547,0.707106781186547));
#26440=DIRECTION('center_axis',(0.707106781186548,0.707106781186548,0.));
#26441=DIRECTION('ref_axis',(-0.707106781186548,0.707106781186548,0.));
#26442=DIRECTION('',(-1.,0.,0.));
#26443=DIRECTION('center_axis',(0.,1.,0.));
#26444=DIRECTION('ref_axis',(0.,0.,1.));
#26445=DIRECTION('',(0.,0.,-1.));
#26446=DIRECTION('center_axis',(0.,1.,0.));
#26447=DIRECTION('ref_axis',(-0.707106781186547,0.,0.707106781186547));
#26448=DIRECTION('center_axis',(0.,-1.,0.));
#26449=DIRECTION('ref_axis',(0.,0.,1.));
#26450=DIRECTION('center_axis',(1.,0.,0.));
#26451=DIRECTION('ref_axis',(0.,0.707106781186545,0.70710678118655));
#26452=DIRECTION('center_axis',(1.,0.,0.));
#26453=DIRECTION('ref_axis',(0.,1.,0.));
#26454=DIRECTION('center_axis',(-1.,3.70074341541718E-15,0.));
#26455=DIRECTION('ref_axis',(0.,0.,1.));
#26456=DIRECTION('',(-1.,0.,0.));
#26457=DIRECTION('center_axis',(-0.816496580927725,-0.408248290463866,-0.408248290463863));
#26458=DIRECTION('ref_axis',(-0.577350269189628,0.577350269189628,0.577350269189622));
#26459=DIRECTION('center_axis',(0.,1.,0.));
#26460=DIRECTION('ref_axis',(0.707106781186547,0.,0.707106781186547));
#26461=DIRECTION('center_axis',(0.,-1.,0.));
#26462=DIRECTION('ref_axis',(1.,0.,0.));
#26463=DIRECTION('center_axis',(-0.816496580927725,0.408248290463866,0.408248290463863));
#26464=DIRECTION('ref_axis',(0.577350269189626,0.577350269189629,0.577350269189623));
#26465=DIRECTION('center_axis',(0.,1.,0.));
#26466=DIRECTION('ref_axis',(1.,0.,0.));
#26467=DIRECTION('',(1.,0.,0.));
#26468=DIRECTION('',(0.,0.,-1.));
#26469=DIRECTION('center_axis',(0.,1.,0.));
#26470=DIRECTION('ref_axis',(-0.708113264397705,0.,-0.706098863321579));
#26471=DIRECTION('center_axis',(0.,1.,0.));
#26472=DIRECTION('ref_axis',(-0.708113264397705,0.,-0.706098863321579));
#26473=DIRECTION('',(1.,0.,0.));
#26474=DIRECTION('',(0.,0.,-1.));
#26475=DIRECTION('',(1.,0.,0.));
#26476=DIRECTION('center_axis',(0.,-1.,0.));
#26477=DIRECTION('ref_axis',(0.70710678118655,0.,0.707106781186545));
#26478=DIRECTION('',(0.,0.,-1.));
#26479=DIRECTION('',(-1.,0.,0.));
#26480=DIRECTION('',(0.,0.,-1.));
#26481=DIRECTION('',(-1.,0.,0.));
#26482=DIRECTION('',(0.,0.,1.));
#26483=DIRECTION('',(-1.,0.,0.));
#26484=DIRECTION('',(0.,0.,-1.));
#26485=DIRECTION('',(1.,0.,0.));
#26486=DIRECTION('',(1.,0.,0.));
#26487=DIRECTION('',(0.,0.,1.));
#26488=DIRECTION('',(-1.,0.,0.));
#26489=DIRECTION('',(-1.,0.,0.));
#26490=DIRECTION('',(0.,0.,-1.));
#26491=DIRECTION('',(0.,0.,1.));
#26492=DIRECTION('',(-1.,0.,0.));
#26493=DIRECTION('',(0.,0.,-1.));
#26494=DIRECTION('',(1.,0.,0.));
#26495=DIRECTION('',(0.,0.,1.));
#26496=DIRECTION('',(-1.,0.,0.));
#26497=DIRECTION('center_axis',(0.,1.,0.));
#26498=DIRECTION('ref_axis',(1.,0.,0.));
#26499=DIRECTION('',(-1.,0.,0.));
#26500=DIRECTION('',(0.,0.,-1.));
#26501=DIRECTION('',(1.,0.,0.));
#26502=DIRECTION('center_axis',(0.,1.,0.));
#26503=DIRECTION('ref_axis',(1.,0.,0.));
#26504=DIRECTION('center_axis',(0.,1.,0.));
#26505=DIRECTION('ref_axis',(1.,0.,0.));
#26506=DIRECTION('center_axis',(1.,0.,0.));
#26507=DIRECTION('ref_axis',(0.,-0.707106781186547,0.707106781186547));
#26508=DIRECTION('center_axis',(0.707106781186548,0.,0.707106781186548));
#26509=DIRECTION('ref_axis',(-0.707106781186548,0.,0.707106781186548));
#26510=DIRECTION('',(-1.,0.,0.));
#26511=DIRECTION('center_axis',(0.,0.,-1.));
#26512=DIRECTION('ref_axis',(-0.70710678118655,-0.707106781186545,0.));
#26513=DIRECTION('',(0.,0.,-1.));
#26514=DIRECTION('center_axis',(1.,0.,0.));
#26515=DIRECTION('ref_axis',(0.,0.,-1.));
#26516=DIRECTION('center_axis',(-1.,0.,0.));
#26517=DIRECTION('ref_axis',(0.,0.,-1.));
#26518=DIRECTION('center_axis',(0.,-1.,0.));
#26519=DIRECTION('ref_axis',(0.,0.,1.));
#26520=DIRECTION('center_axis',(-1.,0.,0.));
#26521=DIRECTION('ref_axis',(0.,0.,-1.));
#26522=DIRECTION('center_axis',(0.,0.,1.));
#26523=DIRECTION('ref_axis',(-0.707106781186553,0.707106781186542,0.));
#26524=DIRECTION('center_axis',(-0.70710678118655,0.,-0.707106781186545));
#26525=DIRECTION('ref_axis',(-0.707106781186545,8.17756488897796E-17,0.70710678118655));
#26526=DIRECTION('',(0.,0.,1.));
#26527=DIRECTION('',(0.,0.,1.));
#26528=DIRECTION('center_axis',(0.,-0.822977969666381,-0.568073288796263));
#26529=DIRECTION('ref_axis',(0.,-0.568073288796263,0.822977969666381));
#26530=DIRECTION('',(-1.,0.,0.));
#26531=DIRECTION('',(0.,-0.568073288796263,0.822977969666381));
#26532=DIRECTION('',(-1.,0.,0.));
#26533=DIRECTION('center_axis',(0.,0.568073288796263,0.822977969666381));
#26534=DIRECTION('ref_axis',(0.707106781186551,0.581933303118231,-0.401688474718779));
#26535=DIRECTION('center_axis',(0.,0.,-1.));
#26536=DIRECTION('ref_axis',(9.51759469461333E-17,1.,0.));
#26537=DIRECTION('',(0.,0.568073288796263,0.822977969666381));
#26538=DIRECTION('center_axis',(0.,-0.822977969666381,0.568073288796263));
#26539=DIRECTION('ref_axis',(0.,0.568073288796263,0.822977969666381));
#26540=DIRECTION('',(-1.,0.,0.));
#26541=DIRECTION('',(0.,0.568073288796263,0.822977969666381));
#26542=DIRECTION('center_axis',(0.,-0.568073288796263,0.822977969666381));
#26543=DIRECTION('ref_axis',(0.707106781186551,0.581933303118231,0.401688474718779));
#26544=DIRECTION('center_axis',(0.,1.,0.));
#26545=DIRECTION('ref_axis',(0.,0.,1.));
#26546=DIRECTION('',(0.,-0.568073288796263,0.822977969666381));
#26547=DIRECTION('center_axis',(0.,-0.822977969666381,-0.568073288796263));
#26548=DIRECTION('ref_axis',(0.,-0.568073288796263,0.822977969666381));
#26549=DIRECTION('',(-1.,0.,0.));
#26550=DIRECTION('',(0.,-0.568073288796263,0.822977969666381));
#26551=DIRECTION('center_axis',(0.,-1.,0.));
#26552=DIRECTION('ref_axis',(0.70710678118655,0.,0.707106781186545));
#26553=DIRECTION('',(0.,-1.,0.));
#26554=DIRECTION('center_axis',(0.,-0.707106781186548,0.707106781186548));
#26555=DIRECTION('ref_axis',(0.,0.707106781186548,0.707106781186548));
#26556=DIRECTION('center_axis',(0.,0.885458437419924,0.464718576777243));
#26557=DIRECTION('ref_axis',(-3.07205107678817E-16,-0.464718576777243,0.885458437419924));
#26558=DIRECTION('center_axis',(0.,0.,-1.));
#26559=DIRECTION('ref_axis',(0.,-1.,0.));
#26560=DIRECTION('',(0.,-1.,0.));
#26561=DIRECTION('center_axis',(-0.408248290463865,0.408248290463858,-0.816496580927728));
#26562=DIRECTION('ref_axis',(0.577350269189634,-0.577350269189621,-0.577350269189622));
#26563=DIRECTION('center_axis',(0.,-1.,0.));
#26564=DIRECTION('ref_axis',(0.707106781186551,0.,-0.707106781186544));
#26565=DIRECTION('center_axis',(0.,0.,1.));
#26566=DIRECTION('ref_axis',(0.70710678118655,0.707106781186545,0.));
#26567=DIRECTION('center_axis',(0.,0.954719322541023,-0.297508008575921));
#26568=DIRECTION('ref_axis',(0.,0.297508008575921,0.954719322541023));
#26569=DIRECTION('',(0.,0.,1.));
#26570=DIRECTION('center_axis',(0.,-0.568073288796263,-0.822977969666381));
#26571=DIRECTION('ref_axis',(0.707106781186551,-0.581933303118231,0.401688474718779));
#26572=DIRECTION('center_axis',(0.,1.,0.));
#26573=DIRECTION('ref_axis',(0.70710678118655,0.,-0.707106781186545));
#26574=DIRECTION('center_axis',(0.,-1.,0.));
#26575=DIRECTION('ref_axis',(0.,0.,-1.));
#26576=DIRECTION('center_axis',(-1.,0.,0.));
#26577=DIRECTION('ref_axis',(0.,0.707106781186545,-0.70710678118655));
#26578=DIRECTION('center_axis',(-1.,0.,0.));
#26579=DIRECTION('ref_axis',(0.,1.,0.));
#26580=DIRECTION('center_axis',(-1.,0.,0.));
#26581=DIRECTION('ref_axis',(0.,0.707106781186545,-0.70710678118655));
#26582=DIRECTION('center_axis',(0.40824829046386,-0.816496580927726,-0.408248290463866));
#26583=DIRECTION('ref_axis',(0.577350269189622,0.577350269189628,-0.577350269189628));
#26584=DIRECTION('center_axis',(-1.,0.,0.));
#26585=DIRECTION('ref_axis',(0.,-0.707106781186547,0.707106781186547));
#26586=DIRECTION('',(-1.,0.,0.));
#26587=DIRECTION('center_axis',(-0.707106781186548,-0.707106781186548,0.));
#26588=DIRECTION('ref_axis',(0.707106781186548,-0.707106781186548,0.));
#26589=DIRECTION('center_axis',(0.,0.,1.));
#26590=DIRECTION('ref_axis',(1.,0.,0.));
#26591=DIRECTION('',(0.,-1.,0.));
#26592=DIRECTION('',(1.,0.,0.));
#26593=DIRECTION('',(0.,-1.,0.));
#26594=DIRECTION('',(1.,0.,0.));
#26595=DIRECTION('',(0.,1.,0.));
#26596=DIRECTION('',(-1.,0.,0.));
#26597=DIRECTION('center_axis',(1.,0.,0.));
#26598=DIRECTION('ref_axis',(0.,0.707106781186547,0.707106781186547));
#26599=DIRECTION('center_axis',(-0.707106781186548,0.707106781186548,0.));
#26600=DIRECTION('ref_axis',(0.707106781186548,0.707106781186548,0.));
#26601=DIRECTION('',(-1.,0.,0.));
#26602=DIRECTION('center_axis',(1.,0.,0.));
#26603=DIRECTION('ref_axis',(0.,0.,-1.));
#26604=DIRECTION('center_axis',(-1.,0.,0.));
#26605=DIRECTION('ref_axis',(0.,0.,-1.));
#26606=DIRECTION('center_axis',(0.,-1.,0.));
#26607=DIRECTION('ref_axis',(0.,0.,1.));
#26608=DIRECTION('center_axis',(1.,0.,0.));
#26609=DIRECTION('ref_axis',(0.,0.,-1.));
#26610=DIRECTION('center_axis',(-1.,0.,0.));
#26611=DIRECTION('ref_axis',(0.,0.,-1.));
#26612=DIRECTION('center_axis',(-1.,0.,0.));
#26613=DIRECTION('ref_axis',(0.,0.,-1.));
#26614=DIRECTION('center_axis',(-1.,0.,0.));
#26615=DIRECTION('ref_axis',(0.,0.,-1.));
#26616=DIRECTION('',(-1.,0.,0.));
#26617=DIRECTION('center_axis',(-1.,0.,0.));
#26618=DIRECTION('ref_axis',(0.,0.,1.));
#26619=DIRECTION('center_axis',(-1.,0.,0.));
#26620=DIRECTION('ref_axis',(0.,0.,-1.));
#26621=DIRECTION('',(0.,0.,1.));
#26622=DIRECTION('',(0.,1.,0.));
#26623=DIRECTION('',(0.,0.,-1.));
#26624=DIRECTION('',(0.,-1.,0.));
#26625=DIRECTION('',(0.,0.,1.));
#26626=DIRECTION('center_axis',(-1.,0.,0.));
#26627=DIRECTION('ref_axis',(0.,0.,-1.));
#26628=DIRECTION('center_axis',(1.,0.,0.));
#26629=DIRECTION('ref_axis',(0.,0.,-1.));
#26630=DIRECTION('center_axis',(0.,-1.,0.));
#26631=DIRECTION('ref_axis',(0.,0.,1.));
#26632=DIRECTION('center_axis',(1.,0.,0.));
#26633=DIRECTION('ref_axis',(0.,0.,-1.));
#26634=DIRECTION('center_axis',(0.,0.,1.));
#26635=DIRECTION('ref_axis',(-0.70710678118655,0.707106781186545,0.));
#26636=DIRECTION('center_axis',(0.,0.,-1.));
#26637=DIRECTION('ref_axis',(-1.,0.,0.));
#26638=DIRECTION('center_axis',(0.707106781186548,0.,0.707106781186548));
#26639=DIRECTION('ref_axis',(-0.707106781186548,4.088782444489E-17,0.707106781186548));
#26640=DIRECTION('center_axis',(-1.,0.,0.));
#26641=DIRECTION('ref_axis',(0.,0.,-1.));
#26642=DIRECTION('center_axis',(-1.,0.,0.));
#26643=DIRECTION('ref_axis',(0.,0.,-1.));
#26644=DIRECTION('center_axis',(-1.,0.,0.));
#26645=DIRECTION('ref_axis',(0.,0.,-1.));
#26646=DIRECTION('',(-1.,0.,0.));
#26647=DIRECTION('center_axis',(-1.,0.,0.));
#26648=DIRECTION('ref_axis',(0.,0.,1.));
#26649=DIRECTION('',(0.,1.,0.));
#26650=DIRECTION('center_axis',(-1.,0.,0.));
#26651=DIRECTION('ref_axis',(0.,0.,-1.));
#26652=DIRECTION('center_axis',(1.,0.,0.));
#26653=DIRECTION('ref_axis',(0.,0.707106781186545,0.70710678118655));
#26654=DIRECTION('',(1.,0.,0.));
#26655=DIRECTION('center_axis',(0.,0.,1.));
#26656=DIRECTION('ref_axis',(1.,0.,0.));
#26657=DIRECTION('center_axis',(1.,0.,0.));
#26658=DIRECTION('ref_axis',(0.,0.707106781186545,0.70710678118655));
#26659=DIRECTION('center_axis',(-0.707106781186548,0.,0.707106781186547));
#26660=DIRECTION('ref_axis',(0.707106781186547,-4.088782444489E-17,0.707106781186548));
#26661=DIRECTION('center_axis',(0.,0.,-1.));
#26662=DIRECTION('ref_axis',(0.70710678118655,0.707106781186545,0.));
#26663=DIRECTION('center_axis',(0.,0.,-1.));
#26664=DIRECTION('ref_axis',(0.70710678118655,0.707106781186545,0.));
#26665=DIRECTION('',(0.,0.,-1.));
#26666=DIRECTION('center_axis',(0.,0.,1.));
#26667=DIRECTION('ref_axis',(1.,0.,0.));
#26668=DIRECTION('',(0.,1.,0.));
#26669=DIRECTION('center_axis',(0.,0.,1.));
#26670=DIRECTION('ref_axis',(-0.70710678118655,0.707106781186545,0.));
#26671=DIRECTION('center_axis',(0.,0.,-1.));
#26672=DIRECTION('ref_axis',(-0.70710678118655,0.707106781186545,0.));
#26673=DIRECTION('center_axis',(-0.707106781186548,0.,-0.707106781186548));
#26674=DIRECTION('ref_axis',(-0.707106781186548,4.088782444489E-17,0.707106781186548));
#26675=DIRECTION('',(0.,0.,1.));
#26676=DIRECTION('center_axis',(-1.,0.,0.));
#26677=DIRECTION('ref_axis',(0.,0.,1.));
#26678=DIRECTION('',(0.,0.,1.));
#26679=DIRECTION('',(0.,1.,0.));
#26680=DIRECTION('',(0.,-1.,0.));
#26681=DIRECTION('center_axis',(1.,0.,0.));
#26682=DIRECTION('ref_axis',(0.,0.707106781186545,0.70710678118655));
#26683=DIRECTION('center_axis',(-0.707106781186548,0.,0.707106781186548));
#26684=DIRECTION('ref_axis',(0.707106781186548,4.088782444489E-17,0.707106781186548));
#26685=DIRECTION('',(1.,0.,0.));
#26686=DIRECTION('center_axis',(0.,0.,1.));
#26687=DIRECTION('ref_axis',(1.,0.,0.));
#26688=DIRECTION('',(0.,-1.,0.));
#26689=DIRECTION('',(-1.,0.,0.));
#26690=DIRECTION('',(0.,-1.,0.));
#26691=DIRECTION('center_axis',(1.,0.,0.));
#26692=DIRECTION('ref_axis',(0.,0.707106781186545,0.70710678118655));
#26693=DIRECTION('center_axis',(-1.,0.,0.));
#26694=DIRECTION('ref_axis',(0.,0.707106781186545,0.70710678118655));
#26695=DIRECTION('',(1.,0.,0.));
#26696=DIRECTION('center_axis',(0.,0.,1.));
#26697=DIRECTION('ref_axis',(1.,0.,0.));
#26698=DIRECTION('',(0.,-1.,0.));
#26699=DIRECTION('',(-1.,0.,0.));
#26700=DIRECTION('center_axis',(-1.,0.,0.));
#26701=DIRECTION('ref_axis',(0.,0.70710678118655,-0.707106781186545));
#26702=DIRECTION('center_axis',(0.707106781186548,0.,-0.707106781186548));
#26703=DIRECTION('ref_axis',(-0.707106781186548,0.,-0.707106781186548));
#26704=DIRECTION('',(-1.,0.,0.));
#26705=DIRECTION('center_axis',(-0.707106781186548,0.,-0.707106781186548));
#26706=DIRECTION('ref_axis',(0.707106781186548,0.,-0.707106781186548));
#26707=DIRECTION('center_axis',(0.,0.,1.));
#26708=DIRECTION('ref_axis',(-1.,0.,0.));
#26709=DIRECTION('',(0.,-1.,0.));
#26710=DIRECTION('',(-1.,0.,0.));
#26711=DIRECTION('center_axis',(0.,0.,1.));
#26712=DIRECTION('ref_axis',(1.,0.,0.));
#26713=DIRECTION('',(-1.,0.,0.));
#26714=DIRECTION('',(0.,-1.,0.));
#26715=DIRECTION('center_axis',(1.,0.,0.));
#26716=DIRECTION('ref_axis',(0.,0.70710678118655,0.707106781186545));
#26717=DIRECTION('center_axis',(-0.707106781186548,0.,0.707106781186548));
#26718=DIRECTION('ref_axis',(0.707106781186548,0.,0.707106781186548));
#26719=DIRECTION('',(1.,0.,0.));
#26720=DIRECTION('center_axis',(0.707106781186548,0.,0.707106781186548));
#26721=DIRECTION('ref_axis',(-0.707106781186548,0.,0.707106781186548));
#26722=DIRECTION('center_axis',(0.,0.,-1.));
#26723=DIRECTION('ref_axis',(1.,0.,0.));
#26724=DIRECTION('',(0.,-1.,0.));
#26725=DIRECTION('',(1.,0.,0.));
#26726=DIRECTION('center_axis',(0.,0.,-1.));
#26727=DIRECTION('ref_axis',(1.,0.,0.));
#26728=DIRECTION('',(1.,0.,0.));
#26729=DIRECTION('',(0.,-1.,0.));
#26730=DIRECTION('center_axis',(-1.,0.,0.));
#26731=DIRECTION('ref_axis',(0.,0.70710678118655,-0.707106781186545));
#26732=DIRECTION('center_axis',(0.707106781186548,0.,-0.707106781186548));
#26733=DIRECTION('ref_axis',(-0.707106781186548,0.,-0.707106781186548));
#26734=DIRECTION('',(-1.,0.,0.));
#26735=DIRECTION('center_axis',(-0.707106781186548,0.,-0.707106781186548));
#26736=DIRECTION('ref_axis',(0.707106781186548,0.,-0.707106781186548));
#26737=DIRECTION('center_axis',(0.,0.,1.));
#26738=DIRECTION('ref_axis',(-1.,0.,0.));
#26739=DIRECTION('',(0.,-1.,0.));
#26740=DIRECTION('',(-1.,0.,0.));
#26741=DIRECTION('center_axis',(0.,0.,1.));
#26742=DIRECTION('ref_axis',(1.,0.,0.));
#26743=DIRECTION('',(-1.,0.,0.));
#26744=DIRECTION('',(0.,-1.,0.));
#26745=DIRECTION('center_axis',(1.,0.,0.));
#26746=DIRECTION('ref_axis',(0.,0.70710678118655,0.707106781186545));
#26747=DIRECTION('center_axis',(-0.707106781186547,0.,0.707106781186548));
#26748=DIRECTION('ref_axis',(0.707106781186548,4.088782444489E-17,0.707106781186547));
#26749=DIRECTION('',(1.,0.,0.));
#26750=DIRECTION('center_axis',(0.707106781186547,0.,0.707106781186548));
#26751=DIRECTION('ref_axis',(-0.707106781186548,4.088782444489E-17,0.707106781186547));
#26752=DIRECTION('center_axis',(0.,0.,-1.));
#26753=DIRECTION('ref_axis',(1.,0.,0.));
#26754=DIRECTION('',(0.,-1.,0.));
#26755=DIRECTION('',(1.,0.,0.));
#26756=DIRECTION('center_axis',(0.,0.,-1.));
#26757=DIRECTION('ref_axis',(1.,0.,0.));
#26758=DIRECTION('',(1.,0.,0.));
#26759=DIRECTION('',(0.,-1.,0.));
#26760=DIRECTION('center_axis',(0.,-1.,0.));
#26761=DIRECTION('ref_axis',(0.,0.,-1.));
#26762=DIRECTION('center_axis',(-1.,0.,-1.22464679914735E-16));
#26763=DIRECTION('ref_axis',(-1.22464679914735E-16,0.,1.));
#26764=DIRECTION('center_axis',(0.,-1.,0.));
#26765=DIRECTION('ref_axis',(1.,0.,0.));
#26766=DIRECTION('center_axis',(0.,-1.,0.));
#26767=DIRECTION('ref_axis',(1.,0.,0.));
#26768=DIRECTION('center_axis',(0.,0.,-1.));
#26769=DIRECTION('ref_axis',(0.707106781186545,0.70710678118655,0.));
#26770=DIRECTION('',(0.,0.,-1.));
#26771=DIRECTION('center_axis',(-1.,0.,0.));
#26772=DIRECTION('ref_axis',(0.,0.,-1.));
#26773=DIRECTION('',(0.,0.,-1.));
#26774=DIRECTION('center_axis',(0.,0.,1.));
#26775=DIRECTION('ref_axis',(-0.707106781186545,0.70710678118655,0.));
#26776=DIRECTION('',(0.,0.,1.));
#26777=DIRECTION('center_axis',(1.,0.,0.));
#26778=DIRECTION('ref_axis',(0.,0.,1.));
#26779=DIRECTION('',(0.,0.,1.));
#26780=DIRECTION('center_axis',(0.,0.,-1.));
#26781=DIRECTION('ref_axis',(0.707106781186545,0.70710678118655,0.));
#26782=DIRECTION('',(0.,0.,-1.));
#26783=DIRECTION('center_axis',(-1.,0.,0.));
#26784=DIRECTION('ref_axis',(0.,0.,-1.));
#26785=DIRECTION('',(0.,0.,-1.));
#26786=DIRECTION('center_axis',(0.,0.,1.));
#26787=DIRECTION('ref_axis',(-0.707106781186545,0.70710678118655,0.));
#26788=DIRECTION('',(0.,0.,1.));
#26789=DIRECTION('center_axis',(1.,0.,0.));
#26790=DIRECTION('ref_axis',(0.,0.,1.));
#26791=DIRECTION('',(0.,0.,1.));
#26792=DIRECTION('center_axis',(0.,-1.,0.));
#26793=DIRECTION('ref_axis',(0.,0.,-1.));
#26794=DIRECTION('center_axis',(-1.,0.,0.));
#26795=DIRECTION('ref_axis',(0.,0.,1.));
#26796=DIRECTION('center_axis',(0.,-1.,0.));
#26797=DIRECTION('ref_axis',(1.,0.,0.));
#26798=DIRECTION('center_axis',(0.,-1.,0.));
#26799=DIRECTION('ref_axis',(1.,0.,0.));
#26800=DIRECTION('center_axis',(0.,-1.,0.));
#26801=DIRECTION('ref_axis',(1.,0.,0.));
#26802=DIRECTION('',(0.,-1.,0.));
#26803=DIRECTION('center_axis',(0.,-1.,0.));
#26804=DIRECTION('ref_axis',(1.,0.,0.));
#26805=DIRECTION('center_axis',(0.,-1.,0.));
#26806=DIRECTION('ref_axis',(0.,0.,-1.));
#26807=DIRECTION('center_axis',(-1.,0.,0.));
#26808=DIRECTION('ref_axis',(0.,0.,1.));
#26809=DIRECTION('center_axis',(0.,-1.,0.));
#26810=DIRECTION('ref_axis',(1.,0.,0.));
#26811=DIRECTION('center_axis',(0.,-1.,0.));
#26812=DIRECTION('ref_axis',(1.,0.,0.));
#26813=DIRECTION('center_axis',(0.,-1.,0.));
#26814=DIRECTION('ref_axis',(1.,0.,0.));
#26815=DIRECTION('',(0.,-1.,0.));
#26816=DIRECTION('center_axis',(0.,-1.,0.));
#26817=DIRECTION('ref_axis',(1.,0.,0.));
#26818=DIRECTION('center_axis',(0.,-1.,0.));
#26819=DIRECTION('ref_axis',(1.,0.,0.));
#26820=DIRECTION('',(0.,-1.,0.));
#26821=DIRECTION('center_axis',(0.,-1.,0.));
#26822=DIRECTION('ref_axis',(1.,0.,0.));
#26823=DIRECTION('center_axis',(0.,1.,0.));
#26824=DIRECTION('ref_axis',(-0.708113264397705,0.,-0.706098863321579));
#26825=DIRECTION('center_axis',(0.,-1.,0.));
#26826=DIRECTION('ref_axis',(1.,0.,0.));
#26827=DIRECTION('center_axis',(0.706098863321579,0.,-0.708113264397705));
#26828=DIRECTION('ref_axis',(0.708113264397705,0.,0.706098863321579));
#26829=DIRECTION('center_axis',(-1.,0.,0.));
#26830=DIRECTION('ref_axis',(0.,0.,1.));
#26831=DIRECTION('center_axis',(1.,0.,0.));
#26832=DIRECTION('ref_axis',(0.,0.,-1.));
#26833=DIRECTION('center_axis',(0.,-1.,0.));
#26834=DIRECTION('ref_axis',(0.,0.,-1.));
#26835=DIRECTION('center_axis',(1.,0.,0.));
#26836=DIRECTION('ref_axis',(0.,0.,-1.));
#26837=DIRECTION('center_axis',(0.,0.,-1.));
#26838=DIRECTION('ref_axis',(0.70710678118655,0.707106781186545,0.));
#26839=DIRECTION('',(0.,0.,-1.));
#26840=DIRECTION('center_axis',(0.,0.,1.));
#26841=DIRECTION('ref_axis',(0.707106781186551,0.707106781186544,0.));
#26842=DIRECTION('',(0.,0.,-1.));
#26843=DIRECTION('center_axis',(-1.,0.,0.));
#26844=DIRECTION('ref_axis',(0.,0.,1.));
#26845=DIRECTION('center_axis',(1.,0.,0.));
#26846=DIRECTION('ref_axis',(0.,0.,-1.));
#26847=DIRECTION('center_axis',(0.,-1.,0.));
#26848=DIRECTION('ref_axis',(0.,0.,-1.));
#26849=DIRECTION('center_axis',(1.,0.,0.));
#26850=DIRECTION('ref_axis',(0.,0.,-1.));
#26851=DIRECTION('',(0.,1.,0.));
#26852=DIRECTION('',(0.,0.,-1.));
#26853=DIRECTION('',(0.,1.,0.));
#26854=DIRECTION('',(0.,0.,1.));
#26855=DIRECTION('center_axis',(1.,0.,0.));
#26856=DIRECTION('ref_axis',(0.,0.707106781186545,0.70710678118655));
#26857=DIRECTION('center_axis',(1.,0.,0.));
#26858=DIRECTION('ref_axis',(0.,1.,0.));
#26859=DIRECTION('center_axis',(-1.,0.,0.));
#26860=DIRECTION('ref_axis',(0.,0.,1.));
#26861=DIRECTION('center_axis',(0.,1.,0.));
#26862=DIRECTION('ref_axis',(0.707106781186547,0.,0.707106781186547));
#26863=DIRECTION('center_axis',(0.,-1.,0.));
#26864=DIRECTION('ref_axis',(1.,0.,0.));
#26865=DIRECTION('center_axis',(-0.816496580927725,0.408248290463866,0.408248290463863));
#26866=DIRECTION('ref_axis',(0.577350269189628,0.577350269189628,0.577350269189622));
#26867=DIRECTION('center_axis',(-0.816496580927725,-0.408248290463866,-0.408248290463863));
#26868=DIRECTION('ref_axis',(-0.577350269189628,0.577350269189628,0.577350269189622));
#26869=DIRECTION('center_axis',(0.,1.,0.));
#26870=DIRECTION('ref_axis',(-0.707106781186547,0.,0.707106781186547));
#26871=DIRECTION('center_axis',(0.,1.,0.));
#26872=DIRECTION('ref_axis',(-0.707106781186547,0.,0.707106781186547));
#26873=DIRECTION('center_axis',(0.,1.,0.));
#26874=DIRECTION('ref_axis',(-1.,0.,0.));
#26875=DIRECTION('center_axis',(0.,0.,1.));
#26876=DIRECTION('ref_axis',(0.707106781186547,-0.707106781186547,0.));
#26877=DIRECTION('center_axis',(0.,0.,-1.));
#26878=DIRECTION('ref_axis',(1.,0.,0.));
#26879=DIRECTION('',(0.,0.,-1.));
#26880=DIRECTION('center_axis',(0.707106781186548,0.,-0.707106781186548));
#26881=DIRECTION('ref_axis',(0.707106781186548,0.,0.707106781186548));
#26882=DIRECTION('center_axis',(0.,1.,0.));
#26883=DIRECTION('ref_axis',(0.707106781186547,0.,0.707106781186547));
#26884=DIRECTION('center_axis',(0.,1.,0.));
#26885=DIRECTION('ref_axis',(0.,0.,1.));
#26886=DIRECTION('center_axis',(-0.816496580927726,-0.408248290463864,0.408248290463863));
#26887=DIRECTION('ref_axis',(0.577350269189625,-0.577350269189627,0.577350269189625));
#26888=DIRECTION('center_axis',(1.,0.,0.));
#26889=DIRECTION('ref_axis',(0.,-0.707106781186548,0.707106781186547));
#26890=DIRECTION('center_axis',(0.,1.,0.));
#26891=DIRECTION('ref_axis',(1.,0.,0.));
#26892=DIRECTION('',(1.,0.,0.));
#26893=DIRECTION('',(1.,0.,0.));
#26894=DIRECTION('',(0.,0.,1.));
#26895=DIRECTION('',(1.,0.,0.));
#26896=DIRECTION('',(0.,0.,1.));
#26897=DIRECTION('center_axis',(0.,1.,0.));
#26898=DIRECTION('ref_axis',(0.70710678118655,0.,0.707106781186545));
#26899=DIRECTION('',(-1.,0.,0.));
#26900=DIRECTION('',(0.,0.,1.));
#26901=DIRECTION('',(-1.,0.,0.));
#26902=DIRECTION('',(0.,0.,-1.));
#26903=DIRECTION('center_axis',(-1.,0.,0.));
#26904=DIRECTION('ref_axis',(0.,-0.707106781186549,0.707106781186546));
#26905=DIRECTION('center_axis',(-1.,0.,0.));
#26906=DIRECTION('ref_axis',(0.,-0.707106781186548,0.707106781186547));
#26907=DIRECTION('center_axis',(0.,1.,0.));
#26908=DIRECTION('ref_axis',(0.707106781186547,0.,-0.707106781186547));
#26909=DIRECTION('center_axis',(0.,1.,0.));
#26910=DIRECTION('ref_axis',(1.,0.,0.));
#26911=DIRECTION('',(0.,1.,0.));
#26912=DIRECTION('',(0.,-1.,0.));
#26913=DIRECTION('center_axis',(0.,0.,1.));
#26914=DIRECTION('ref_axis',(0.707106781186547,-0.707106781186547,0.));
#26915=DIRECTION('center_axis',(0.,0.,1.));
#26916=DIRECTION('ref_axis',(0.,-1.,0.));
#26917=DIRECTION('',(0.,0.,1.));
#26918=DIRECTION('center_axis',(0.,0.,-1.));
#26919=DIRECTION('ref_axis',(1.,0.,0.));
#26920=DIRECTION('center_axis',(0.,1.,0.));
#26921=DIRECTION('ref_axis',(0.707106781186547,0.,0.707106781186547));
#26922=DIRECTION('center_axis',(0.,1.,0.));
#26923=DIRECTION('ref_axis',(0.,0.,1.));
#26924=DIRECTION('',(0.,1.,0.));
#26925=DIRECTION('center_axis',(-0.408248290463863,-0.816496580927727,-0.408248290463863));
#26926=DIRECTION('ref_axis',(0.577350269189626,-0.577350269189626,0.577350269189626));
#26927=DIRECTION('center_axis',(1.,0.,0.));
#26928=DIRECTION('ref_axis',(0.,-0.707106781186547,0.707106781186547));
#26929=DIRECTION('center_axis',(-0.408248290463863,-0.816496580927727,0.408248290463863));
#26930=DIRECTION('ref_axis',(0.577350269189626,-0.577350269189626,-0.577350269189626));
#26931=DIRECTION('center_axis',(1.,0.,0.));
#26932=DIRECTION('ref_axis',(0.,-0.707106781186547,-0.707106781186547));
#26933=DIRECTION('center_axis',(0.,0.,-1.));
#26934=DIRECTION('ref_axis',(-1.,0.,0.));
#26935=DIRECTION('',(1.,0.,0.));
#26936=DIRECTION('',(0.,-1.,0.));
#26937=DIRECTION('',(-1.,0.,0.));
#26938=DIRECTION('center_axis',(1.,0.,0.));
#26939=DIRECTION('ref_axis',(0.,-0.707106781186547,-0.707106781186547));
#26940=DIRECTION('center_axis',(1.,0.,0.));
#26941=DIRECTION('ref_axis',(0.,-1.,0.));
#26942=DIRECTION('center_axis',(1.,0.,0.));
#26943=DIRECTION('ref_axis',(0.,-0.707106781186547,0.707106781186547));
#26944=DIRECTION('center_axis',(0.,0.,-1.));
#26945=DIRECTION('ref_axis',(-0.707106781186547,-0.707106781186547,0.));
#26946=DIRECTION('center_axis',(0.,-1.85037170770859E-15,-1.));
#26947=DIRECTION('ref_axis',(0.,-1.,1.85037170770859E-15));
#26948=DIRECTION('center_axis',(-0.707106781186548,0.,-0.707106781186548));
#26949=DIRECTION('ref_axis',(-0.707106781186548,0.,0.707106781186548));
#26950=DIRECTION('center_axis',(-0.816496580927726,0.408248290463864,-0.408248290463863));
#26951=DIRECTION('ref_axis',(-0.577350269189626,-0.577350269189629,0.577350269189623));
#26952=DIRECTION('center_axis',(-1.,0.,0.));
#26953=DIRECTION('ref_axis',(0.,0.,1.));
#26954=DIRECTION('center_axis',(1.,0.,0.));
#26955=DIRECTION('ref_axis',(0.,0.,-1.));
#26956=DIRECTION('center_axis',(0.,-1.,0.));
#26957=DIRECTION('ref_axis',(0.,0.,-1.));
#26958=DIRECTION('center_axis',(-1.,0.,0.));
#26959=DIRECTION('ref_axis',(0.,0.,-1.));
#26960=DIRECTION('center_axis',(-1.,0.,0.));
#26961=DIRECTION('ref_axis',(0.,0.,-1.));
#26962=DIRECTION('center_axis',(-1.,0.,0.));
#26963=DIRECTION('ref_axis',(0.,0.,-1.));
#26964=DIRECTION('',(-1.,0.,0.));
#26965=DIRECTION('center_axis',(1.,0.,0.));
#26966=DIRECTION('ref_axis',(0.,0.,-1.));
#26967=DIRECTION('',(1.,0.,0.));
#26968=DIRECTION('center_axis',(-1.,0.,0.));
#26969=DIRECTION('ref_axis',(0.,0.,-1.));
#26970=DIRECTION('',(-1.,0.,0.));
#26971=DIRECTION('center_axis',(1.,0.,0.));
#26972=DIRECTION('ref_axis',(0.,0.,-1.));
#26973=DIRECTION('',(1.,0.,0.));
#26974=DIRECTION('center_axis',(-1.,0.,0.));
#26975=DIRECTION('ref_axis',(0.,0.,-1.));
#26976=DIRECTION('',(-1.,0.,0.));
#26977=DIRECTION('',(1.,0.,0.));
#26978=DIRECTION('center_axis',(-1.,0.,0.));
#26979=DIRECTION('ref_axis',(0.,0.,-1.));
#26980=DIRECTION('',(-1.,0.,0.));
#26981=DIRECTION('center_axis',(1.,0.,0.));
#26982=DIRECTION('ref_axis',(0.,0.,-1.));
#26983=DIRECTION('',(0.,1.,0.));
#26984=DIRECTION('center_axis',(-1.,0.,0.));
#26985=DIRECTION('ref_axis',(0.,-0.707106781186547,0.707106781186547));
#26986=DIRECTION('center_axis',(1.,0.,0.));
#26987=DIRECTION('ref_axis',(0.,0.,-1.));
#26988=DIRECTION('center_axis',(1.,0.,0.));
#26989=DIRECTION('ref_axis',(0.,-0.707106781186547,0.707106781186547));
#26990=DIRECTION('center_axis',(1.,0.,0.));
#26991=DIRECTION('ref_axis',(0.,0.,-1.));
#26992=DIRECTION('center_axis',(0.,0.568073288796263,0.82297796966638));
#26993=DIRECTION('ref_axis',(-0.707106781186551,-0.581933303118232,0.40168847471878));
#26994=DIRECTION('center_axis',(0.,-0.954719322541023,0.29750800857592));
#26995=DIRECTION('ref_axis',(1.72031375589253E-17,0.29750800857592,0.954719322541023));
#26996=DIRECTION('',(0.,-0.568073288796263,-0.82297796966638));
#26997=DIRECTION('',(0.,0.568073288796263,0.82297796966638));
#26998=DIRECTION('center_axis',(0.,-0.464718576777245,0.885458437419923));
#26999=DIRECTION('ref_axis',(1.07487763314402E-16,-0.885458437419923,-0.464718576777245));
#27000=DIRECTION('center_axis',(0.,0.82297796966638,-0.568073288796263));
#27001=DIRECTION('ref_axis',(0.,0.568073288796263,0.82297796966638));
#27002=DIRECTION('',(0.,0.568073288796263,0.82297796966638));
#27003=DIRECTION('',(1.,0.,0.));
#27004=DIRECTION('center_axis',(-1.,0.,0.));
#27005=DIRECTION('ref_axis',(0.,0.,1.));
#27006=DIRECTION('',(0.,0.,1.));
#27007=DIRECTION('center_axis',(-1.,0.,0.));
#27008=DIRECTION('ref_axis',(0.,-1.,3.70074341541719E-15));
#27009=DIRECTION('',(0.,0.,1.));
#27010=DIRECTION('',(0.,-0.568073288796263,-0.822977969666381));
#27011=DIRECTION('center_axis',(-1.,0.,0.));
#27012=DIRECTION('ref_axis',(0.,0.,1.));
#27013=DIRECTION('',(0.,-1.,0.));
#27014=DIRECTION('',(0.,0.,-1.));
#27015=DIRECTION('',(0.,1.,0.));
#27016=DIRECTION('',(0.,0.,1.));
#27017=DIRECTION('center_axis',(0.,1.,0.));
#27018=DIRECTION('ref_axis',(-0.70710678118655,0.,0.707106781186545));
#27019=DIRECTION('center_axis',(0.,-0.707106781186548,0.707106781186548));
#27020=DIRECTION('ref_axis',(0.,0.707106781186548,0.707106781186548));
#27021=DIRECTION('',(0.,-1.,0.));
#27022=DIRECTION('center_axis',(0.,0.707106781186548,0.707106781186547));
#27023=DIRECTION('ref_axis',(0.,-0.707106781186547,0.707106781186548));
#27024=DIRECTION('center_axis',(0.,-0.464718576777245,0.885458437419923));
#27025=DIRECTION('ref_axis',(0.,0.885458437419923,0.464718576777245));
#27026=DIRECTION('',(0.,1.,0.));
#27027=DIRECTION('center_axis',(0.,0.464718576777246,0.885458437419923));
#27028=DIRECTION('ref_axis',(0.,-0.885458437419923,0.464718576777246));
#27029=DIRECTION('center_axis',(0.,0.,-1.));
#27030=DIRECTION('ref_axis',(-0.707106781186545,-0.70710678118655,0.));
#27031=DIRECTION('center_axis',(0.,0.954719322541023,-0.29750800857592));
#27032=DIRECTION('ref_axis',(-6.88125502357011E-17,-0.29750800857592,-0.954719322541023));
#27033=DIRECTION('',(0.,0.,-1.));
#27034=DIRECTION('center_axis',(0.,0.,-1.));
#27035=DIRECTION('ref_axis',(-0.707106781186544,-0.707106781186551,0.));
#27036=DIRECTION('center_axis',(0.,0.,-1.));
#27037=DIRECTION('ref_axis',(-0.707106781186545,-0.70710678118655,0.));
#27038=DIRECTION('center_axis',(0.,-0.707106781186548,0.707106781186548));
#27039=DIRECTION('ref_axis',(-4.088782444489E-17,-0.707106781186548,-0.707106781186548));
#27040=DIRECTION('center_axis',(0.,-0.954719322541023,-0.297508008575921));
#27041=DIRECTION('ref_axis',(1.72031375589253E-17,-0.297508008575921,0.954719322541023));
#27042=DIRECTION('',(0.,0.,-1.));
#27043=DIRECTION('center_axis',(0.,0.82297796966638,0.568073288796263));
#27044=DIRECTION('ref_axis',(-3.28483356716743E-17,-0.568073288796263,0.82297796966638));
#27045=DIRECTION('',(0.,0.,-1.));
#27046=DIRECTION('center_axis',(0.,0.822977969666381,-0.568073288796263));
#27047=DIRECTION('ref_axis',(3.28483356716743E-17,-0.568073288796263,-0.822977969666381));
#27048=DIRECTION('',(0.,0.,-1.));
#27049=DIRECTION('center_axis',(-1.,0.,0.));
#27050=DIRECTION('ref_axis',(0.,0.,1.));
#27051=DIRECTION('',(0.,0.,1.));
#27052=DIRECTION('',(0.,1.,0.));
#27053=DIRECTION('center_axis',(-1.,0.,0.));
#27054=DIRECTION('ref_axis',(0.,0.,1.));
#27055=DIRECTION('',(0.,-0.568073288796263,0.82297796966638));
#27056=DIRECTION('',(0.,-0.568073288796263,-0.82297796966638));
#27057=DIRECTION('',(0.,0.568073288796263,-0.822977969666381));
#27058=DIRECTION('',(0.,0.,1.));
#27059=DIRECTION('center_axis',(-1.,0.,0.));
#27060=DIRECTION('ref_axis',(0.,0.,1.));
#27061=DIRECTION('',(0.,-0.568073288796263,-0.822977969666381));
#27062=DIRECTION('',(0.,0.568073288796263,0.822977969666381));
#27063=DIRECTION('center_axis',(1.,0.,0.));
#27064=DIRECTION('ref_axis',(0.,0.,-1.));
#27065=DIRECTION('center_axis',(-1.,0.,0.));
#27066=DIRECTION('ref_axis',(0.,-0.822977969666383,0.568073288796259));
#27067=DIRECTION('center_axis',(0.,-0.568073288796263,-0.822977969666381));
#27068=DIRECTION('ref_axis',(-0.707106781186551,0.581933303118232,-0.40168847471878));
#27069=DIRECTION('center_axis',(0.,1.1421113633536E-15,-1.));
#27070=DIRECTION('ref_axis',(-1.90351893892266E-16,1.,1.1421113633536E-15));
#27071=DIRECTION('center_axis',(0.,1.,0.));
#27072=DIRECTION('ref_axis',(0.,0.,-1.));
#27073=DIRECTION('',(0.,-0.568073288796263,-0.822977969666381));
#27074=DIRECTION('',(0.,0.568073288796263,0.822977969666381));
#27075=DIRECTION('center_axis',(0.,0.82297796966638,0.568073288796263));
#27076=DIRECTION('ref_axis',(5.40669131959885E-16,0.568073288796263,-0.82297796966638));
#27077=DIRECTION('',(0.,0.568073288796263,0.822977969666381));
#27078=DIRECTION('center_axis',(0.,0.568073288796263,0.82297796966638));
#27079=DIRECTION('ref_axis',(-0.707106781186551,-0.581933303118232,0.40168847471878));
#27080=DIRECTION('center_axis',(0.,3.04563030227627E-15,-1.));
#27081=DIRECTION('ref_axis',(1.427639204192E-16,-1.,-3.04563030227627E-15));
#27082=DIRECTION('center_axis',(0.,-1.,0.));
#27083=DIRECTION('ref_axis',(1.31393342686697E-16,0.,1.));
#27084=DIRECTION('',(0.,0.568073288796263,0.82297796966638));
#27085=DIRECTION('',(0.,-0.568073288796263,-0.82297796966638));
#27086=DIRECTION('center_axis',(0.,-0.822977969666381,-0.568073288796263));
#27087=DIRECTION('ref_axis',(9.19137524331805E-16,-0.568073288796263,0.82297796966638));
#27088=DIRECTION('center_axis',(0.,0.568073288796263,-0.822977969666381));
#27089=DIRECTION('ref_axis',(-0.707106781186551,0.581933303118232,0.401688474718779));
#27090=DIRECTION('',(0.,-0.568073288796263,0.822977969666381));
#27091=DIRECTION('center_axis',(0.,0.464718576777247,0.885458437419922));
#27092=DIRECTION('ref_axis',(5.37438816572011E-17,0.885458437419922,-0.464718576777247));
#27093=DIRECTION('',(0.,0.568073288796263,-0.822977969666381));
#27094=DIRECTION('center_axis',(-1.,0.,0.));
#27095=DIRECTION('ref_axis',(0.,0.,1.));
#27096=DIRECTION('',(0.,-0.568073288796263,0.82297796966638));
#27097=DIRECTION('center_axis',(0.,0.82297796966638,0.568073288796263));
#27098=DIRECTION('ref_axis',(0.,-0.568073288796263,0.82297796966638));
#27099=DIRECTION('center_axis',(0.,0.82297796966638,0.568073288796263));
#27100=DIRECTION('ref_axis',(6.48802958351862E-16,-0.568073288796263,0.82297796966638));
#27101=DIRECTION('',(1.,0.,0.));
#27102=DIRECTION('',(0.,-0.568073288796263,0.82297796966638));
#27103=DIRECTION('',(1.,0.,0.));
#27104=DIRECTION('center_axis',(0.,0.82297796966638,0.568073288796263));
#27105=DIRECTION('ref_axis',(0.,0.568073288796263,-0.82297796966638));
#27106=DIRECTION('center_axis',(0.,0.568073288796263,0.822977969666381));
#27107=DIRECTION('ref_axis',(-0.707106781186549,-0.581933303118233,0.401688474718781));
#27108=DIRECTION('center_axis',(0.,0.568073288796261,0.822977969666382));
#27109=DIRECTION('ref_axis',(-1.,0.,0.));
#27110=DIRECTION('',(0.,0.568073288796263,0.822977969666381));
#27111=DIRECTION('center_axis',(0.,-0.822977969666381,-0.568073288796263));
#27112=DIRECTION('ref_axis',(0.,0.568073288796263,-0.822977969666381));
#27113=DIRECTION('center_axis',(0.,-0.822977969666381,-0.568073288796263));
#27114=DIRECTION('ref_axis',(-5.40669131959885E-16,0.568073288796263,-0.822977969666381));
#27115=DIRECTION('',(1.,0.,0.));
#27116=DIRECTION('',(0.,0.568073288796263,-0.822977969666381));
#27117=DIRECTION('',(1.,0.,0.));
#27118=DIRECTION('center_axis',(0.,-0.822977969666381,-0.568073288796263));
#27119=DIRECTION('ref_axis',(-3.28483356716743E-17,-0.568073288796263,0.822977969666381));
#27120=DIRECTION('center_axis',(0.,-0.822977969666381,-0.568073288796263));
#27121=DIRECTION('ref_axis',(0.,0.568073288796263,-0.822977969666381));
#27122=DIRECTION('center_axis',(0.,-0.568073288796263,-0.822977969666381));
#27123=DIRECTION('ref_axis',(-0.707106781186551,0.581933303118232,-0.40168847471878));
#27124=DIRECTION('',(0.,-0.568073288796263,-0.822977969666381));
#27125=DIRECTION('center_axis',(-1.,0.,0.));
#27126=DIRECTION('ref_axis',(0.,0.707106781186545,-0.70710678118655));
#27127=DIRECTION('center_axis',(1.,0.,0.));
#27128=DIRECTION('ref_axis',(0.,0.,-1.));
#27129=DIRECTION('center_axis',(0.,1.,0.));
#27130=DIRECTION('ref_axis',(-0.707106781186545,0.,-0.70710678118655));
#27131=DIRECTION('center_axis',(0.,1.,0.));
#27132=DIRECTION('ref_axis',(0.,0.,-1.));
#27133=DIRECTION('center_axis',(0.,-1.,0.));
#27134=DIRECTION('ref_axis',(-1.,0.,0.));
#27135=DIRECTION('center_axis',(-0.408248290463866,-0.816496580927725,-0.408248290463863));
#27136=DIRECTION('ref_axis',(-0.577350269189628,0.577350269189628,-0.577350269189622));
#27137=DIRECTION('center_axis',(0.,0.,-1.));
#27138=DIRECTION('ref_axis',(-0.707106781186547,0.707106781186547,0.));
#27139=DIRECTION('center_axis',(0.408248290463865,-0.816496580927726,0.408248290463862));
#27140=DIRECTION('ref_axis',(-0.577350269189628,-0.577350269189625,-0.577350269189625));
#27141=DIRECTION('center_axis',(0.,0.,1.));
#27142=DIRECTION('ref_axis',(-0.707106781186547,0.707106781186547,0.));
#27143=DIRECTION('center_axis',(0.,-0.707106781186548,-0.707106781186548));
#27144=DIRECTION('ref_axis',(0.,0.707106781186548,-0.707106781186548));
#27145=DIRECTION('center_axis',(0.,0.,-1.));
#27146=DIRECTION('ref_axis',(-0.707106781186547,0.707106781186547,0.));
#27147=DIRECTION('center_axis',(0.,-0.954719322541023,-0.297508008575921));
#27148=DIRECTION('ref_axis',(-3.44062751178505E-17,0.297508008575921,-0.954719322541023));
#27149=DIRECTION('',(0.,0.,1.));
#27150=DIRECTION('center_axis',(0.,1.,0.));
#27151=DIRECTION('ref_axis',(0.70710678118655,0.,0.707106781186545));
#27152=DIRECTION('',(0.,-1.,0.));
#27153=DIRECTION('center_axis',(0.,0.,1.));
#27154=DIRECTION('ref_axis',(1.,0.,0.));
#27155=DIRECTION('center_axis',(1.,0.,0.));
#27156=DIRECTION('ref_axis',(0.,0.,-1.));
#27157=DIRECTION('center_axis',(0.,-1.,0.));
#27158=DIRECTION('ref_axis',(0.,0.,1.));
#27159=DIRECTION('center_axis',(1.,0.,0.));
#27160=DIRECTION('ref_axis',(0.,-0.822977969666381,0.568073288796262));
#27161=DIRECTION('center_axis',(1.,0.,0.));
#27162=DIRECTION('ref_axis',(0.,-0.822977969666381,0.568073288796262));
#27163=DIRECTION('center_axis',(-1.,0.,0.));
#27164=DIRECTION('ref_axis',(0.,0.,1.));
#27165=DIRECTION('',(0.,-0.568073288796263,-0.822977969666381));
#27166=DIRECTION('',(0.,0.,1.));
#27167=DIRECTION('',(0.,-0.568073288796263,-0.822977969666381));
#27168=DIRECTION('center_axis',(0.,-1.,0.));
#27169=DIRECTION('ref_axis',(0.,0.,1.));
#27170=DIRECTION('',(-1.,0.,0.));
#27171=DIRECTION('center_axis',(0.,0.822977969666381,-0.568073288796263));
#27172=DIRECTION('ref_axis',(0.,-0.568073288796263,-0.822977969666381));
#27173=DIRECTION('center_axis',(0.,0.822977969666381,-0.568073288796263));
#27174=DIRECTION('ref_axis',(0.,-0.568073288796263,-0.822977969666381));
#27175=DIRECTION('center_axis',(0.,-1.85037170770859E-15,-1.));
#27176=DIRECTION('ref_axis',(0.,-1.,1.85037170770859E-15));
#27177=DIRECTION('center_axis',(0.,0.,1.));
#27178=DIRECTION('ref_axis',(-0.707106781186553,-0.707106781186542,0.));
#27179=DIRECTION('',(0.,0.,1.));
#27180=DIRECTION('center_axis',(0.,0.822977969666381,-0.568073288796263));
#27181=DIRECTION('ref_axis',(0.,0.568073288796263,0.822977969666381));
#27182=DIRECTION('center_axis',(0.,0.822977969666381,-0.568073288796263));
#27183=DIRECTION('ref_axis',(0.,0.568073288796263,0.822977969666381));
#27184=DIRECTION('',(1.,0.,0.));
#27185=DIRECTION('',(0.,0.568073288796263,0.822977969666381));
#27186=DIRECTION('',(1.,0.,0.));
#27187=DIRECTION('center_axis',(0.,0.,-1.));
#27188=DIRECTION('ref_axis',(-0.70710678118655,0.707106781186545,0.));
#27189=DIRECTION('',(0.,0.,-1.));
#27190=DIRECTION('center_axis',(0.,-0.822977969666381,-0.568073288796263));
#27191=DIRECTION('ref_axis',(0.,0.568073288796263,-0.822977969666381));
#27192=DIRECTION('',(1.,0.,0.));
#27193=DIRECTION('',(0.,0.568073288796263,-0.822977969666381));
#27194=DIRECTION('',(1.,0.,0.));
#27195=DIRECTION('center_axis',(0.,-1.,0.));
#27196=DIRECTION('ref_axis',(-0.70710678118655,0.,-0.707106781186545));
#27197=DIRECTION('',(0.,-1.,0.));
#27198=DIRECTION('center_axis',(0.,0.,1.));
#27199=DIRECTION('ref_axis',(0.,-1.,0.));
#27200=DIRECTION('',(0.,-1.,0.));
#27201=DIRECTION('center_axis',(0.,-0.568073288796263,0.82297796966638));
#27202=DIRECTION('ref_axis',(-0.707106781186551,-0.581933303118231,-0.40168847471878));
#27203=DIRECTION('',(0.,-0.568073288796263,0.82297796966638));
#27204=DIRECTION('center_axis',(0.,0.82297796966638,0.568073288796263));
#27205=DIRECTION('ref_axis',(0.,-0.568073288796263,0.82297796966638));
#27206=DIRECTION('',(1.,0.,0.));
#27207=DIRECTION('',(0.,-0.568073288796263,0.82297796966638));
#27208=DIRECTION('',(1.,0.,0.));
#27209=DIRECTION('center_axis',(0.,1.,0.));
#27210=DIRECTION('ref_axis',(0.,0.,1.));
#27211=DIRECTION('',(0.,0.,1.));
#27212=DIRECTION('center_axis',(-1.,0.,0.));
#27213=DIRECTION('ref_axis',(0.,0.,1.));
#27214=DIRECTION('center_axis',(0.,-1.,0.));
#27215=DIRECTION('ref_axis',(0.,0.,-1.));
#27216=DIRECTION('center_axis',(-1.,0.,0.));
#27217=DIRECTION('ref_axis',(0.,0.,-1.));
#27218=DIRECTION('center_axis',(-1.,0.,0.));
#27219=DIRECTION('ref_axis',(0.,0.,-1.));
#27220=DIRECTION('center_axis',(-1.,0.,0.));
#27221=DIRECTION('ref_axis',(0.,0.,-1.));
#27222=DIRECTION('',(-1.,0.,0.));
#27223=DIRECTION('center_axis',(1.,0.,0.));
#27224=DIRECTION('ref_axis',(0.,-0.822977969666381,0.568073288796262));
#27225=DIRECTION('',(-1.,0.,0.));
#27226=DIRECTION('center_axis',(1.,0.,0.));
#27227=DIRECTION('ref_axis',(0.,-0.822977969666381,0.568073288796262));
#27228=DIRECTION('center_axis',(0.,-1.,0.));
#27229=DIRECTION('ref_axis',(0.,0.,-1.));
#27230=DIRECTION('',(0.,0.,-1.));
#27231=DIRECTION('center_axis',(-1.,0.,0.));
#27232=DIRECTION('ref_axis',(0.,-0.822977969666381,0.568073288796262));
#27233=DIRECTION('center_axis',(-1.,0.,0.));
#27234=DIRECTION('ref_axis',(0.,-0.822977969666381,0.568073288796262));
#27235=DIRECTION('center_axis',(1.,0.,0.));
#27236=DIRECTION('ref_axis',(0.,0.,-1.));
#27237=DIRECTION('',(0.,0.568073288796263,0.822977969666381));
#27238=DIRECTION('center_axis',(0.,0.822977969666381,-0.568073288796263));
#27239=DIRECTION('ref_axis',(0.,0.568073288796263,0.822977969666381));
#27240=DIRECTION('center_axis',(1.,0.,0.));
#27241=DIRECTION('ref_axis',(0.,0.,-1.));
#27242=DIRECTION('',(0.,-0.568073288796263,-0.822977969666381));
#27243=DIRECTION('center_axis',(0.,-0.822977969666381,0.568073288796263));
#27244=DIRECTION('ref_axis',(0.,-0.568073288796263,-0.822977969666381));
#27245=DIRECTION('center_axis',(0.,1.,0.));
#27246=DIRECTION('ref_axis',(0.,0.,1.));
#27247=DIRECTION('',(0.,0.,1.));
#27248=DIRECTION('',(1.,0.,0.));
#27249=DIRECTION('center_axis',(0.,-0.822977969666381,0.568073288796263));
#27250=DIRECTION('ref_axis',(0.,-0.568073288796263,-0.822977969666381));
#27251=DIRECTION('',(0.,-0.568073288796263,-0.822977969666381));
#27252=DIRECTION('center_axis',(1.,0.,0.));
#27253=DIRECTION('ref_axis',(0.,0.,-1.));
#27254=DIRECTION('center_axis',(0.,0.82297796966638,-0.568073288796263));
#27255=DIRECTION('ref_axis',(0.,0.568073288796263,0.82297796966638));
#27256=DIRECTION('',(0.,0.568073288796263,0.82297796966638));
#27257=DIRECTION('center_axis',(1.,0.,0.));
#27258=DIRECTION('ref_axis',(0.,0.,-1.));
#27259=DIRECTION('center_axis',(0.,0.,-1.));
#27260=DIRECTION('ref_axis',(0.,1.,0.));
#27261=DIRECTION('',(1.,0.,0.));
#27262=DIRECTION('',(0.,1.,0.));
#27263=DIRECTION('center_axis',(0.,-0.822977969666381,0.568073288796263));
#27264=DIRECTION('ref_axis',(0.,-0.568073288796263,-0.822977969666381));
#27265=DIRECTION('',(0.,-0.568073288796263,-0.822977969666381));
#27266=DIRECTION('center_axis',(1.,0.,0.));
#27267=DIRECTION('ref_axis',(0.,0.,-1.));
#27268=DIRECTION('center_axis',(-1.,0.,0.));
#27269=DIRECTION('ref_axis',(0.,0.,1.));
#27270=DIRECTION('',(0.,0.,-1.));
#27271=DIRECTION('center_axis',(0.,1.,0.));
#27272=DIRECTION('ref_axis',(0.,0.,-1.));
#27273=DIRECTION('center_axis',(0.,-0.822977969666381,0.568073288796263));
#27274=DIRECTION('ref_axis',(0.,0.568073288796263,0.822977969666381));
#27275=DIRECTION('',(0.,0.568073288796263,0.822977969666381));
#27276=DIRECTION('',(-1.,0.,0.));
#27277=DIRECTION('center_axis',(0.,1.,0.));
#27278=DIRECTION('ref_axis',(0.,0.,-1.));
#27279=DIRECTION('',(0.,0.,-1.));
#27280=DIRECTION('center_axis',(-1.,0.,0.));
#27281=DIRECTION('ref_axis',(0.,0.,1.));
#27282=DIRECTION('center_axis',(0.,0.82297796966638,-0.568073288796263));
#27283=DIRECTION('ref_axis',(0.,-0.568073288796263,-0.82297796966638));
#27284=DIRECTION('',(-1.,0.,0.));
#27285=DIRECTION('',(0.,-0.568073288796263,-0.82297796966638));
#27286=DIRECTION('center_axis',(0.,0.,1.));
#27287=DIRECTION('ref_axis',(0.,1.,0.));
#27288=DIRECTION('',(0.,1.,0.));
#27289=DIRECTION('center_axis',(0.,0.82297796966638,-0.568073288796263));
#27290=DIRECTION('ref_axis',(0.,-0.568073288796263,-0.82297796966638));
#27291=DIRECTION('',(0.,-0.568073288796263,-0.82297796966638));
#27292=DIRECTION('center_axis',(-1.,0.,0.));
#27293=DIRECTION('ref_axis',(0.,0.,1.));
#27294=DIRECTION('center_axis',(-1.,0.,0.));
#27295=DIRECTION('ref_axis',(0.,0.,1.));
#27296=DIRECTION('center_axis',(0.,1.,0.));
#27297=DIRECTION('ref_axis',(1.,0.,0.));
#27298=DIRECTION('center_axis',(0.,1.,0.));
#27299=DIRECTION('ref_axis',(1.,0.,0.));
#27300=DIRECTION('center_axis',(0.,1.,0.));
#27301=DIRECTION('ref_axis',(1.,0.,0.));
#27302=DIRECTION('center_axis',(0.,1.,0.));
#27303=DIRECTION('ref_axis',(1.,0.,0.));
#27304=DIRECTION('center_axis',(0.,0.,1.));
#27305=DIRECTION('ref_axis',(1.,0.,0.));
#27306=DIRECTION('',(0.,0.,-1.));
#27307=DIRECTION('',(0.,0.,1.));
#27308=DIRECTION('center_axis',(0.,0.,1.));
#27309=DIRECTION('ref_axis',(1.,0.,0.));
#27310=DIRECTION('',(0.,0.,-1.));
#27311=DIRECTION('',(0.,0.,1.));
#27312=DIRECTION('center_axis',(0.,-1.,0.));
#27313=DIRECTION('ref_axis',(0.,0.,-1.));
#27314=DIRECTION('center_axis',(0.,-1.,0.));
#27315=DIRECTION('ref_axis',(0.,0.,-1.));
#27316=DIRECTION('center_axis',(0.,-1.,0.));
#27317=DIRECTION('ref_axis',(0.,0.,-1.));
#27318=DIRECTION('center_axis',(0.,-1.,0.));
#27319=DIRECTION('ref_axis',(0.,0.,-1.));
#27320=DIRECTION('center_axis',(0.,1.,0.));
#27321=DIRECTION('ref_axis',(0.,0.,1.));
#27322=DIRECTION('center_axis',(-1.,0.,0.));
#27323=DIRECTION('ref_axis',(0.,0.,1.));
#27324=DIRECTION('center_axis',(1.,0.,0.));
#27325=DIRECTION('ref_axis',(0.,0.,-1.));
#27326=DIRECTION('center_axis',(0.,1.,0.));
#27327=DIRECTION('ref_axis',(-1.,0.,0.));
#27328=DIRECTION('center_axis',(0.,0.,1.));
#27329=DIRECTION('ref_axis',(1.,0.,0.));
#27330=DIRECTION('center_axis',(1.,0.,0.));
#27331=DIRECTION('ref_axis',(0.,0.,-1.));
#90982=CARTESIAN_POINT('',(0.,0.,0.));
#90983=CARTESIAN_POINT('Origin',(0.,14.688,9.576));
#90984=CARTESIAN_POINT('',(-7.65475852003184,22.032,9.576));
#90985=CARTESIAN_POINT('',(-6.79895050724742,22.032,8.976));
#90986=CARTESIAN_POINT('Ctrl Pts',(-7.65475852003184,22.032,9.576));
#90987=CARTESIAN_POINT('Ctrl Pts',(-7.65475852003184,22.032,9.50993230753524));
#90988=CARTESIAN_POINT('Ctrl Pts',(-7.6355023933674,22.032,9.43302512212287));
#90989=CARTESIAN_POINT('Ctrl Pts',(-7.57108059612176,22.032,9.30349794685379));
#90990=CARTESIAN_POINT('Ctrl Pts',(-7.50985737643954,22.032,9.23175552494297));
#90991=CARTESIAN_POINT('Ctrl Pts',(-7.37339958496305,22.032,9.12015369808754));
#90992=CARTESIAN_POINT('Ctrl Pts',(-7.26915110200772,22.032,9.06654458042145));
#90993=CARTESIAN_POINT('Ctrl Pts',(-7.06240578389491,22.032,8.99697822671308));
#90994=CARTESIAN_POINT('Ctrl Pts',(-6.91939858523134,22.032,8.976));
#90995=CARTESIAN_POINT('Ctrl Pts',(-6.79895050724742,22.032,8.976));
#90996=CARTESIAN_POINT('',(7.65475852003184,22.032,9.576));
#90997=CARTESIAN_POINT('Origin',(0.,14.688,9.576));
#90998=CARTESIAN_POINT('',(6.79895050724742,22.032,8.976));
#90999=CARTESIAN_POINT('Ctrl Pts',(6.79895050724742,22.032,8.976));
#91000=CARTESIAN_POINT('Ctrl Pts',(6.91939858523134,22.032,8.976));
#91001=CARTESIAN_POINT('Ctrl Pts',(7.06240578389491,22.032,8.99697822671308));
#91002=CARTESIAN_POINT('Ctrl Pts',(7.26915110200772,22.032,9.06654458042145));
#91003=CARTESIAN_POINT('Ctrl Pts',(7.37339958496305,22.032,9.12015369808754));
#91004=CARTESIAN_POINT('Ctrl Pts',(7.50985737643954,22.032,9.23175552494297));
#91005=CARTESIAN_POINT('Ctrl Pts',(7.57108059612176,22.032,9.30349794685379));
#91006=CARTESIAN_POINT('Ctrl Pts',(7.6355023933674,22.032,9.43302512212287));
#91007=CARTESIAN_POINT('Ctrl Pts',(7.65475852003183,22.032,9.50993230753524));
#91008=CARTESIAN_POINT('Ctrl Pts',(7.65475852003183,22.032,9.576));
#91009=CARTESIAN_POINT('Origin',(0.,14.688,8.976));
#91010=CARTESIAN_POINT('Origin',(0.,14.688,8.976));
#91011=CARTESIAN_POINT('',(-8.976,22.032,8.976));
#91012=CARTESIAN_POINT('Origin',(0.,14.688,9.576));
#91013=CARTESIAN_POINT('',(8.976,20.3414138359048,9.576));
#91014=CARTESIAN_POINT('',(8.976,19.1142272874311,8.976));
#91015=CARTESIAN_POINT('Ctrl Pts',(8.976,20.3414138359048,9.576));
#91016=CARTESIAN_POINT('Ctrl Pts',(8.976,20.3414138359048,9.54827127066274));
#91017=CARTESIAN_POINT('Ctrl Pts',(8.976,20.3367898671095,9.51531964531999));
#91018=CARTESIAN_POINT('Ctrl Pts',(8.976,20.3212334425194,9.45910065247902));
#91019=CARTESIAN_POINT('Ctrl Pts',(8.976,20.3065635015877,9.42543456124496));
#91020=CARTESIAN_POINT('Ctrl Pts',(8.976,20.249339321466,9.32728853684005));
#91021=CARTESIAN_POINT('Ctrl Pts',(8.976,20.1766041453243,9.25923361702201));
#91022=CARTESIAN_POINT('Ctrl Pts',(8.976,20.0032332384638,9.14149743330231));
#91023=CARTESIAN_POINT('Ctrl Pts',(8.976,19.8621493346214,9.08527290977984));
#91024=CARTESIAN_POINT('Ctrl Pts',(8.976,19.5489440827006,8.9996546128544));
#91025=CARTESIAN_POINT('Ctrl Pts',(8.976,19.3123620171841,8.976));
#91026=CARTESIAN_POINT('Ctrl Pts',(8.976,19.1142272874311,8.976));
#91027=CARTESIAN_POINT('',(10.502406415234,16.1810249459574,9.5759999995841));
#91028=CARTESIAN_POINT('Origin',(0.,14.688,9.576));
#91029=CARTESIAN_POINT('',(10.3410376317382,16.32,9.19200000000005));
#91030=CARTESIAN_POINT('Ctrl Pts',(10.3410376317382,16.32,9.19200000000005));
#91031=CARTESIAN_POINT('Ctrl Pts',(10.3617248081483,16.32,9.21653309283687));
#91032=CARTESIAN_POINT('Ctrl Pts',(10.3805706312753,16.318496659833,9.2425856919711));
#91033=CARTESIAN_POINT('Ctrl Pts',(10.427575989582,16.3085883313445,9.31828555819472));
#91034=CARTESIAN_POINT('Ctrl Pts',(10.4505455557009,16.2959510697933,9.36877738492597));
#91035=CARTESIAN_POINT('Ctrl Pts',(10.4861453619965,16.2525805866431,9.47477477792537));
#91036=CARTESIAN_POINT('Ctrl Pts',(10.4967081983238,16.2211079934846,9.5278768615026));
#91037=CARTESIAN_POINT('Ctrl Pts',(10.5024064153566,16.1810249450952,9.576));
#91038=CARTESIAN_POINT('',(9.87403868738623,16.32,8.976));
#91039=CARTESIAN_POINT('Ctrl Pts',(9.87403868738623,16.32,8.976));
#91040=CARTESIAN_POINT('Ctrl Pts',(9.94938560299478,16.32,8.976));
#91041=CARTESIAN_POINT('Ctrl Pts',(10.038098637739,16.32,8.99346724198458));
#91042=CARTESIAN_POINT('Ctrl Pts',(10.1769613378484,16.32,9.05056345745539));
#91043=CARTESIAN_POINT('Ctrl Pts',(10.2518064406884,16.32,9.1001029151404));
#91044=CARTESIAN_POINT('Ctrl Pts',(10.3170794694341,16.32,9.16489488688007));
#91045=CARTESIAN_POINT('Ctrl Pts',(10.3292581499021,16.32,9.17803061550182));
#91046=CARTESIAN_POINT('Ctrl Pts',(10.3410376317382,16.32,9.19200000000005));
#91047=CARTESIAN_POINT('Origin',(0.,14.688,8.976));
#91048=CARTESIAN_POINT('Origin',(0.,14.688,8.976));
#91049=CARTESIAN_POINT('',(8.976,16.32,8.976));
#91050=CARTESIAN_POINT('',(5.406,16.32,8.976));
#91051=CARTESIAN_POINT('',(8.976,8.16,8.976));
#91052=CARTESIAN_POINT('Origin',(0.,14.688,9.576));
#91053=CARTESIAN_POINT('',(5.47747094926116,6.312,8.976));
#91054=CARTESIAN_POINT('',(7.58586053127791,8.16,8.976));
#91055=CARTESIAN_POINT('Origin',(0.,14.688,8.976));
#91056=CARTESIAN_POINT('',(8.18447918304358,8.16,9.19200000701435));
#91057=CARTESIAN_POINT('Ctrl Pts',(8.18447918091711,8.16,9.19200000927994));
#91058=CARTESIAN_POINT('Ctrl Pts',(8.17765408238493,8.16,9.18559400894369));
#91059=CARTESIAN_POINT('Ctrl Pts',(8.17079622196017,8.16,9.17943259569684));
#91060=CARTESIAN_POINT('Ctrl Pts',(8.09540917035175,8.16,9.11433225757306));
#91061=CARTESIAN_POINT('Ctrl Pts',(8.00027281944003,8.16,9.06175915897253));
#91062=CARTESIAN_POINT('Ctrl Pts',(7.8158147055935,8.16,8.99600010426086));
#91063=CARTESIAN_POINT('Ctrl Pts',(7.69110952727826,8.16,8.976));
#91064=CARTESIAN_POINT('Ctrl Pts',(7.58586053127791,8.16,8.976));
#91065=CARTESIAN_POINT('',(8.46817714968195,8.2989750539222,9.57599999941013));
#91066=CARTESIAN_POINT('Ctrl Pts',(8.46817714985942,8.29897505415743,9.57599999910267));
#91067=CARTESIAN_POINT('Ctrl Pts',(8.46646237140931,8.29670224292752,9.57327129421563));
#91068=CARTESIAN_POINT('Ctrl Pts',(8.46474068975494,8.29445309065062,9.5705217301252));
#91069=CARTESIAN_POINT('Ctrl Pts',(8.42551239387429,8.24397830303708,9.50768581373269));
#91070=CARTESIAN_POINT('Ctrl Pts',(8.38629718940947,8.20954290244375,9.44114604862779));
#91071=CARTESIAN_POINT('Ctrl Pts',(8.29342701346891,8.16764410001386,9.30890416369621));
#91072=CARTESIAN_POINT('Ctrl Pts',(8.24325036594714,8.16000000085317,9.2471623230443));
#91073=CARTESIAN_POINT('Ctrl Pts',(8.18447918091711,8.16,9.19200000927994));
#91074=CARTESIAN_POINT('',(5.65341383590482,5.712,9.576));
#91075=CARTESIAN_POINT('Origin',(0.,14.688,9.576));
#91076=CARTESIAN_POINT('Ctrl Pts',(5.65341383590482,5.712,9.576));
#91077=CARTESIAN_POINT('Ctrl Pts',(5.65341383590482,5.712,9.52772474461145));
#91078=CARTESIAN_POINT('Ctrl Pts',(5.65173396439858,5.71782566101816,9.47980816220151));
#91079=CARTESIAN_POINT('Ctrl Pts',(5.64844008976608,5.72922449769278,9.43326698381046));
#91080=CARTESIAN_POINT('Ctrl Pts',(5.64659978410904,5.73559308968745,9.40726417452521));
#91081=CARTESIAN_POINT('Ctrl Pts',(5.64425566453178,5.74370160503296,9.38168922134117));
#91082=CARTESIAN_POINT('Ctrl Pts',(5.6414192185381,5.75350649531546,9.35671706581409));
#91083=CARTESIAN_POINT('Ctrl Pts',(5.63717068251911,5.76819263057785,9.31931282738847));
#91084=CARTESIAN_POINT('Ctrl Pts',(5.63186786836281,5.78651310378535,9.28369622394997));
#91085=CARTESIAN_POINT('Ctrl Pts',(5.62561273253842,5.80807427644408,9.25033319920716));
#91086=CARTESIAN_POINT('Ctrl Pts',(5.61998111348851,5.8274862147444,9.22029582656189));
#91087=CARTESIAN_POINT('Ctrl Pts',(5.61357756657825,5.84952614262748,9.192082716188));
#91088=CARTESIAN_POINT('Ctrl Pts',(5.6064764971916,5.87392073737792,9.16601639098558));
#91089=CARTESIAN_POINT('Ctrl Pts',(5.59861749266153,5.90091909779573,9.13716786737686));
#91090=CARTESIAN_POINT('Ctrl Pts',(5.58998168778861,5.9305354967636,9.1112326479035));
#91091=CARTESIAN_POINT('Ctrl Pts',(5.58070580865448,5.96225420525281,9.08847781685686));
#91092=CARTESIAN_POINT('Ctrl Pts',(5.57155614999854,5.99354130499686,9.06603261960497));
#91093=CARTESIAN_POINT('Ctrl Pts',(5.56178371804112,6.02687598894637,9.04667972811001));
#91094=CARTESIAN_POINT('Ctrl Pts',(5.55151973301419,6.06179064324785,9.03066040140691));
#91095=CARTESIAN_POINT('Ctrl Pts',(5.54013886714959,6.10050455370966,9.01289792338588));
#91096=CARTESIAN_POINT('Ctrl Pts',(5.52823111361269,6.1408904656362,8.99935811831371));
#91097=CARTESIAN_POINT('Ctrl Pts',(5.51599488507964,6.18224768010664,8.99019769931974));
#91098=CARTESIAN_POINT('Ctrl Pts',(5.50371027646634,6.22376841435361,8.98100106150189));
#91099=CARTESIAN_POINT('Ctrl Pts',(5.49114480790582,6.26609816507474,8.97625599324861));
#91100=CARTESIAN_POINT('Ctrl Pts',(5.4785070788898,6.30852211597862,8.97601007981572));
#91101=CARTESIAN_POINT('Ctrl Pts',(5.47816173573397,6.30968140821139,8.97600335989628));
#91102=CARTESIAN_POINT('Ctrl Pts',(5.47781635774676,6.31084070775401,8.976));
#91103=CARTESIAN_POINT('Ctrl Pts',(5.47747094926116,6.312,8.976));
#91104=CARTESIAN_POINT('Origin',(8.16,6.312,9.576));
#91105=CARTESIAN_POINT('',(-5.47747094926116,6.312,8.976));
#91106=CARTESIAN_POINT('',(8.16,6.312,8.976));
#91107=CARTESIAN_POINT('',(-5.65341383590482,5.712,9.576));
#91108=CARTESIAN_POINT('',(8.16,5.712,9.576));
#91109=CARTESIAN_POINT('Ctrl Pts',(-5.65341383590481,5.712,9.576));
#91110=CARTESIAN_POINT('Ctrl Pts',(-5.65341383590481,5.712,9.527724744611));
#91111=CARTESIAN_POINT('Ctrl Pts',(-5.65173396439855,5.71782566101826,9.47980816220062));
#91112=CARTESIAN_POINT('Ctrl Pts',(-5.64844008976599,5.7292244976931,9.43326698380916));
#91113=CARTESIAN_POINT('Ctrl Pts',(-5.64659978410896,5.73559308968772,9.40726417452436));
#91114=CARTESIAN_POINT('Ctrl Pts',(-5.64425566453173,5.74370160503312,9.38168922134076));
#91115=CARTESIAN_POINT('Ctrl Pts',(-5.6414192185381,5.75350649531546,9.35671706581409));
#91116=CARTESIAN_POINT('Ctrl Pts',(-5.63717068251911,5.76819263057784,9.31931282738848));
#91117=CARTESIAN_POINT('Ctrl Pts',(-5.63186786836281,5.78651310378534,9.28369622395));
#91118=CARTESIAN_POINT('Ctrl Pts',(-5.62561273253842,5.80807427644406,9.2503331992072));
#91119=CARTESIAN_POINT('Ctrl Pts',(-5.61998111348852,5.82748621474438,9.22029582656191));
#91120=CARTESIAN_POINT('Ctrl Pts',(-5.61357756657826,5.84952614262748,9.19208271618801));
#91121=CARTESIAN_POINT('Ctrl Pts',(-5.6064764971916,5.87392073737792,9.16601639098558));
#91122=CARTESIAN_POINT('Ctrl Pts',(-5.59861749266153,5.90091909779573,9.13716786737686));
#91123=CARTESIAN_POINT('Ctrl Pts',(-5.58998168778862,5.93053549676361,9.1112326479035));
#91124=CARTESIAN_POINT('Ctrl Pts',(-5.58070580865448,5.96225420525282,9.08847781685685));
#91125=CARTESIAN_POINT('Ctrl Pts',(-5.57155614999855,5.99354130499686,9.06603261960497));
#91126=CARTESIAN_POINT('Ctrl Pts',(-5.56178371804112,6.02687598894637,9.04667972811));
#91127=CARTESIAN_POINT('Ctrl Pts',(-5.55151973301419,6.06179064324785,9.03066040140691));
#91128=CARTESIAN_POINT('Ctrl Pts',(-5.54013886714958,6.10050455370967,9.01289792338587));
#91129=CARTESIAN_POINT('Ctrl Pts',(-5.52823111361269,6.1408904656362,8.99935811831371));
#91130=CARTESIAN_POINT('Ctrl Pts',(-5.51599488507965,6.18224768010664,8.99019769931973));
#91131=CARTESIAN_POINT('Ctrl Pts',(-5.50371027646635,6.22376841435361,8.98100106150188));
#91132=CARTESIAN_POINT('Ctrl Pts',(-5.49114480790581,6.2660981650747,8.97625599324862));
#91133=CARTESIAN_POINT('Ctrl Pts',(-5.47850707888982,6.30852211597862,8.97601007981572));
#91134=CARTESIAN_POINT('Ctrl Pts',(-5.47816173573398,6.30968140821139,8.97600335989628));
#91135=CARTESIAN_POINT('Ctrl Pts',(-5.47781635774676,6.310840707754,8.976));
#91136=CARTESIAN_POINT('Ctrl Pts',(-5.47747094926116,6.312,8.976));
#91137=CARTESIAN_POINT('Origin',(0.,14.688,9.576));
#91138=CARTESIAN_POINT('',(-8.46817714968195,8.2989750539222,9.57599999941013));
#91139=CARTESIAN_POINT('Origin',(0.,14.688,9.576));
#91140=CARTESIAN_POINT('',(-8.18447918304357,8.16,9.19200000701434));
#91141=CARTESIAN_POINT('Ctrl Pts',(-8.1844791809171,8.16,9.19200000927993));
#91142=CARTESIAN_POINT('Ctrl Pts',(-8.1949045656255,8.16000000015134,9.20178521851308));
#91143=CARTESIAN_POINT('Ctrl Pts',(-8.20514137021707,8.16023917963785,9.21185509928412));
#91144=CARTESIAN_POINT('Ctrl Pts',(-8.26618938143075,8.16340256599659,9.27462639810538));
#91145=CARTESIAN_POINT('Ctrl Pts',(-8.31021435687686,8.1731928977421,9.33158129444371));
#91146=CARTESIAN_POINT('Ctrl Pts',(-8.39504149753827,8.21647648944954,9.45541831434885));
#91147=CARTESIAN_POINT('Ctrl Pts',(-8.43230979342604,8.25143554213401,9.51892473628901));
#91148=CARTESIAN_POINT('Ctrl Pts',(-8.46817715042332,8.29897505490483,9.576));
#91149=CARTESIAN_POINT('',(-7.58586053127791,8.16,8.976));
#91150=CARTESIAN_POINT('Ctrl Pts',(-7.58586053127791,8.16,8.976));
#91151=CARTESIAN_POINT('Ctrl Pts',(-7.69110952727826,8.16,8.976));
#91152=CARTESIAN_POINT('Ctrl Pts',(-7.8158147055935,8.16,8.99600010426086));
#91153=CARTESIAN_POINT('Ctrl Pts',(-8.00027281944003,8.16,9.06175915897253));
#91154=CARTESIAN_POINT('Ctrl Pts',(-8.09540917035175,8.16,9.11433225757306));
#91155=CARTESIAN_POINT('Ctrl Pts',(-8.17079622196017,8.16,9.17943259569684));
#91156=CARTESIAN_POINT('Ctrl Pts',(-8.17765408238493,8.16,9.18559400894369));
#91157=CARTESIAN_POINT('Ctrl Pts',(-8.1844791809171,8.16,9.19200000927993));
#91158=CARTESIAN_POINT('Origin',(0.,14.688,8.976));
#91159=CARTESIAN_POINT('Origin',(0.,14.688,8.976));
#91160=CARTESIAN_POINT('',(-8.976,8.16,8.976));
#91161=CARTESIAN_POINT('Origin',(0.,14.688,9.576));
#91162=CARTESIAN_POINT('',(-10.50240641504,16.1810249473222,9.57599999836851));
#91163=CARTESIAN_POINT('',(-10.3410376317382,16.32,9.19200000000005));
#91164=CARTESIAN_POINT('Ctrl Pts',(-10.5024064150668,16.1810249471335,9.57599999755277));
#91165=CARTESIAN_POINT('Ctrl Pts',(-10.4982985638155,16.209920862045,9.54130797221599));
#91166=CARTESIAN_POINT('Ctrl Pts',(-10.4916339518921,16.2346056625403,9.50370530112817));
#91167=CARTESIAN_POINT('Ctrl Pts',(-10.4665021542091,16.2822987670594,9.40995456416038));
#91168=CARTESIAN_POINT('Ctrl Pts',(-10.4452499964683,16.3001798040925,9.35450358157013));
#91169=CARTESIAN_POINT('Ctrl Pts',(-10.3942868948604,16.3171607866726,9.26213931607076));
#91170=CARTESIAN_POINT('Ctrl Pts',(-10.3694620651598,16.32,9.22570876963314));
#91171=CARTESIAN_POINT('Ctrl Pts',(-10.3410376317382,16.32,9.19200000000005));
#91172=CARTESIAN_POINT('',(-8.976,20.3414138359048,9.576));
#91173=CARTESIAN_POINT('Origin',(0.,14.688,9.576));
#91174=CARTESIAN_POINT('',(-8.976,19.1142272874311,8.976));
#91175=CARTESIAN_POINT('Ctrl Pts',(-8.976,19.1142272874311,8.976));
#91176=CARTESIAN_POINT('Ctrl Pts',(-8.976,19.3123620171841,8.976));
#91177=CARTESIAN_POINT('Ctrl Pts',(-8.976,19.5489440827006,8.9996546128544));
#91178=CARTESIAN_POINT('Ctrl Pts',(-8.976,19.8621493346214,9.08527290977984));
#91179=CARTESIAN_POINT('Ctrl Pts',(-8.976,20.0032332384638,9.14149743330231));
#91180=CARTESIAN_POINT('Ctrl Pts',(-8.976,20.1766041453243,9.25923361702201));
#91181=CARTESIAN_POINT('Ctrl Pts',(-8.976,20.249339321466,9.32728853684005));
#91182=CARTESIAN_POINT('Ctrl Pts',(-8.976,20.3065635015877,9.42543456124496));
#91183=CARTESIAN_POINT('Ctrl Pts',(-8.976,20.3212334425194,9.45910065247902));
#91184=CARTESIAN_POINT('Ctrl Pts',(-8.976,20.3367898671095,9.51531964531999));
#91185=CARTESIAN_POINT('Ctrl Pts',(-8.976,20.3414138359048,9.54827127066274));
#91186=CARTESIAN_POINT('Ctrl Pts',(-8.976,20.3414138359048,9.576));
#91187=CARTESIAN_POINT('',(-9.87403868738623,16.32,8.976));
#91188=CARTESIAN_POINT('Origin',(0.,14.688,8.976));
#91189=CARTESIAN_POINT('Ctrl Pts',(-10.3410376317382,16.32,9.19200000000005));
#91190=CARTESIAN_POINT('Ctrl Pts',(-10.3292581499021,16.32,9.17803061550182));
#91191=CARTESIAN_POINT('Ctrl Pts',(-10.3170794694341,16.32,9.16489488688007));
#91192=CARTESIAN_POINT('Ctrl Pts',(-10.2518064406884,16.32,9.1001029151404));
#91193=CARTESIAN_POINT('Ctrl Pts',(-10.1769613378484,16.32,9.05056345745539));
#91194=CARTESIAN_POINT('Ctrl Pts',(-10.038098637739,16.32,8.99346724198458));
#91195=CARTESIAN_POINT('Ctrl Pts',(-9.94938560299478,16.32,8.976));
#91196=CARTESIAN_POINT('Ctrl Pts',(-9.87403868738623,16.32,8.976));
#91197=CARTESIAN_POINT('Origin',(0.,14.688,8.976));
#91198=CARTESIAN_POINT('',(-8.976,16.32,8.976));
#91199=CARTESIAN_POINT('',(-8.976,8.16,8.976));
#91200=CARTESIAN_POINT('',(-5.406,16.32,8.976));
#91201=CARTESIAN_POINT('Origin',(-9.486,15.72,7.128));
#91202=CARTESIAN_POINT('',(-8.976,16.32,7.128));
#91203=CARTESIAN_POINT('',(-8.976,15.72,6.528));
#91204=CARTESIAN_POINT('Origin',(-8.976,15.72,7.128));
#91205=CARTESIAN_POINT('',(-13.464,15.72,6.528));
#91206=CARTESIAN_POINT('',(-9.486,15.72,6.528));
#91207=CARTESIAN_POINT('',(-13.464,16.32,7.128));
#91208=CARTESIAN_POINT('Origin',(-13.464,15.72,7.128));
#91209=CARTESIAN_POINT('',(-9.486,16.32,7.128));
#91210=CARTESIAN_POINT('Origin',(-8.16,8.16,6.528));
#91211=CARTESIAN_POINT('',(-8.976,8.76,6.528));
#91212=CARTESIAN_POINT('',(-8.976,8.16,6.528));
#91213=CARTESIAN_POINT('',(-13.464,8.76,6.528));
#91214=CARTESIAN_POINT('',(-4.08,8.76,6.528));
#91215=CARTESIAN_POINT('',(-13.464,7.752,6.528));
#91216=CARTESIAN_POINT('Origin',(-4.08,8.76,7.128));
#91217=CARTESIAN_POINT('',(-8.376,8.16,7.128));
#91218=CARTESIAN_POINT('Origin',(-8.376,8.76,7.128));
#91219=CARTESIAN_POINT('',(-13.464,8.16,7.128));
#91220=CARTESIAN_POINT('',(-4.08,8.16,7.128));
#91221=CARTESIAN_POINT('Origin',(-13.464,8.76,7.128));
#91222=CARTESIAN_POINT('Origin',(0.,8.16,-8.16));
#91223=CARTESIAN_POINT('',(-8.376,8.16,-10.7469750549048));
#91224=CARTESIAN_POINT('',(-8.376,8.16,-12.24));
#91225=CARTESIAN_POINT('',(-8.16,8.16,-11.208));
#91226=CARTESIAN_POINT('Origin',(-8.76,8.16,-11.208));
#91227=CARTESIAN_POINT('',(-8.16,8.16,-13.272));
#91228=CARTESIAN_POINT('',(-8.16,8.16,-9.384));
#91229=CARTESIAN_POINT('',(-8.376,8.16,-13.7330249450952));
#91230=CARTESIAN_POINT('Origin',(-8.76,8.16,-13.272));
#91231=CARTESIAN_POINT('',(-8.376,8.16,-16.32));
#91232=CARTESIAN_POINT('',(-8.376,8.16,-12.24));
#91233=CARTESIAN_POINT('',(8.376,8.16,-16.32));
#91234=CARTESIAN_POINT('Origin',(0.,8.16,-16.32));
#91235=CARTESIAN_POINT('',(8.376,8.16,-13.7330249450952));
#91236=CARTESIAN_POINT('',(8.376,8.16,0.408000000000001));
#91237=CARTESIAN_POINT('',(8.16,8.16,-13.272));
#91238=CARTESIAN_POINT('Origin',(8.76,8.16,-13.272));
#91239=CARTESIAN_POINT('',(8.16,8.16,-11.208));
#91240=CARTESIAN_POINT('',(8.16,8.16,-11.016));
#91241=CARTESIAN_POINT('',(8.376,8.16,-10.7469750549048));
#91242=CARTESIAN_POINT('Origin',(8.76,8.16,-11.208));
#91243=CARTESIAN_POINT('',(8.376,8.16,7.128));
#91244=CARTESIAN_POINT('',(8.376,8.16,0.408000000000001));
#91245=CARTESIAN_POINT('',(13.464,8.16,7.128));
#91246=CARTESIAN_POINT('',(6.732,8.16,7.128));
#91247=CARTESIAN_POINT('',(13.464,8.16,9.192));
#91248=CARTESIAN_POINT('',(13.464,8.16,6.528));
#91249=CARTESIAN_POINT('',(4.08,8.16,9.192));
#91250=CARTESIAN_POINT('',(-13.464,8.16,9.192));
#91251=CARTESIAN_POINT('',(-7.752,8.16,9.192));
#91252=CARTESIAN_POINT('',(-13.464,8.16,8.976));
#91253=CARTESIAN_POINT('Origin',(8.376,8.76,0.408000000000001));
#91254=CARTESIAN_POINT('',(8.76,8.29897505490484,-10.608));
#91255=CARTESIAN_POINT('Ctrl Pts',(8.76,8.29897505490484,-10.608));
#91256=CARTESIAN_POINT('Ctrl Pts',(8.74559886385357,8.28697996366506,-10.608));
#91257=CARTESIAN_POINT('Ctrl Pts',(8.73070136992335,8.27571625725086,-10.6085196615488));
#91258=CARTESIAN_POINT('Ctrl Pts',(8.67676732474104,8.23871780749174,-10.6125388608906));
#91259=CARTESIAN_POINT('Ctrl Pts',(8.63186213304349,8.21512617965098,-10.6199246683574));
#91260=CARTESIAN_POINT('Ctrl Pts',(8.54101113694863,8.18110084923513,-10.6473790996848));
#91261=CARTESIAN_POINT('Ctrl Pts',(8.495153215849,8.1705557020042,-10.6676000307859));
#91262=CARTESIAN_POINT('Ctrl Pts',(8.42740104856703,8.16155857905989,-10.7075963115084));
#91263=CARTESIAN_POINT('Ctrl Pts',(8.40091268315884,8.16,-10.726224615184));
#91264=CARTESIAN_POINT('Ctrl Pts',(8.37600000000002,8.16,-10.7469750549048));
#91265=CARTESIAN_POINT('',(8.976,8.76,-10.608));
#91266=CARTESIAN_POINT('Origin',(8.376,8.76,-10.608));
#91267=CARTESIAN_POINT('',(8.976,8.76,6.528));
#91268=CARTESIAN_POINT('',(8.976,8.76,0.408000000000001));
#91269=CARTESIAN_POINT('Origin',(8.376,8.76,7.128));
#91270=CARTESIAN_POINT('Origin',(6.732,8.76,7.128));
#91271=CARTESIAN_POINT('',(13.464,8.76,6.528));
#91272=CARTESIAN_POINT('',(6.732,8.76,6.528));
#91273=CARTESIAN_POINT('Origin',(13.464,8.76,7.128));
#91274=CARTESIAN_POINT('Origin',(29.184,12.9636733990013,2.14076058017042));
#91275=CARTESIAN_POINT('',(29.7833084014095,14.3409676242539,0.0947520315295645));
#91276=CARTESIAN_POINT('',(29.7833084014095,8.04157168141595,9.22080000000005));
#91277=CARTESIAN_POINT('',(29.7833084014095,12.9399716334749,2.12440006945309));
#91278=CARTESIAN_POINT('',(29.7786415493758,7.944,9.27200892297725));
#91279=CARTESIAN_POINT('Origin',(29.184,8.0964461888534,9.192));
#91280=CARTESIAN_POINT('',(29.7684724489276,7.85881694748949,9.29752631904628));
#91281=CARTESIAN_POINT('Ctrl Pts',(29.7786415493758,7.944,9.27200892297725));
#91282=CARTESIAN_POINT('Ctrl Pts',(29.7773539804922,7.92576669289312,9.28157838007491));
#91283=CARTESIAN_POINT('Ctrl Pts',(29.7753882078911,7.90558549327391,9.28823908356366));
#91284=CARTESIAN_POINT('Ctrl Pts',(29.7712795144075,7.87601848599256,9.29474689974779));
#91285=CARTESIAN_POINT('Ctrl Pts',(29.7699574919428,7.86745703528122,9.29627565780888));
#91286=CARTESIAN_POINT('Ctrl Pts',(29.7684724489276,7.85881694748801,9.29752631903611));
#91287=CARTESIAN_POINT('',(29.184,8.3232,7.80729593694088));
#91288=CARTESIAN_POINT('Origin',(29.184,7.7232,9.73272845308249));
#91289=CARTESIAN_POINT('',(29.184,13.9939352485079,-0.408));
#91290=CARTESIAN_POINT('',(29.184,12.4698866172014,1.79991660689266));
#91291=CARTESIAN_POINT('',(29.184,14.6544658518362,-1.36492254071927));
#91292=CARTESIAN_POINT('Ctrl Pts',(29.184,14.6544658518362,-1.36492254071922));
#91293=CARTESIAN_POINT('Ctrl Pts',(29.1975798724823,14.6506113776277,-1.35933849475044));
#91294=CARTESIAN_POINT('Ctrl Pts',(29.210686992401,14.6467933040737,-1.35299257799626));
#91295=CARTESIAN_POINT('Ctrl Pts',(29.2845418076992,14.6246038654931,-1.31233545441248));
#91296=CARTESIAN_POINT('Ctrl Pts',(29.3450946879031,14.6026441192603,-1.25400741265493));
#91297=CARTESIAN_POINT('Ctrl Pts',(29.4303036451774,14.5605239942317,-1.1392095265953));
#91298=CARTESIAN_POINT('Ctrl Pts',(29.4669570195186,14.5351279130215,-1.06861054279322));
#91299=CARTESIAN_POINT('Ctrl Pts',(29.5168097217215,14.4724115251156,-0.925286302443268));
#91300=CARTESIAN_POINT('Ctrl Pts',(29.5300379575436,14.4344630406425,-0.852846813728985));
#91301=CARTESIAN_POINT('Ctrl Pts',(29.5300379575436,14.3909332450409,-0.789784417536817));
#91302=CARTESIAN_POINT('Ctrl Pts',(29.5300379575436,14.3517774897719,-0.733058772083134));
#91303=CARTESIAN_POINT('Ctrl Pts',(29.5188800554652,14.3030632457182,-0.677492662862742));
#91304=CARTESIAN_POINT('Ctrl Pts',(29.4694940045382,14.2020866968451,-0.583709983027462));
#91305=CARTESIAN_POINT('Ctrl Pts',(29.4311957085096,14.1505667362922,-0.544734083228222));
#91306=CARTESIAN_POINT('Ctrl Pts',(29.3431197137225,14.0686594841341,-0.481660747664236));
#91307=CARTESIAN_POINT('Ctrl Pts',(29.2811054870975,14.0289285262802,-0.449765893805952));
#91308=CARTESIAN_POINT('Ctrl Pts',(29.2105917253688,14.0021338893618,-0.419073891481067));
#91309=CARTESIAN_POINT('Ctrl Pts',(29.1974888758462,13.9977638944778,-0.413546628135857));
#91310=CARTESIAN_POINT('Ctrl Pts',(29.184,13.9939352485079,-0.407999999999951));
#91311=CARTESIAN_POINT('',(29.184,20.3587352485079,-9.6288));
#91312=CARTESIAN_POINT('',(29.184,12.4698866172014,1.79991660689266));
#91313=CARTESIAN_POINT('',(29.7835166971462,21.456077579674,-10.204722420326));
#91314=CARTESIAN_POINT('Origin',(29.184,21.5019541534552,-10.2288));
#91315=CARTESIAN_POINT('',(29.784,21.432,-10.1274561623021));
#91316=CARTESIAN_POINT('Origin',(29.184,21.432,-10.1274561623021));
#91317=CARTESIAN_POINT('',(29.784,21.0528,-9.57810231614827));
#91318=CARTESIAN_POINT('',(29.784,12.9636733990013,2.14076058017042));
#91319=CARTESIAN_POINT('',(29.7833084014095,21.0528,-9.62879999999999));
#91320=CARTESIAN_POINT('Origin',(29.184,21.0528,-9.57810231614827));
#91321=CARTESIAN_POINT('',(29.7833084014095,14.688,-0.408000000000001));
#91322=CARTESIAN_POINT('',(29.7833084014095,12.9399716334749,2.12440006945309));
#91323=CARTESIAN_POINT('',(29.784,14.688,-0.357302316148278));
#91324=CARTESIAN_POINT('Origin',(29.184,14.688,-0.357302316148276));
#91325=CARTESIAN_POINT('',(29.784,14.3584650549638,0.120100873455422));
#91326=CARTESIAN_POINT('',(29.784,12.9636733990013,2.14076058017042));
#91327=CARTESIAN_POINT('Origin',(29.184,14.3584650549638,0.120100873455422));
#91328=CARTESIAN_POINT('Origin',(29.784,8.3232,7.80729593694088));
#91329=CARTESIAN_POINT('',(28.968,8.3232,7.80729593694088));
#91330=CARTESIAN_POINT('',(29.784,8.3232,7.80729593694088));
#91331=CARTESIAN_POINT('',(28.968,13.9939352485079,-0.408));
#91332=CARTESIAN_POINT('',(28.968,13.9939352485079,-0.408));
#91333=CARTESIAN_POINT('',(29.784,13.9939352485079,-0.408));
#91334=CARTESIAN_POINT('Origin',(29.784,8.3232,7.80729593694088));
#91335=CARTESIAN_POINT('',(28.968,14.688,-1.41350406305912));
#91336=CARTESIAN_POINT('Origin',(28.9300379575436,14.324200550172,-0.886461270359634));
#91337=CARTESIAN_POINT('',(28.968,20.3587352485079,-9.6288));
#91338=CARTESIAN_POINT('',(28.968,20.3587352485079,-9.6288));
#91339=CARTESIAN_POINT('',(29.784,20.3587352485079,-9.6288));
#91340=CARTESIAN_POINT('Origin',(29.784,7.344,-10.608));
#91341=CARTESIAN_POINT('',(29.784,18.9366533000554,5.79779797752167));
#91342=CARTESIAN_POINT('',(29.784,11.2069968487015,-5.40029406097811));
#91343=CARTESIAN_POINT('',(29.784,18.7060084170374,6.41846497492097));
#91344=CARTESIAN_POINT('Origin',(29.784,19.9512,6.528));
#91345=CARTESIAN_POINT('',(29.784,13.7190338627358,-0.806254571695441));
#91346=CARTESIAN_POINT('Origin',(29.784,7.344,-10.608));
#91347=CARTESIAN_POINT('',(29.784,21.432,9.192));
#91348=CARTESIAN_POINT('',(29.784,21.432,-9.384));
#91349=CARTESIAN_POINT('',(29.784,21.3495435339861,9.192));
#91350=CARTESIAN_POINT('',(29.784,7.344,9.192));
#91351=CARTESIAN_POINT('',(29.784,20.3324059608682,7.71845454150864));
#91352=CARTESIAN_POINT('',(29.784,14.2128206445356,-1.1470985449732));
#91353=CARTESIAN_POINT('',(29.784,20.8019222240139,7.44384479993543));
#91354=CARTESIAN_POINT('Origin',(29.784,19.9512,6.528));
#91355=CARTESIAN_POINT('',(29.784,21.0528,7.80729593694088));
#91356=CARTESIAN_POINT('',(29.784,11.7007836305014,-5.74113803425587));
#91357=CARTESIAN_POINT('',(29.784,21.0528,7.11874312522449));
#91358=CARTESIAN_POINT('',(29.784,21.0528,-1.40035203152956));
#91359=CARTESIAN_POINT('',(29.784,21.0528,5.93725687477551));
#91360=CARTESIAN_POINT('Origin',(29.784,19.9512,6.528));
#91361=CARTESIAN_POINT('',(29.784,21.0528,-1.40035203152956));
#91362=CARTESIAN_POINT('Origin',(29.784,7.344,-10.608));
#91363=CARTESIAN_POINT('',(29.784,21.432,-10.2288));
#91364=CARTESIAN_POINT('',(29.784,7.94403556938437,-10.2288));
#91365=CARTESIAN_POINT('',(29.784,13.8513676242539,-10.2288));
#91366=CARTESIAN_POINT('',(29.784,7.944,-10.2288515300056));
#91367=CARTESIAN_POINT('',(29.784,11.0304206445356,-5.7574985449732));
#91368=CARTESIAN_POINT('',(29.784,7.944,-13.272));
#91369=CARTESIAN_POINT('',(29.784,7.944,-11.424));
#91370=CARTESIAN_POINT('',(29.784,21.432,-13.272));
#91371=CARTESIAN_POINT('',(29.784,7.344,-13.272));
#91372=CARTESIAN_POINT('',(29.784,21.432,-9.384));
#91373=CARTESIAN_POINT('Origin',(29.184,7.944,-11.424));
#91374=CARTESIAN_POINT('',(29.7737557460509,7.83359999999999,-10.1944488701125));
#91375=CARTESIAN_POINT('',(29.7737557460508,7.83359999999999,9.192));
#91376=CARTESIAN_POINT('',(29.7737557460508,7.83359999999999,-11.424));
#91377=CARTESIAN_POINT('',(29.184,7.344,9.192));
#91378=CARTESIAN_POINT('Origin',(29.184,7.944,9.192));
#91379=CARTESIAN_POINT('',(29.184,7.344,-13.272));
#91380=CARTESIAN_POINT('',(29.184,7.344,-11.424));
#91381=CARTESIAN_POINT('Origin',(29.184,7.944,-13.272));
#91382=CARTESIAN_POINT('Origin',(29.184,7.944,-10.2288515300056));
#91383=CARTESIAN_POINT('Origin',(29.184,7.944,9.192));
#91384=CARTESIAN_POINT('Ctrl Pts',(29.768472448926,7.85881694748961,9.29752631904605));
#91385=CARTESIAN_POINT('Ctrl Pts',(29.7694086634445,7.85478211554245,9.28908396170822));
#91386=CARTESIAN_POINT('Ctrl Pts',(29.7702047557464,7.85115959495503,9.28049359804113));
#91387=CARTESIAN_POINT('Ctrl Pts',(29.7728449807647,7.83875603249717,9.24614397494659));
#91388=CARTESIAN_POINT('Ctrl Pts',(29.7737557460509,7.8336,9.21936998988089));
#91389=CARTESIAN_POINT('Ctrl Pts',(29.7737557460509,7.8336,9.192));
#91390=CARTESIAN_POINT('',(29.184,7.944,9.792));
#91391=CARTESIAN_POINT('Origin',(29.184,7.944,9.192));
#91392=CARTESIAN_POINT('Origin',(29.184,7.944,9.192));
#91393=CARTESIAN_POINT('Origin',(29.184,7.344,9.192));
#91394=CARTESIAN_POINT('',(29.7737557460508,8.08439812505511,9.30240000000001));
#91395=CARTESIAN_POINT('Origin',(29.184,8.02645646601385,9.192));
#91396=CARTESIAN_POINT('',(29.7737557460509,21.2916018749449,9.30240000000001));
#91397=CARTESIAN_POINT('',(29.7737557460508,7.344,9.30240000000001));
#91398=CARTESIAN_POINT('Origin',(29.184,21.3495435339861,9.192));
#91399=CARTESIAN_POINT('',(29.184,21.432,9.792));
#91400=CARTESIAN_POINT('Origin',(29.184,21.432,9.192));
#91401=CARTESIAN_POINT('',(29.184,7.344,9.792));
#91402=CARTESIAN_POINT('Origin',(8.76,7.344,-11.208));
#91403=CARTESIAN_POINT('',(8.16,7.944,-11.208));
#91404=CARTESIAN_POINT('',(8.76,7.944,-10.608));
#91405=CARTESIAN_POINT('Origin',(8.76,7.944,-11.208));
#91406=CARTESIAN_POINT('',(8.76,7.344,-10.608));
#91407=CARTESIAN_POINT('',(8.16,7.344,-11.208));
#91408=CARTESIAN_POINT('Origin',(8.76,7.944,-13.056));
#91409=CARTESIAN_POINT('',(8.76,7.344,-11.208));
#91410=CARTESIAN_POINT('Origin',(8.76,7.944,-11.208));
#91411=CARTESIAN_POINT('',(8.16,7.944,-13.272));
#91412=CARTESIAN_POINT('',(8.16,7.944,-13.056));
#91413=CARTESIAN_POINT('',(8.76,7.344,-13.272));
#91414=CARTESIAN_POINT('Origin',(8.76,7.944,-13.272));
#91415=CARTESIAN_POINT('',(8.76,7.344,-13.056));
#91416=CARTESIAN_POINT('Origin',(8.76,7.344,-13.272));
#91417=CARTESIAN_POINT('',(8.76,8.29897505490484,-13.872));
#91418=CARTESIAN_POINT('Ctrl Pts',(8.76,8.29897505490484,-13.872));
#91419=CARTESIAN_POINT('Ctrl Pts',(8.73508731684117,8.27822461518402,-13.872));
#91420=CARTESIAN_POINT('Ctrl Pts',(8.70859895143297,8.25959631150844,-13.8704414209401));
#91421=CARTESIAN_POINT('Ctrl Pts',(8.640846784151,8.21960003078587,-13.8614442979958));
#91422=CARTESIAN_POINT('Ctrl Pts',(8.59498886305137,8.19937909968476,-13.8508991507649));
#91423=CARTESIAN_POINT('Ctrl Pts',(8.5041378669565,8.17192466835744,-13.816873820349));
#91424=CARTESIAN_POINT('Ctrl Pts',(8.45923267525896,8.16453886089061,-13.7932821925083));
#91425=CARTESIAN_POINT('Ctrl Pts',(8.40529863007666,8.16051966154879,-13.7562837427492));
#91426=CARTESIAN_POINT('Ctrl Pts',(8.39040113614645,8.16,-13.745020036335));
#91427=CARTESIAN_POINT('Ctrl Pts',(8.37600000000002,8.16,-13.7330249450952));
#91428=CARTESIAN_POINT('',(8.76,7.944,-13.872));
#91429=CARTESIAN_POINT('',(8.76,7.344,-13.872));
#91430=CARTESIAN_POINT('Origin',(8.76,7.944,-13.272));
#91431=CARTESIAN_POINT('',(8.16,7.344,-13.272));
#91432=CARTESIAN_POINT('Origin',(8.76,7.944,-13.272));
#91433=CARTESIAN_POINT('Origin',(8.76,7.944,-13.272));
#91434=CARTESIAN_POINT('Origin',(8.76,7.944,-11.208));
#91435=CARTESIAN_POINT('Origin',(8.76,7.944,-11.208));
#91436=CARTESIAN_POINT('Origin',(8.16,7.344,-10.608));
#91437=CARTESIAN_POINT('',(13.464,7.944,-10.608));
#91438=CARTESIAN_POINT('',(13.566,7.944,-10.608));
#91439=CARTESIAN_POINT('',(13.464,21.432,-10.608));
#91440=CARTESIAN_POINT('',(13.464,7.344,-10.608));
#91441=CARTESIAN_POINT('',(8.976,21.432,-10.608));
#91442=CARTESIAN_POINT('',(4.08,21.432,-10.608));
#91443=CARTESIAN_POINT('',(8.976,7.752,-10.608));
#91444=CARTESIAN_POINT('Origin',(13.566,7.944,-11.208));
#91445=CARTESIAN_POINT('',(14.064,7.344,-11.208));
#91446=CARTESIAN_POINT('',(13.566,7.344,-11.208));
#91447=CARTESIAN_POINT('Origin',(14.064,7.944,-11.208));
#91448=CARTESIAN_POINT('Origin',(18.972,7.344,-12.24));
#91449=CARTESIAN_POINT('',(24.378,7.344,-13.272));
#91450=CARTESIAN_POINT('',(27.528,7.344,9.192));
#91451=CARTESIAN_POINT('',(22.95,7.344,9.192));
#91452=CARTESIAN_POINT('',(27.528,7.344,-11.208));
#91453=CARTESIAN_POINT('',(27.528,7.344,-11.424));
#91454=CARTESIAN_POINT('',(14.904,7.344,-11.208));
#91455=CARTESIAN_POINT('',(13.566,7.344,-11.208));
#91456=CARTESIAN_POINT('',(14.904,7.344,9.192));
#91457=CARTESIAN_POINT('',(14.904,7.344,-1.224));
#91458=CARTESIAN_POINT('',(14.064,7.344,9.192));
#91459=CARTESIAN_POINT('',(13.566,7.344,9.192));
#91460=CARTESIAN_POINT('',(14.064,7.344,-11.424));
#91461=CARTESIAN_POINT('Origin',(24.378,7.944,-13.272));
#91462=CARTESIAN_POINT('',(29.184,7.944,-13.872));
#91463=CARTESIAN_POINT('',(24.378,7.944,-13.872));
#91464=CARTESIAN_POINT('Origin',(29.184,7.944,-13.272));
#91465=CARTESIAN_POINT('Origin',(29.784,7.344,-13.872));
#91466=CARTESIAN_POINT('',(8.976,8.76,-13.872));
#91467=CARTESIAN_POINT('Origin',(8.376,8.76,-13.872));
#91468=CARTESIAN_POINT('',(8.976,21.432,-13.872));
#91469=CARTESIAN_POINT('',(8.976,7.752,-13.872));
#91470=CARTESIAN_POINT('',(29.184,21.432,-13.872));
#91471=CARTESIAN_POINT('',(14.892,21.432,-13.872));
#91472=CARTESIAN_POINT('',(29.184,7.344,-13.872));
#91473=CARTESIAN_POINT('Origin',(0.,8.76,-16.32));
#91474=CARTESIAN_POINT('',(8.976,8.76,-16.32));
#91475=CARTESIAN_POINT('Origin',(8.376,8.76,-16.32));
#91476=CARTESIAN_POINT('',(-8.976,8.76,-16.32));
#91477=CARTESIAN_POINT('Origin',(-8.376,8.76,-16.32));
#91478=CARTESIAN_POINT('Origin',(0.,8.76,-16.32));
#91479=CARTESIAN_POINT('Origin',(-8.376,8.76,-12.24));
#91480=CARTESIAN_POINT('',(-8.76,8.29897505490484,-13.872));
#91481=CARTESIAN_POINT('',(-8.976,8.76,-13.872));
#91482=CARTESIAN_POINT('Origin',(-8.376,8.76,-13.872));
#91483=CARTESIAN_POINT('',(-8.976,8.76,-12.24));
#91484=CARTESIAN_POINT('Ctrl Pts',(-8.76,8.29897505490484,-13.872));
#91485=CARTESIAN_POINT('Ctrl Pts',(-8.74559886385357,8.28697996366506,-13.872));
#91486=CARTESIAN_POINT('Ctrl Pts',(-8.73070136992335,8.27571625725086,-13.8714803384512));
#91487=CARTESIAN_POINT('Ctrl Pts',(-8.67676732474104,8.23871780749174,-13.8674611391094));
#91488=CARTESIAN_POINT('Ctrl Pts',(-8.63186213304349,8.21512617965098,-13.8600753316426));
#91489=CARTESIAN_POINT('Ctrl Pts',(-8.54101113694863,8.18110084923513,-13.8326209003152));
#91490=CARTESIAN_POINT('Ctrl Pts',(-8.495153215849,8.1705557020042,-13.8123999692141));
#91491=CARTESIAN_POINT('Ctrl Pts',(-8.42740104856703,8.16155857905989,-13.7724036884916));
#91492=CARTESIAN_POINT('Ctrl Pts',(-8.40091268315884,8.16,-13.753775384816));
#91493=CARTESIAN_POINT('Ctrl Pts',(-8.37600000000002,8.16,-13.7330249450952));
#91494=CARTESIAN_POINT('Origin',(8.376,8.76,0.408000000000001));
#91495=CARTESIAN_POINT('',(8.976,8.76,0.408000000000001));
#91496=CARTESIAN_POINT('Origin',(-8.976,8.16,-16.32));
#91497=CARTESIAN_POINT('',(-8.976,21.432,-13.872));
#91498=CARTESIAN_POINT('',(-8.976,7.752,-13.872));
#91499=CARTESIAN_POINT('',(-8.976,22.032,-13.272));
#91500=CARTESIAN_POINT('Origin',(-8.976,21.432,-13.272));
#91501=CARTESIAN_POINT('',(-8.976,22.032,-16.32));
#91502=CARTESIAN_POINT('',(-8.976,22.032,-16.32));
#91503=CARTESIAN_POINT('',(-8.976,8.16,-16.32));
#91504=CARTESIAN_POINT('Origin',(0.,14.688,10.008));
#91505=CARTESIAN_POINT('',(-5.47747094926117,6.312,10.608));
#91506=CARTESIAN_POINT('',(5.47747094926117,6.312,10.608));
#91507=CARTESIAN_POINT('Origin',(0.,14.688,10.608));
#91508=CARTESIAN_POINT('',(5.65341383590482,5.712,10.008));
#91509=CARTESIAN_POINT('Ctrl Pts',(5.47747094926117,6.312,10.608));
#91510=CARTESIAN_POINT('Ctrl Pts',(5.47781635774676,6.31084070775401,10.608));
#91511=CARTESIAN_POINT('Ctrl Pts',(5.47816173573397,6.30968140821139,10.6079966401037));
#91512=CARTESIAN_POINT('Ctrl Pts',(5.4785070788898,6.30852211597863,10.6079899201843));
#91513=CARTESIAN_POINT('Ctrl Pts',(5.49114480790582,6.26609816507474,10.6077440067514));
#91514=CARTESIAN_POINT('Ctrl Pts',(5.50371027646633,6.22376841435361,10.6029989384981));
#91515=CARTESIAN_POINT('Ctrl Pts',(5.51599488507963,6.18224768010663,10.5938023006803));
#91516=CARTESIAN_POINT('Ctrl Pts',(5.52823111361268,6.14089046563618,10.5846418816863));
#91517=CARTESIAN_POINT('Ctrl Pts',(5.54013886714959,6.10050455370965,10.5711020766141));
#91518=CARTESIAN_POINT('Ctrl Pts',(5.55151973301418,6.06179064324784,10.5533395985931));
#91519=CARTESIAN_POINT('Ctrl Pts',(5.56320230330928,6.02205043492371,10.5351062409062));
#91520=CARTESIAN_POINT('Ctrl Pts',(5.57424805579781,5.98435659900368,10.5125540425903));
#91521=CARTESIAN_POINT('Ctrl Pts',(5.58446349626691,5.94940030608872,10.4860391845607));
#91522=CARTESIAN_POINT('Ctrl Pts',(5.592321877119,5.92250965328389,10.4656422321956));
#91523=CARTESIAN_POINT('Ctrl Pts',(5.59968890535143,5.89723842986285,10.4428992332132));
#91524=CARTESIAN_POINT('Ctrl Pts',(5.6064764971916,5.87392073737792,10.4179836090144));
#91525=CARTESIAN_POINT('Ctrl Pts',(5.61530694331658,5.84358514382786,10.385569155945));
#91526=CARTESIAN_POINT('Ctrl Pts',(5.62305875077558,5.81689014477726,10.3498344468399));
#91527=CARTESIAN_POINT('Ctrl Pts',(5.62958883887762,5.79436341720472,10.3114013318231));
#91528=CARTESIAN_POINT('Ctrl Pts',(5.63414258927943,5.77865442627962,10.2846000375349));
#91529=CARTESIAN_POINT('Ctrl Pts',(5.63810222290114,5.76497252652513,10.256485863173));
#91530=CARTESIAN_POINT('Ctrl Pts',(5.6414192185381,5.75350649531545,10.2272829341859));
#91531=CARTESIAN_POINT('Ctrl Pts',(5.6473255065113,5.73308992271604,10.1752837978781));
#91532=CARTESIAN_POINT('Ctrl Pts',(5.65109711175118,5.72002855160651,10.1206710696132));
#91533=CARTESIAN_POINT('Ctrl Pts',(5.65263031820826,5.71471580384279,10.0650227061865));
#91534=CARTESIAN_POINT('Ctrl Pts',(5.65315130687732,5.71291051442879,10.0461132066454));
#91535=CARTESIAN_POINT('Ctrl Pts',(5.65341383590482,5.712,10.0270842550942));
#91536=CARTESIAN_POINT('Ctrl Pts',(5.65341383590482,5.712,10.008));
#91537=CARTESIAN_POINT('',(-5.65341383590482,5.712,10.008));
#91538=CARTESIAN_POINT('Origin',(0.,14.688,10.008));
#91539=CARTESIAN_POINT('Ctrl Pts',(-5.47747094926117,6.312,10.608));
#91540=CARTESIAN_POINT('Ctrl Pts',(-5.47781635774676,6.31084070775401,10.608));
#91541=CARTESIAN_POINT('Ctrl Pts',(-5.47816173573397,6.30968140821138,10.6079966401037));
#91542=CARTESIAN_POINT('Ctrl Pts',(-5.4785070788898,6.30852211597862,10.6079899201843));
#91543=CARTESIAN_POINT('Ctrl Pts',(-5.49114480790583,6.26609816507479,10.6077440067514));
#91544=CARTESIAN_POINT('Ctrl Pts',(-5.50371027646632,6.22376841435361,10.6029989384981));
#91545=CARTESIAN_POINT('Ctrl Pts',(-5.51599488507963,6.18224768010662,10.5938023006803));
#91546=CARTESIAN_POINT('Ctrl Pts',(-5.52823111361268,6.14089046563617,10.5846418816863));
#91547=CARTESIAN_POINT('Ctrl Pts',(-5.54013886714959,6.10050455370965,10.5711020766141));
#91548=CARTESIAN_POINT('Ctrl Pts',(-5.55151973301419,6.06179064324784,10.5533395985931));
#91549=CARTESIAN_POINT('Ctrl Pts',(-5.56320230330927,6.02205043492372,10.5351062409062));
#91550=CARTESIAN_POINT('Ctrl Pts',(-5.5742480557978,5.98435659900372,10.5125540425904));
#91551=CARTESIAN_POINT('Ctrl Pts',(-5.5844634962669,5.94940030608877,10.4860391845607));
#91552=CARTESIAN_POINT('Ctrl Pts',(-5.592321877119,5.92250965328393,10.4656422321957));
#91553=CARTESIAN_POINT('Ctrl Pts',(-5.59968890535143,5.89723842986286,10.4428992332132));
#91554=CARTESIAN_POINT('Ctrl Pts',(-5.6064764971916,5.87392073737792,10.4179836090144));
#91555=CARTESIAN_POINT('Ctrl Pts',(-5.61530694331635,5.84358514382866,10.3855691559459));
#91556=CARTESIAN_POINT('Ctrl Pts',(-5.62305875077517,5.81689014477869,10.3498344468418));
#91557=CARTESIAN_POINT('Ctrl Pts',(-5.6295888388771,5.79436341720653,10.3114013318262));
#91558=CARTESIAN_POINT('Ctrl Pts',(-5.63414258927913,5.77865442628068,10.284600037537));
#91559=CARTESIAN_POINT('Ctrl Pts',(-5.63810222290101,5.76497252652559,10.2564858631742));
#91560=CARTESIAN_POINT('Ctrl Pts',(-5.6414192185381,5.75350649531547,10.2272829341859));
#91561=CARTESIAN_POINT('Ctrl Pts',(-5.64732550651149,5.73308992271537,10.1752837978765));
#91562=CARTESIAN_POINT('Ctrl Pts',(-5.65109711175142,5.72002855160565,10.1206710696096));
#91563=CARTESIAN_POINT('Ctrl Pts',(-5.6526303182084,5.71471580384227,10.065022706181));
#91564=CARTESIAN_POINT('Ctrl Pts',(-5.65315130687736,5.71291051442862,10.0461132066417));
#91565=CARTESIAN_POINT('Ctrl Pts',(-5.65341383590481,5.712,10.0270842550924));
#91566=CARTESIAN_POINT('Ctrl Pts',(-5.65341383590481,5.712,10.008));
#91567=CARTESIAN_POINT('Origin',(8.16,6.312,10.008));
#91568=CARTESIAN_POINT('',(8.16,5.712,10.008));
#91569=CARTESIAN_POINT('',(8.16,6.312,10.608));
#91570=CARTESIAN_POINT('Origin',(0.,14.688,8.976));
#91571=CARTESIAN_POINT('',(-7.65475852003184,22.032,8.976));
#91572=CARTESIAN_POINT('',(-7.65475852003184,22.032,8.976));
#91573=CARTESIAN_POINT('',(-8.976,20.3414138359048,8.976));
#91574=CARTESIAN_POINT('Origin',(0.,14.688,8.976));
#91575=CARTESIAN_POINT('',(-8.976,20.3414138359048,8.976));
#91576=CARTESIAN_POINT('',(-10.5576815636768,15.72,9.792));
#91577=CARTESIAN_POINT('Ctrl Pts',(-10.5024064151123,16.1810249468138,9.57599999793657));
#91578=CARTESIAN_POINT('Ctrl Pts',(-10.5040548222992,16.1694295329184,9.58992128726773));
#91579=CARTESIAN_POINT('Ctrl Pts',(-10.5057544224536,16.1573351630669,9.60315512266065));
#91580=CARTESIAN_POINT('Ctrl Pts',(-10.5148744531694,16.09155916125,9.66912629289288));
#91581=CARTESIAN_POINT('Ctrl Pts',(-10.5237938127571,16.0240325570758,9.71543522609453));
#91582=CARTESIAN_POINT('Ctrl Pts',(-10.5415281847411,15.8760247207448,9.77687307989452));
#91583=CARTESIAN_POINT('Ctrl Pts',(-10.5502978947739,15.7955372335741,9.792));
#91584=CARTESIAN_POINT('Ctrl Pts',(-10.5576815636768,15.72,9.792));
#91585=CARTESIAN_POINT('',(-8.79707224023993,8.76,9.792));
#91586=CARTESIAN_POINT('Origin',(0.,14.688,9.792));
#91587=CARTESIAN_POINT('Ctrl Pts',(-8.79707224023993,8.76,9.792));
#91588=CARTESIAN_POINT('Ctrl Pts',(-8.74475140209822,8.68235658016152,9.792));
#91589=CARTESIAN_POINT('Ctrl Pts',(-8.68731298961922,8.59955491146768,9.77616481923648));
#91590=CARTESIAN_POINT('Ctrl Pts',(-8.57761412027184,8.44595653818896,9.71004233715158));
#91591=CARTESIAN_POINT('Ctrl Pts',(-8.52538586265315,8.37511979542016,9.65979463855841));
#91592=CARTESIAN_POINT('Ctrl Pts',(-8.47797223677067,8.31197307918123,9.59120848887458));
#91593=CARTESIAN_POINT('Ctrl Pts',(-8.47304047669745,8.3054210319946,9.58373894855639));
#91594=CARTESIAN_POINT('Ctrl Pts',(-8.46817714985943,8.29897505415743,9.57599999910268));
#91595=CARTESIAN_POINT('',(-5.65341383590482,5.712,8.976));
#91596=CARTESIAN_POINT('',(5.65341383590482,5.712,8.976));
#91597=CARTESIAN_POINT('',(8.79707224023993,8.76,9.792));
#91598=CARTESIAN_POINT('Ctrl Pts',(8.46817714985943,8.29897505415743,9.57599999910267));
#91599=CARTESIAN_POINT('Ctrl Pts',(8.47304047669745,8.3054210319946,9.58373894855639));
#91600=CARTESIAN_POINT('Ctrl Pts',(8.47797223677067,8.31197307918123,9.59120848887458));
#91601=CARTESIAN_POINT('Ctrl Pts',(8.52538586265315,8.37511979542016,9.65979463855841));
#91602=CARTESIAN_POINT('Ctrl Pts',(8.57761412027184,8.44595653818896,9.71004233715158));
#91603=CARTESIAN_POINT('Ctrl Pts',(8.68731298961922,8.59955491146768,9.77616481923648));
#91604=CARTESIAN_POINT('Ctrl Pts',(8.74475140209822,8.68235658016152,9.792));
#91605=CARTESIAN_POINT('Ctrl Pts',(8.79707224023993,8.76,9.792));
#91606=CARTESIAN_POINT('',(10.5576815636768,15.72,9.792));
#91607=CARTESIAN_POINT('Origin',(0.,14.688,9.792));
#91608=CARTESIAN_POINT('Ctrl Pts',(10.5576815636768,15.72,9.792));
#91609=CARTESIAN_POINT('Ctrl Pts',(10.5502978947739,15.7955372335741,9.792));
#91610=CARTESIAN_POINT('Ctrl Pts',(10.5415281847411,15.8760247207448,9.77687307989452));
#91611=CARTESIAN_POINT('Ctrl Pts',(10.5237938127571,16.0240325570758,9.71543522609453));
#91612=CARTESIAN_POINT('Ctrl Pts',(10.5148744531694,16.09155916125,9.66912629289288));
#91613=CARTESIAN_POINT('Ctrl Pts',(10.505754422511,16.1573351626526,9.60315512307621));
#91614=CARTESIAN_POINT('Ctrl Pts',(10.5040548224124,16.169429532113,9.58992128814926));
#91615=CARTESIAN_POINT('Ctrl Pts',(10.502406415277,16.1810249456554,9.57599999932742));
#91616=CARTESIAN_POINT('',(8.976,20.3414138359048,8.976));
#91617=CARTESIAN_POINT('',(8.976,20.3414138359048,8.976));
#91618=CARTESIAN_POINT('',(7.65475852003184,22.032,8.976));
#91619=CARTESIAN_POINT('Origin',(0.,14.688,8.976));
#91620=CARTESIAN_POINT('',(7.65475852003184,22.032,8.976));
#91621=CARTESIAN_POINT('Origin',(0.,14.688,10.608));
#91622=CARTESIAN_POINT('',(4.65,14.688,10.608));
#91623=CARTESIAN_POINT('Origin',(0.,14.688,10.608));
#91624=CARTESIAN_POINT('Origin',(0.,14.688,10.008));
#91625=CARTESIAN_POINT('',(4.05,14.688,10.008));
#91626=CARTESIAN_POINT('Origin',(4.65,14.688,10.008));
#91627=CARTESIAN_POINT('',(-4.05,14.688,10.008));
#91628=CARTESIAN_POINT('Origin',(0.,14.688,10.008));
#91629=CARTESIAN_POINT('Origin',(0.,14.688,10.008));
#91630=CARTESIAN_POINT('Origin',(0.,14.688,-28.56));
#91631=CARTESIAN_POINT('',(4.05,14.688,-23.2866976394846));
#91632=CARTESIAN_POINT('',(-4.04973455112235,14.6878444994985,-23.2871855929692));
#91633=CARTESIAN_POINT('Ctrl Pts',(4.05,14.688,-23.2866976394846));
#91634=CARTESIAN_POINT('Ctrl Pts',(4.05,15.3075500635423,-23.2866976394846));
#91635=CARTESIAN_POINT('Ctrl Pts',(3.75477117913856,16.5345337141539,-23.5265143677541));
#91636=CARTESIAN_POINT('Ctrl Pts',(2.62544753954527,17.9400713904106,-24.2003505240322));
#91637=CARTESIAN_POINT('Ctrl Pts',(0.963114040854605,18.771782200002,-24.7161072950123));
#91638=CARTESIAN_POINT('Ctrl Pts',(-0.963758699703665,18.7714859564189,
-24.7169298905911));
#91639=CARTESIAN_POINT('Ctrl Pts',(-2.6247891146146,17.9416552607379,-24.198643675026));
#91640=CARTESIAN_POINT('Ctrl Pts',(-3.62840603788501,16.6894320905695,-23.603545323179));
#91641=CARTESIAN_POINT('Ctrl Pts',(-4.00295463234946,15.5145058470135,-23.3225641391335));
#91642=CARTESIAN_POINT('Ctrl Pts',(-4.04973093528918,14.8944907445965,-23.2872300244039));
#91643=CARTESIAN_POINT('Ctrl Pts',(-4.04973455112235,14.6878444994985,-23.2871855929692));
#91644=CARTESIAN_POINT('Ctrl Pts',(-4.04973455112235,14.6878444994985,-23.2871855929692));
#91645=CARTESIAN_POINT('Ctrl Pts',(-4.04973816739522,14.4811731258246,-23.2871411561315));
#91646=CARTESIAN_POINT('Ctrl Pts',(-4.00297597826243,13.8612353802335,-23.3222143734744));
#91647=CARTESIAN_POINT('Ctrl Pts',(-3.56692412346984,12.4914312155395,-23.6515378504812));
#91648=CARTESIAN_POINT('Ctrl Pts',(-2.45900653907373,11.2979783098687,-24.2862429721702));
#91649=CARTESIAN_POINT('Ctrl Pts',(-0.748537331746902,10.6045971182748,
-24.7151300001489));
#91650=CARTESIAN_POINT('Ctrl Pts',(0.962955411192786,10.6052665520818,-24.7155432146706));
#91651=CARTESIAN_POINT('Ctrl Pts',(2.62588127377557,11.4354962256271,-24.2004773236733));
#91652=CARTESIAN_POINT('Ctrl Pts',(3.75468223968067,12.8417317939884,-23.5263877718132));
#91653=CARTESIAN_POINT('Ctrl Pts',(4.05,14.0684499364577,-23.2866976394846));
#91654=CARTESIAN_POINT('Ctrl Pts',(4.05,14.688,-23.2866976394846));
#91655=CARTESIAN_POINT('',(-4.05,14.688,-28.56));
#91656=CARTESIAN_POINT('Ctrl Pts',(4.05,14.688,-23.2866976394846));
#91657=CARTESIAN_POINT('Ctrl Pts',(4.05,15.3075500635423,-23.2866976394846));
#91658=CARTESIAN_POINT('Ctrl Pts',(3.75477117913856,16.5345337141539,-23.5265143677541));
#91659=CARTESIAN_POINT('Ctrl Pts',(2.62544753954527,17.9400713904106,-24.2003505240322));
#91660=CARTESIAN_POINT('Ctrl Pts',(0.963114040854605,18.771782200002,-24.7161072950123));
#91661=CARTESIAN_POINT('Ctrl Pts',(-0.963758699703665,18.7714859564189,
-24.7169298905911));
#91662=CARTESIAN_POINT('Ctrl Pts',(-2.6247891146146,17.9416552607379,-24.198643675026));
#91663=CARTESIAN_POINT('Ctrl Pts',(-3.62840603788501,16.6894320905695,-23.603545323179));
#91664=CARTESIAN_POINT('Ctrl Pts',(-4.06538382593506,15.3186709166685,-23.275730620087));
#91665=CARTESIAN_POINT('Ctrl Pts',(-4.06526477212672,14.056908092805,-23.2751714313369));
#91666=CARTESIAN_POINT('Ctrl Pts',(-3.56692412346984,12.4914312155395,-23.6515378504812));
#91667=CARTESIAN_POINT('Ctrl Pts',(-2.45900653907373,11.2979783098687,-24.2862429721702));
#91668=CARTESIAN_POINT('Ctrl Pts',(-0.748537331746902,10.6045971182748,
-24.7151300001489));
#91669=CARTESIAN_POINT('Ctrl Pts',(0.962955411192786,10.6052665520818,-24.7155432146706));
#91670=CARTESIAN_POINT('Ctrl Pts',(2.62588127377557,11.4354962256271,-24.2004773236733));
#91671=CARTESIAN_POINT('Ctrl Pts',(3.75468223968067,12.8417317939884,-23.5263877718132));
#91672=CARTESIAN_POINT('Ctrl Pts',(4.05,14.0684499364577,-23.2866976394846));
#91673=CARTESIAN_POINT('Ctrl Pts',(4.05,14.688,-23.2866976394846));
#91674=CARTESIAN_POINT('Ctrl Pts',(4.05,14.688,-23.4100889968443));
#91675=CARTESIAN_POINT('Ctrl Pts',(4.05,15.2948979871226,-23.4100889968443));
#91676=CARTESIAN_POINT('Ctrl Pts',(3.76867099305398,16.5013175070435,-23.639268673431));
#91677=CARTESIAN_POINT('Ctrl Pts',(2.65216251760359,17.9217437403638,-24.2971624934918));
#91678=CARTESIAN_POINT('Ctrl Pts',(0.976083825977573,18.7724547871576,-24.8055724681825));
#91679=CARTESIAN_POINT('Ctrl Pts',(-0.976707458134028,18.7723064866295,
-24.8063670697087));
#91680=CARTESIAN_POINT('Ctrl Pts',(-2.65136659769237,17.9228893188326,-24.2955099393282));
#91681=CARTESIAN_POINT('Ctrl Pts',(-3.64400988855577,16.6582656006921,-23.7143336666613));
#91682=CARTESIAN_POINT('Ctrl Pts',(-4.06492675298839,15.3040417018377,-23.3994826671362));
#91683=CARTESIAN_POINT('Ctrl Pts',(-4.06464463936234,14.0716337705481,-23.3990003982703));
#91684=CARTESIAN_POINT('Ctrl Pts',(-3.58515476920467,12.5248416966978,-23.7603792715584));
#91685=CARTESIAN_POINT('Ctrl Pts',(-2.48508839011874,11.313229839728,-24.3818697514195));
#91686=CARTESIAN_POINT('Ctrl Pts',(-0.758425187594836,10.6039383832458,
-24.8046262524058));
#91687=CARTESIAN_POINT('Ctrl Pts',(0.975880653594945,10.6046020570128,-24.8050171266545));
#91688=CARTESIAN_POINT('Ctrl Pts',(2.6526462246547,11.4538234315344,-24.2972989549263));
#91689=CARTESIAN_POINT('Ctrl Pts',(3.76856749003345,12.8749501508879,-23.6391422854865));
#91690=CARTESIAN_POINT('Ctrl Pts',(4.05,14.0811020128774,-23.4100889968443));
#91691=CARTESIAN_POINT('Ctrl Pts',(4.05,14.688,-23.4100889968443));
#91692=CARTESIAN_POINT('Ctrl Pts',(4.12855382656681,14.688,-23.6556995045996));
#91693=CARTESIAN_POINT('Ctrl Pts',(4.12855382656681,15.2818241953714,-23.6556995045996));
#91694=CARTESIAN_POINT('Ctrl Pts',(3.86076516644458,16.4700009555522,-23.8638320218397));
#91695=CARTESIAN_POINT('Ctrl Pts',(2.73730116859749,17.9289229358609,-24.49025998471));
#91696=CARTESIAN_POINT('Ctrl Pts',(1.01067042684546,18.8148204133092,-24.9841553078376));
#91697=CARTESIAN_POINT('Ctrl Pts',(-1.01128961537565,18.81490920269,-24.9848957767023));
#91698=CARTESIAN_POINT('Ctrl Pts',(-2.7362314416444,17.9293448956734,-24.4886857048216));
#91699=CARTESIAN_POINT('Ctrl Pts',(-3.73581578291115,16.6318988939734,-23.9350596006894));
#91700=CARTESIAN_POINT('Ctrl Pts',(-4.14332588928732,15.2877734013966,-23.645879002476));
#91701=CARTESIAN_POINT('Ctrl Pts',(-4.14284376717838,14.0880200943702,-23.6455590375256));
#91702=CARTESIAN_POINT('Ctrl Pts',(-3.67922724871041,12.5523416357812,-23.9772276275149));
#91703=CARTESIAN_POINT('Ctrl Pts',(-2.56593899372256,11.3002974171402,-24.5726577012497));
#91704=CARTESIAN_POINT('Ctrl Pts',(-0.784992190544882,10.5616209397369,
-24.9832529516161));
#91705=CARTESIAN_POINT('Ctrl Pts',(1.01033058468266,10.5622313569691,-24.9836167715101));
#91706=CARTESIAN_POINT('Ctrl Pts',(2.73786236787182,11.4466555002175,-24.4904092543238));
#91707=CARTESIAN_POINT('Ctrl Pts',(3.86063072387617,12.9062661228527,-23.863707029497));
#91708=CARTESIAN_POINT('Ctrl Pts',(4.12855382656681,14.0941758046286,-23.6556995045996));
#91709=CARTESIAN_POINT('Ctrl Pts',(4.12855382656681,14.688,-23.6556995045996));
#91710=CARTESIAN_POINT('Ctrl Pts',(4.49055124896869,14.688,-23.9298855992356));
#91711=CARTESIAN_POINT('Ctrl Pts',(4.49055124896869,15.309268298706,-23.9298855992356));
#91712=CARTESIAN_POINT('Ctrl Pts',(4.19325789149789,16.5538991992546,-24.1296173306374));
#91713=CARTESIAN_POINT('Ctrl Pts',(2.96189964638343,18.0879203899391,-24.7457991886986));
#91714=CARTESIAN_POINT('Ctrl Pts',(1.09093099096877,19.0172471491435,-25.2365322104703));
#91715=CARTESIAN_POINT('Ctrl Pts',(-1.09160318155618,19.0173730121423,-25.2372474923589));
#91716=CARTESIAN_POINT('Ctrl Pts',(-2.96090595211656,18.0882153913716,-24.7443467710194));
#91717=CARTESIAN_POINT('Ctrl Pts',(-4.05617421288598,16.724281413124,-24.1994319815307));
#91718=CARTESIAN_POINT('Ctrl Pts',(-4.5067990157527,15.3149441912885,-23.9201607483296));
#91719=CARTESIAN_POINT('Ctrl Pts',(-4.50633590484044,14.0608366102828,-23.9198852215378));
#91720=CARTESIAN_POINT('Ctrl Pts',(-3.99334656067512,12.4505111204035,-24.2401598119502));
#91721=CARTESIAN_POINT('Ctrl Pts',(-2.77546567797919,11.1340757856475,-24.8276385061613));
#91722=CARTESIAN_POINT('Ctrl Pts',(-0.847516003767398,10.35925003365,-25.2356985806033));
#91723=CARTESIAN_POINT('Ctrl Pts',(1.09064974524935,10.3598283214159,-25.2360026321993));
#91724=CARTESIAN_POINT('Ctrl Pts',(2.96246104371384,11.2876559203943,-24.745975080844));
#91725=CARTESIAN_POINT('Ctrl Pts',(4.19313151491998,12.8223742307126,-24.1294895193316));
#91726=CARTESIAN_POINT('Ctrl Pts',(4.49055124896869,14.066731701294,-23.9298855992356));
#91727=CARTESIAN_POINT('Ctrl Pts',(4.49055124896869,14.688,-23.9298855992356));
#91728=CARTESIAN_POINT('Ctrl Pts',(4.82914930550667,14.688,-23.8884972217762));
#91729=CARTESIAN_POINT('Ctrl Pts',(4.82914930550667,15.3651411087864,-23.8884972217762));
#91730=CARTESIAN_POINT('Ctrl Pts',(4.48512211029089,16.7118615149729,-24.1201883032215));
#91731=CARTESIAN_POINT('Ctrl Pts',(3.1421225816263,18.2961229501612,-24.7935064927671));
#91732=CARTESIAN_POINT('Ctrl Pts',(1.15312867962539,19.2416794724688,-25.3160151570556));
#91733=CARTESIAN_POINT('Ctrl Pts',(-1.15390197288246,19.2415063677517,-25.3168334602295));
#91734=CARTESIAN_POINT('Ctrl Pts',(-3.14117672259674,18.2973849550254,-24.791625445862));
#91735=CARTESIAN_POINT('Ctrl Pts',(-4.33514015399536,16.8869796321539,-24.1971733451445));
#91736=CARTESIAN_POINT('Ctrl Pts',(-4.84744213589749,15.3752521866832,-23.8780908288589));
#91737=CARTESIAN_POINT('Ctrl Pts',(-4.84723895642577,14.0004341195354,-23.8776880000878));
#91738=CARTESIAN_POINT('Ctrl Pts',(-4.26310394920718,12.2736358697371,-24.243691927209));
#91739=CARTESIAN_POINT('Ctrl Pts',(-2.94305481018679,10.9230737806569,-24.8807692542566));
#91740=CARTESIAN_POINT('Ctrl Pts',(-0.896059274970361,10.1347927110523,
-25.3149364648599));
#91741=CARTESIAN_POINT('Ctrl Pts',(1.15283203136582,10.1354726840367,-25.3154441441371));
#91742=CARTESIAN_POINT('Ctrl Pts',(3.14266649875182,11.0794084952916,-24.7936105411821));
#91743=CARTESIAN_POINT('Ctrl Pts',(4.48499771640589,12.6644309839937,-24.1200645189159));
#91744=CARTESIAN_POINT('Ctrl Pts',(4.82914930550667,14.0108588912136,-23.8884972217762));
#91745=CARTESIAN_POINT('Ctrl Pts',(4.82914930550667,14.688,-23.8884972217762));
#91746=CARTESIAN_POINT('Ctrl Pts',(4.98309455587392,14.688,-23.7857447483302));
#91747=CARTESIAN_POINT('Ctrl Pts',(4.98309455587392,15.3993352581412,-23.7857447483302));
#91748=CARTESIAN_POINT('Ctrl Pts',(4.61984686946115,16.8080942643989,-24.0427403253296));
#91749=CARTESIAN_POINT('Ctrl Pts',(3.23033415828164,18.4218597445456,-24.7648455472437));
#91750=CARTESIAN_POINT('Ctrl Pts',(1.18500946510329,19.3767869703726,-25.3175476456579));
#91751=CARTESIAN_POINT('Ctrl Pts',(-1.1858026493011,19.3764468388513,-25.3184291664214));
#91752=CARTESIAN_POINT('Ctrl Pts',(-3.22952403638349,18.4236782623287,-24.7630164311167));
#91753=CARTESIAN_POINT('Ctrl Pts',(-4.46436799355182,16.9859405484317,-24.1252892575041));
#91754=CARTESIAN_POINT('Ctrl Pts',(-5.00202271865554,15.4121036450639,-23.7739921258239));
#91755=CARTESIAN_POINT('Ctrl Pts',(-5.00187623559771,13.9634129954428,-23.773392880573));
#91756=CARTESIAN_POINT('Ctrl Pts',(-4.38872103231554,12.1660136178416,-24.1767196449283));
#91757=CARTESIAN_POINT('Ctrl Pts',(-3.02554619696707,10.7957528742936,-24.8568907495462));
#91758=CARTESIAN_POINT('Ctrl Pts',(-0.920995630295405,9.99964854320438,
-25.3165003439991));
#91759=CARTESIAN_POINT('Ctrl Pts',(1.18481428816398,10.0004171523902,-25.3169431584149));
#91760=CARTESIAN_POINT('Ctrl Pts',(3.23086782215367,10.9536438146089,-24.7649814299536));
#91761=CARTESIAN_POINT('Ctrl Pts',(4.61973743891093,12.568210578283,-24.0426046609116));
#91762=CARTESIAN_POINT('Ctrl Pts',(4.98309455587392,13.9766647418588,-23.7857447483302));
#91763=CARTESIAN_POINT('Ctrl Pts',(4.98309455587392,14.688,-23.7857447483302));
#91764=CARTESIAN_POINT('',(4.98309455587393,14.688,-23.7857447483302));
#91765=CARTESIAN_POINT('Ctrl Pts',(4.98309455587392,14.688,-23.7857447483302));
#91766=CARTESIAN_POINT('Ctrl Pts',(4.82914930550667,14.688,-23.8884972217762));
#91767=CARTESIAN_POINT('Ctrl Pts',(4.49055124896869,14.688,-23.9298855992356));
#91768=CARTESIAN_POINT('Ctrl Pts',(4.12855382656681,14.688,-23.6556995045996));
#91769=CARTESIAN_POINT('Ctrl Pts',(4.05,14.688,-23.4100889968443));
#91770=CARTESIAN_POINT('Ctrl Pts',(4.05,14.688,-23.2866976394846));
#91771=CARTESIAN_POINT('Ctrl Pts',(4.98309455587392,14.688,-23.7857447483302));
#91772=CARTESIAN_POINT('Ctrl Pts',(4.98309455587392,13.9766647418588,-23.7857447483302));
#91773=CARTESIAN_POINT('Ctrl Pts',(4.61973743891093,12.568210578283,-24.0426046609116));
#91774=CARTESIAN_POINT('Ctrl Pts',(3.23086782215367,10.9536438146089,-24.7649814299536));
#91775=CARTESIAN_POINT('Ctrl Pts',(1.18481428816398,10.0004171523902,-25.3169431584149));
#91776=CARTESIAN_POINT('Ctrl Pts',(-0.920995630295405,9.99964854320438,
-25.3165003439991));
#91777=CARTESIAN_POINT('Ctrl Pts',(-3.02554619696707,10.7957528742936,-24.8568907495462));
#91778=CARTESIAN_POINT('Ctrl Pts',(-4.38872103231554,12.1660136178416,-24.1767196449283));
#91779=CARTESIAN_POINT('Ctrl Pts',(-5.00187623559771,13.9634129954428,-23.773392880573));
#91780=CARTESIAN_POINT('Ctrl Pts',(-5.00202271865554,15.4121036450639,-23.7739921258239));
#91781=CARTESIAN_POINT('Ctrl Pts',(-4.46436799355182,16.9859405484317,-24.1252892575041));
#91782=CARTESIAN_POINT('Ctrl Pts',(-3.22952403638349,18.4236782623287,-24.7630164311167));
#91783=CARTESIAN_POINT('Ctrl Pts',(-1.1858026493011,19.3764468388513,-25.3184291664214));
#91784=CARTESIAN_POINT('Ctrl Pts',(1.18500946510329,19.3767869703726,-25.3175476456579));
#91785=CARTESIAN_POINT('Ctrl Pts',(3.23033415828164,18.4218597445456,-24.7648455472437));
#91786=CARTESIAN_POINT('Ctrl Pts',(4.61984686946115,16.8080942643989,-24.0427403253296));
#91787=CARTESIAN_POINT('Ctrl Pts',(4.98309455587392,15.3993352581412,-23.7857447483302));
#91788=CARTESIAN_POINT('Ctrl Pts',(4.98309455587392,14.688,-23.7857447483302));
#91789=CARTESIAN_POINT('Origin',(0.,8.16,-16.32));
#91790=CARTESIAN_POINT('',(-7.46865811617337,22.032,-21.2987269400639));
#91791=CARTESIAN_POINT('Origin',(0.,22.032,-16.32));
#91792=CARTESIAN_POINT('',(-4.97872694006385,22.032,-23.7886581161734));
#91793=CARTESIAN_POINT('Ctrl Pts',(-4.97872694006383,22.032,-23.7886581161734));
#91794=CARTESIAN_POINT('Ctrl Pts',(-5.03175741160795,22.032,-23.7533071557714));
#91795=CARTESIAN_POINT('Ctrl Pts',(-5.08949447272707,22.0291665724821,-23.7140146374592));
#91796=CARTESIAN_POINT('Ctrl Pts',(-5.48848300667678,21.9864710060741,-23.4343486419447));
#91797=CARTESIAN_POINT('Ctrl Pts',(-5.78359160013614,21.8585898122974,-23.1919404268334));
#91798=CARTESIAN_POINT('Ctrl Pts',(-6.09332586727315,21.7641706681883,-22.9115678992333));
#91799=CARTESIAN_POINT('Ctrl Pts',(-6.16342892487598,21.7460214167023,-22.8461071850267));
#91800=CARTESIAN_POINT('Ctrl Pts',(-6.27276491697942,21.7305429498519,-22.7405954419643));
#91801=CARTESIAN_POINT('Ctrl Pts',(-6.31169904868965,21.7276769162343,-22.7023279477922));
#91802=CARTESIAN_POINT('Ctrl Pts',(-6.39092330907367,21.7280892293569,-22.6230057301446));
#91803=CARTESIAN_POINT('Ctrl Pts',(-6.42985838198943,21.7314874092212,-22.5832781971981));
#91804=CARTESIAN_POINT('Ctrl Pts',(-6.54332420993137,21.749515544574,-22.4653264460471));
#91805=CARTESIAN_POINT('Ctrl Pts',(-6.61627959897023,21.7715068490678,-22.3866393454028));
#91806=CARTESIAN_POINT('Ctrl Pts',(-6.86061183082832,21.8583157174666,-22.1139294317882));
#91807=CARTESIAN_POINT('Ctrl Pts',(-7.05075649756721,21.9512509923618,-21.8841548448483));
#91808=CARTESIAN_POINT('Ctrl Pts',(-7.30413662922104,22.0160133376152,-21.5381739817469));
#91809=CARTESIAN_POINT('Ctrl Pts',(-7.38436628991476,22.032,-21.4251742909413));
#91810=CARTESIAN_POINT('Ctrl Pts',(-7.46865811617335,22.032,-21.2987269400639));
#91811=CARTESIAN_POINT('',(8.976,22.032,-16.32));
#91812=CARTESIAN_POINT('Origin',(0.,22.032,-16.32));
#91813=CARTESIAN_POINT('',(8.976,8.16,-16.32));
#91814=CARTESIAN_POINT('Origin',(-4.896,21.432,-21.216));
#91815=CARTESIAN_POINT('',(-3.79798786503066,22.032,-21.216));
#91816=CARTESIAN_POINT('Origin',(-4.896,22.032,-21.216));
#91817=CARTESIAN_POINT('',(-3.264,21.7056,-21.216));
#91818=CARTESIAN_POINT('Origin',(-3.79798786503066,21.432,-21.216));
#91819=CARTESIAN_POINT('Origin',(-4.896,21.7056,-21.216));
#91820=CARTESIAN_POINT('Origin',(0.,22.032,-8.16));
#91821=CARTESIAN_POINT('Origin',(-8.376,8.76,-12.24));
#91822=CARTESIAN_POINT('',(-8.76,8.29897505490484,-10.608));
#91823=CARTESIAN_POINT('Ctrl Pts',(-8.37600000000002,8.16,-10.7469750549048));
#91824=CARTESIAN_POINT('Ctrl Pts',(-8.40091268315884,8.16,-10.726224615184));
#91825=CARTESIAN_POINT('Ctrl Pts',(-8.42740104856703,8.16155857905989,-10.7075963115084));
#91826=CARTESIAN_POINT('Ctrl Pts',(-8.495153215849,8.1705557020042,-10.6676000307859));
#91827=CARTESIAN_POINT('Ctrl Pts',(-8.54101113694863,8.18110084923513,-10.6473790996848));
#91828=CARTESIAN_POINT('Ctrl Pts',(-8.63186213304349,8.21512617965098,-10.6199246683574));
#91829=CARTESIAN_POINT('Ctrl Pts',(-8.67676732474104,8.23871780749174,-10.6125388608906));
#91830=CARTESIAN_POINT('Ctrl Pts',(-8.73070136992335,8.27571625725086,-10.6085196615488));
#91831=CARTESIAN_POINT('Ctrl Pts',(-8.74559886385357,8.28697996366506,-10.608));
#91832=CARTESIAN_POINT('Ctrl Pts',(-8.76,8.29897505490484,-10.608));
#91833=CARTESIAN_POINT('',(-8.976,8.76,-10.608));
#91834=CARTESIAN_POINT('',(-8.976,8.76,-12.24));
#91835=CARTESIAN_POINT('Origin',(-8.376,8.76,-10.608));
#91836=CARTESIAN_POINT('Origin',(27.528,7.344,9.192));
#91837=CARTESIAN_POINT('',(26.928,7.944,9.192));
#91838=CARTESIAN_POINT('',(27.528,7.944,9.792));
#91839=CARTESIAN_POINT('Origin',(27.528,7.944,9.192));
#91840=CARTESIAN_POINT('',(27.528,21.432,9.792));
#91841=CARTESIAN_POINT('',(27.528,7.344,9.792));
#91842=CARTESIAN_POINT('',(26.928,21.432,9.192));
#91843=CARTESIAN_POINT('Origin',(27.528,21.432,9.192));
#91844=CARTESIAN_POINT('',(26.928,7.344,9.192));
#91845=CARTESIAN_POINT('Origin',(13.464,21.432,9.192));
#91846=CARTESIAN_POINT('',(27.528,22.032,9.192));
#91847=CARTESIAN_POINT('Origin',(27.528,21.432,9.192));
#91848=CARTESIAN_POINT('',(13.464,21.432,9.792));
#91849=CARTESIAN_POINT('',(29.184,22.032,9.192));
#91850=CARTESIAN_POINT('Origin',(29.184,21.432,9.192));
#91851=CARTESIAN_POINT('',(13.464,22.032,9.192));
#91852=CARTESIAN_POINT('Origin',(27.528,21.432,9.192));
#91853=CARTESIAN_POINT('Origin',(27.528,21.432,9.192));
#91854=CARTESIAN_POINT('Origin',(29.184,21.432,9.192));
#91855=CARTESIAN_POINT('Origin',(29.184,21.432,9.192));
#91856=CARTESIAN_POINT('Origin',(22.95,7.944,9.192));
#91857=CARTESIAN_POINT('',(22.95,7.944,9.792));
#91858=CARTESIAN_POINT('Origin',(27.528,7.944,9.192));
#91859=CARTESIAN_POINT('Origin',(27.528,7.944,9.192));
#91860=CARTESIAN_POINT('Origin',(27.528,7.944,9.192));
#91861=CARTESIAN_POINT('Origin',(29.184,14.2128206445356,-1.1470985449732));
#91862=CARTESIAN_POINT('',(29.184,20.3587352485079,8.8128));
#91863=CARTESIAN_POINT('Origin',(29.184,21.5019541534552,9.4128));
#91864=CARTESIAN_POINT('',(29.184,19.6120909823364,7.73112305029005));
#91865=CARTESIAN_POINT('',(29.184,13.7190338627358,-0.806254571695441));
#91866=CARTESIAN_POINT('',(29.6730897616957,19.9512000004902,7.778));
#91867=CARTESIAN_POINT('Ctrl Pts',(29.184,19.6120909823364,7.73112305029004));
#91868=CARTESIAN_POINT('Ctrl Pts',(29.2236153010039,19.6120909823364,7.73112305029004));
#91869=CARTESIAN_POINT('Ctrl Pts',(29.2633091750366,19.6181170767952,7.73286634617824));
#91870=CARTESIAN_POINT('Ctrl Pts',(29.3404403169688,19.6411090544722,7.73898290297034));
#91871=CARTESIAN_POINT('Ctrl Pts',(29.3778828026048,19.6580635030102,7.74333332193731));
#91872=CARTESIAN_POINT('Ctrl Pts',(29.4840885147569,19.7211400971071,7.75740174366774));
#91873=CARTESIAN_POINT('Ctrl Pts',(29.5468609707651,19.779797513811,7.76771957622777));
#91874=CARTESIAN_POINT('Ctrl Pts',(29.6241709396688,19.8746468475679,7.77610895998165));
#91875=CARTESIAN_POINT('Ctrl Pts',(29.6500156297378,19.9117444532444,7.77800000003095));
#91876=CARTESIAN_POINT('Ctrl Pts',(29.6730897616957,19.9512000009804,7.778));
#91877=CARTESIAN_POINT('Ctrl Pts',(29.6730897616957,19.9512000009804,7.778));
#91878=CARTESIAN_POINT('Ctrl Pts',(29.6960587249166,19.9904757157272,7.77799999996919));
#91879=CARTESIAN_POINT('Ctrl Pts',(29.7162857661367,20.0320859161527,7.77611545312242));
#91880=CARTESIAN_POINT('Ctrl Pts',(29.7660314239133,20.160153365583,7.7633991486045));
#91881=CARTESIAN_POINT('Ctrl Pts',(29.784,20.2498877771072,7.7448784177953));
#91882=CARTESIAN_POINT('Ctrl Pts',(29.784,20.3324059608682,7.71845454150864));
#91883=CARTESIAN_POINT('Origin',(29.184,8.18063237574607,9.4128));
#91884=CARTESIAN_POINT('',(29.184,9.01726475149214,8.8128));
#91885=CARTESIAN_POINT('Origin',(29.184,7.87404584654483,9.4128));
#91886=CARTESIAN_POINT('',(29.184,8.18063237574607,8.8128));
#91887=CARTESIAN_POINT('Origin',(29.184,15.628584851675,-1.82133984076555));
#91888=CARTESIAN_POINT('',(29.184,14.688,0.59750406305912));
#91889=CARTESIAN_POINT('Origin',(29.184,14.323470193544,0.0694031896036992));
#91890=CARTESIAN_POINT('',(29.184,16.1223716334749,-1.48049586748779));
#91891=CARTESIAN_POINT('Origin',(26.928,7.344,9.792));
#91892=CARTESIAN_POINT('Origin',(29.184,21.432,-9.384));
#91893=CARTESIAN_POINT('Origin',(29.184,21.432,-10.2288));
#91894=CARTESIAN_POINT('',(29.184,22.032,-13.272));
#91895=CARTESIAN_POINT('Origin',(29.184,21.432,-13.272));
#91896=CARTESIAN_POINT('',(29.184,22.032,-9.384));
#91897=CARTESIAN_POINT('Origin',(13.464,19.9512,6.528));
#91898=CARTESIAN_POINT('',(27.528,19.9512,7.778));
#91899=CARTESIAN_POINT('Origin',(27.528,19.9512,6.528));
#91900=CARTESIAN_POINT('',(13.464,19.9512,7.778));
#91901=CARTESIAN_POINT('',(28.968,19.6120909823364,7.73112305029005));
#91902=CARTESIAN_POINT('',(13.464,19.6120909823364,7.73112305029005));
#91903=CARTESIAN_POINT('',(28.968,18.7060084170374,6.41846497492097));
#91904=CARTESIAN_POINT('Origin',(28.968,19.9512,6.528));
#91905=CARTESIAN_POINT('',(13.464,18.7060084170374,6.41846497492097));
#91906=CARTESIAN_POINT('',(29.184,19.3965172404536,5.40780937503389));
#91907=CARTESIAN_POINT('Ctrl Pts',(29.184,19.3965172404536,5.4078093750339));
#91908=CARTESIAN_POINT('Ctrl Pts',(29.2594100037102,19.3965172404536,5.4078093750339));
#91909=CARTESIAN_POINT('Ctrl Pts',(29.3397541554034,19.3827001386888,5.41433241819919));
#91910=CARTESIAN_POINT('Ctrl Pts',(29.4875100123773,19.3285720959285,5.44366515993349));
#91911=CARTESIAN_POINT('Ctrl Pts',(29.5549412887334,19.2884885638861,5.46679459941119));
#91912=CARTESIAN_POINT('Ctrl Pts',(29.6626423483001,19.1996511726765,5.52768435501259));
#91913=CARTESIAN_POINT('Ctrl Pts',(29.7092855081103,19.1449042633456,5.56984732632713));
#91914=CARTESIAN_POINT('Ctrl Pts',(29.7699321343959,19.0357206786645,5.67356042783162));
#91915=CARTESIAN_POINT('Ctrl Pts',(29.784,18.9815769113417,5.73538086530188));
#91916=CARTESIAN_POINT('Ctrl Pts',(29.784,18.9366533000553,5.79779797752169));
#91917=CARTESIAN_POINT('',(28.968,19.3965172404536,5.40780937503389));
#91918=CARTESIAN_POINT('',(13.464,19.3965172404536,5.40780937503389));
#91919=CARTESIAN_POINT('',(28.968,21.0528,5.93725687477551));
#91920=CARTESIAN_POINT('Origin',(28.968,19.9512,6.528));
#91921=CARTESIAN_POINT('',(13.464,21.0528,5.93725687477551));
#91922=CARTESIAN_POINT('',(28.968,21.0528,7.11874312522449));
#91923=CARTESIAN_POINT('',(13.464,21.0528,7.11874312522449));
#91924=CARTESIAN_POINT('',(28.968,20.8019222240139,7.44384479993544));
#91925=CARTESIAN_POINT('Origin',(28.968,19.9512,6.528));
#91926=CARTESIAN_POINT('',(13.464,20.8019222240139,7.44384479993543));
#91927=CARTESIAN_POINT('Origin',(28.9300379575436,10.9840064439642,-5.7254604242248));
#91928=CARTESIAN_POINT('',(28.968,9.01726475149214,-9.6288));
#91929=CARTESIAN_POINT('',(29.184,8.95019645516457,-9.6288));
#91930=CARTESIAN_POINT('Origin',(28.9300379575436,8.28966585183622,-9.6288));
#91931=CARTESIAN_POINT('',(28.968,14.688,-1.41350406305912));
#91932=CARTESIAN_POINT('',(29.184,12.1735582741579,-3.0452127961736));
#91933=CARTESIAN_POINT('',(29.184,10.5366338627358,-5.41665457169544));
#91934=CARTESIAN_POINT('',(29.184,11.0112188528984,-4.72911477825469));
#91935=CARTESIAN_POINT('Ctrl Pts',(29.184,12.1735582741579,-3.04521279617358));
#91936=CARTESIAN_POINT('Ctrl Pts',(29.2104713416293,12.1762030381632,-3.06315131981746));
#91937=CARTESIAN_POINT('Ctrl Pts',(29.234788995256,12.1788567912663,-3.08351224071388));
#91938=CARTESIAN_POINT('Ctrl Pts',(29.3226220296533,12.1881180495744,-3.17032211138502));
#91939=CARTESIAN_POINT('Ctrl Pts',(29.3688042730669,12.1918686315823,-3.24838022420768));
#91940=CARTESIAN_POINT('Ctrl Pts',(29.4381265282101,12.1842209848219,-3.41619439674659));
#91941=CARTESIAN_POINT('Ctrl Pts',(29.4608149636269,12.1728534227401,-3.50613803778445));
#91942=CARTESIAN_POINT('Ctrl Pts',(29.5078391962474,12.1108433156642,-3.77854749423463));
#91943=CARTESIAN_POINT('Ctrl Pts',(29.5133365788438,12.0301406684281,-3.96243903993894));
#91944=CARTESIAN_POINT('Ctrl Pts',(29.5133365788438,11.817993240571,-4.26978082644984));
#91945=CARTESIAN_POINT('Ctrl Pts',(29.5078391962474,11.6746662914965,-4.41044497796478));
#91946=CARTESIAN_POINT('Ctrl Pts',(29.4608149636269,11.4419449032558,-4.56501832883223));
#91947=CARTESIAN_POINT('Ctrl Pts',(29.4381265282101,11.3618762483097,-4.60753997656553));
#91948=CARTESIAN_POINT('Ctrl Pts',(29.3688042730669,11.2076777804307,-4.67419517523491));
#91949=CARTESIAN_POINT('Ctrl Pts',(29.3226220296533,11.1333617005729,-4.69836656570777));
#91950=CARTESIAN_POINT('Ctrl Pts',(29.234788995256,11.0489085147679,-4.72048859000003));
#91951=CARTESIAN_POINT('Ctrl Pts',(29.2104713416293,11.0289295908271,-4.72522695506081));
#91952=CARTESIAN_POINT('Ctrl Pts',(29.184,11.0112188528984,-4.7291147782547));
#91953=CARTESIAN_POINT('',(29.184,8.3232,-8.62329593694088));
#91954=CARTESIAN_POINT('',(29.184,10.5366338627358,-5.41665457169544));
#91955=CARTESIAN_POINT('',(29.5300378243943,8.21336101791777,-9.73863898202413));
#91956=CARTESIAN_POINT('Ctrl Pts',(29.5300378238068,8.21336101894687,-9.73863898202463));
#91957=CARTESIAN_POINT('Ctrl Pts',(29.5299652136275,8.21341227938468,-9.54712666911579));
#91958=CARTESIAN_POINT('Ctrl Pts',(29.5021917223446,8.23493660162334,-9.34335072376269));
#91959=CARTESIAN_POINT('Ctrl Pts',(29.4271072085953,8.27246070308698,-9.05540444339829));
#91960=CARTESIAN_POINT('Ctrl Pts',(29.3964683073732,8.28577461186978,-8.96300054972493));
#91961=CARTESIAN_POINT('Ctrl Pts',(29.3190911130439,8.30919077581502,-8.79060079716896));
#91962=CARTESIAN_POINT('Ctrl Pts',(29.2750026556793,8.32025772712183,-8.70955977314038));
#91963=CARTESIAN_POINT('Ctrl Pts',(29.1991477037336,8.32304864986649,-8.63633187201137));
#91964=CARTESIAN_POINT('Ctrl Pts',(29.1917743349867,8.3232,-8.62968955278653));
#91965=CARTESIAN_POINT('Ctrl Pts',(29.184,8.3232,-8.62329593694086));
#91966=CARTESIAN_POINT('Ctrl Pts',(29.184,8.95019645516454,-9.6288));
#91967=CARTESIAN_POINT('Ctrl Pts',(29.191656667606,8.9458499595919,-9.6288));
#91968=CARTESIAN_POINT('Ctrl Pts',(29.1990327024229,8.94132039915384,-9.62894711890317));
#91969=CARTESIAN_POINT('Ctrl Pts',(29.2633794371802,8.89917561711943,-9.63131462110273));
#91970=CARTESIAN_POINT('Ctrl Pts',(29.3088752624018,8.85082583416841,-9.6405225541825));
#91971=CARTESIAN_POINT('Ctrl Pts',(29.3873519467975,8.74278725437783,-9.6628387793616));
#91972=CARTESIAN_POINT('Ctrl Pts',(29.4198150443329,8.68279394360638,-9.67628824309362));
#91973=CARTESIAN_POINT('Ctrl Pts',(29.499741316798,8.4917590529397,-9.71516781540766));
#91974=CARTESIAN_POINT('Ctrl Pts',(29.5300379575436,8.3509498358972,-9.73863907546699));
#91975=CARTESIAN_POINT('Ctrl Pts',(29.5300379575436,8.21368550110616,-9.73863907546699));
#91976=CARTESIAN_POINT('Ctrl Pts',(29.5300379129813,8.21352326407097,-9.73863904400745));
#91977=CARTESIAN_POINT('Ctrl Pts',(29.5300378238059,8.21336101791847,-9.73863898105247));
#91978=CARTESIAN_POINT('Origin',(13.464,10.6896,-3.264));
#91979=CARTESIAN_POINT('',(27.528,10.6896,-1.764));
#91980=CARTESIAN_POINT('Origin',(27.528,10.6896,-3.264));
#91981=CARTESIAN_POINT('',(28.368,10.6896,-1.764));
#91982=CARTESIAN_POINT('',(13.464,10.6896,-1.764));
#91983=CARTESIAN_POINT('',(28.368,11.0112188528984,-4.72911477825469));
#91984=CARTESIAN_POINT('Origin',(28.368,10.6896,-3.264));
#91985=CARTESIAN_POINT('',(13.464,11.0112188528984,-4.72911477825469));
#91986=CARTESIAN_POINT('',(28.368,12.1735582741579,-3.0452127961736));
#91987=CARTESIAN_POINT('',(13.464,12.1735582741579,-3.0452127961736));
#91988=CARTESIAN_POINT('Origin',(28.368,10.6896,-3.264));
#91989=CARTESIAN_POINT('Origin',(13.566,7.944,9.192));
#91990=CARTESIAN_POINT('',(14.904,7.944,9.792));
#91991=CARTESIAN_POINT('Origin',(14.904,7.944,9.192));
#91992=CARTESIAN_POINT('',(14.064,7.944,9.792));
#91993=CARTESIAN_POINT('',(13.566,7.944,9.792));
#91994=CARTESIAN_POINT('Origin',(14.064,7.944,9.192));
#91995=CARTESIAN_POINT('Origin',(14.904,7.944,-1.224));
#91996=CARTESIAN_POINT('',(15.504,7.944,9.192));
#91997=CARTESIAN_POINT('Origin',(14.904,7.944,9.192));
#91998=CARTESIAN_POINT('',(15.504,7.944,-10.608));
#91999=CARTESIAN_POINT('Origin',(14.904,7.944,-11.208));
#92000=CARTESIAN_POINT('',(15.504,7.944,-1.224));
#92001=CARTESIAN_POINT('Origin',(14.904,7.944,9.192));
#92002=CARTESIAN_POINT('Origin',(14.904,7.944,9.192));
#92003=CARTESIAN_POINT('Origin',(14.064,7.752,9.192));
#92004=CARTESIAN_POINT('',(13.464,7.944,9.192));
#92005=CARTESIAN_POINT('Origin',(14.064,7.944,9.192));
#92006=CARTESIAN_POINT('',(14.064,8.76,9.792));
#92007=CARTESIAN_POINT('',(14.064,7.752,9.792));
#92008=CARTESIAN_POINT('Origin',(14.064,8.76,9.192));
#92009=CARTESIAN_POINT('',(13.464,7.752,9.192));
#92010=CARTESIAN_POINT('Origin',(14.064,7.944,9.192));
#92011=CARTESIAN_POINT('Origin',(14.064,7.944,9.192));
#92012=CARTESIAN_POINT('Origin',(14.064,7.944,-11.424));
#92013=CARTESIAN_POINT('',(13.464,7.944,-11.424));
#92014=CARTESIAN_POINT('Origin',(13.464,7.344,-10.608));
#92015=CARTESIAN_POINT('',(13.464,15.72,6.528));
#92016=CARTESIAN_POINT('',(13.464,8.16,6.528));
#92017=CARTESIAN_POINT('',(13.464,16.32,7.128));
#92018=CARTESIAN_POINT('Origin',(13.464,15.72,7.128));
#92019=CARTESIAN_POINT('',(13.464,16.32,9.192));
#92020=CARTESIAN_POINT('',(13.464,16.32,6.528));
#92021=CARTESIAN_POINT('',(13.464,21.432,9.192));
#92022=CARTESIAN_POINT('',(13.464,7.752,9.192));
#92023=CARTESIAN_POINT('',(13.464,21.432,7.63693253176196));
#92024=CARTESIAN_POINT('',(13.464,21.432,-9.384));
#92025=CARTESIAN_POINT('',(13.464,19.9512,8.378));
#92026=CARTESIAN_POINT('Origin',(13.464,19.9512,6.528));
#92027=CARTESIAN_POINT('',(13.464,21.432,5.41906746823804));
#92028=CARTESIAN_POINT('Origin',(13.464,19.9512,6.528));
#92029=CARTESIAN_POINT('',(13.464,21.432,-9.384));
#92030=CARTESIAN_POINT('',(13.464,10.6896,-1.164));
#92031=CARTESIAN_POINT('Origin',(13.464,10.6896,-3.264));
#92032=CARTESIAN_POINT('Origin',(14.904,19.9512,6.528));
#92033=CARTESIAN_POINT('',(15.504,21.432,7.63693253176196));
#92034=CARTESIAN_POINT('',(15.504,19.9512,4.678));
#92035=CARTESIAN_POINT('Origin',(15.504,19.9512,6.528));
#92036=CARTESIAN_POINT('',(14.904,19.9512,5.278));
#92037=CARTESIAN_POINT('Origin',(14.904,19.9512,4.678));
#92038=CARTESIAN_POINT('',(14.904,19.9512,7.778));
#92039=CARTESIAN_POINT('Origin',(14.904,19.9512,6.528));
#92040=CARTESIAN_POINT('Origin',(14.904,19.9512,6.528));
#92041=CARTESIAN_POINT('',(15.504,21.432,5.41906746823804));
#92042=CARTESIAN_POINT('Origin',(15.504,19.9512,6.528));
#92043=CARTESIAN_POINT('Ctrl Pts',(15.504,21.432,5.41906746823803));
#92044=CARTESIAN_POINT('Ctrl Pts',(15.504,21.4328877903851,5.42173404364279));
#92045=CARTESIAN_POINT('Ctrl Pts',(15.5039980295845,21.4337726990646,5.42440158176169));
#92046=CARTESIAN_POINT('Ctrl Pts',(15.5036999443769,21.5011431619309,5.62822703110169));
#92047=CARTESIAN_POINT('Ctrl Pts',(15.4928973998635,21.5511743231396,5.83454649786246));
#92048=CARTESIAN_POINT('Ctrl Pts',(15.479052798459,21.6048568406253,6.20610495800375));
#92049=CARTESIAN_POINT('Ctrl Pts',(15.4748965230232,21.6166,6.36623586415006));
#92050=CARTESIAN_POINT('Ctrl Pts',(15.4748965230232,21.6166,6.68976413584994));
#92051=CARTESIAN_POINT('Ctrl Pts',(15.479052798459,21.6048568406253,6.84989504199625));
#92052=CARTESIAN_POINT('Ctrl Pts',(15.4928973998635,21.5511743231396,7.22145350213754));
#92053=CARTESIAN_POINT('Ctrl Pts',(15.5036999443769,21.5011431619309,7.42777296889831));
#92054=CARTESIAN_POINT('Ctrl Pts',(15.5039980295845,21.4337726990639,7.63159841824056));
#92055=CARTESIAN_POINT('Ctrl Pts',(15.504,21.4328877903859,7.63426595635496));
#92056=CARTESIAN_POINT('Ctrl Pts',(15.504,21.432,7.63693253176197));
#92057=CARTESIAN_POINT('Origin',(14.904,21.432,0.816000000000001));
#92058=CARTESIAN_POINT('',(15.504,21.432,-10.608));
#92059=CARTESIAN_POINT('',(15.504,21.432,0.816000000000001));
#92060=CARTESIAN_POINT('',(14.904,22.032,-11.208));
#92061=CARTESIAN_POINT('Origin',(14.904,21.432,-11.208));
#92062=CARTESIAN_POINT('',(14.904,22.032,9.192));
#92063=CARTESIAN_POINT('',(14.904,22.032,0.816000000000001));
#92064=CARTESIAN_POINT('',(15.504,21.432,9.192));
#92065=CARTESIAN_POINT('Origin',(14.904,21.432,9.192));
#92066=CARTESIAN_POINT('',(15.504,21.432,0.816000000000001));
#92067=CARTESIAN_POINT('Origin',(13.464,19.9512,6.528));
#92068=CARTESIAN_POINT('',(14.064,19.9512,7.778));
#92069=CARTESIAN_POINT('Origin',(14.064,19.9512,6.528));
#92070=CARTESIAN_POINT('',(13.464,19.9512,7.778));
#92071=CARTESIAN_POINT('Origin',(14.904,10.6896,-3.264));
#92072=CARTESIAN_POINT('',(15.504,10.6896,-5.364));
#92073=CARTESIAN_POINT('Origin',(15.504,10.6896,-3.264));
#92074=CARTESIAN_POINT('',(14.904,10.6896,-4.764));
#92075=CARTESIAN_POINT('Origin',(14.904,10.6896,-5.364));
#92076=CARTESIAN_POINT('',(14.904,10.6896,-1.764));
#92077=CARTESIAN_POINT('Origin',(14.904,10.6896,-3.264));
#92078=CARTESIAN_POINT('Origin',(14.904,10.6896,-3.264));
#92079=CARTESIAN_POINT('Origin',(13.464,10.6896,-3.264));
#92080=CARTESIAN_POINT('',(14.064,10.6896,-1.764));
#92081=CARTESIAN_POINT('Origin',(14.064,10.6896,-3.264));
#92082=CARTESIAN_POINT('',(13.464,10.6896,-1.764));
#92083=CARTESIAN_POINT('Origin',(15.504,7.344,9.792));
#92084=CARTESIAN_POINT('',(15.504,7.344,-10.608));
#92085=CARTESIAN_POINT('',(15.504,7.752,9.192));
#92086=CARTESIAN_POINT('Origin',(14.064,10.6896,-3.264));
#92087=CARTESIAN_POINT('Origin',(14.064,10.6896,-1.164));
#92088=CARTESIAN_POINT('Origin',(14.064,19.9512,6.528));
#92089=CARTESIAN_POINT('Origin',(14.064,19.9512,8.378));
#92090=CARTESIAN_POINT('Ctrl Pts',(13.464,21.432,7.63693253176197));
#92091=CARTESIAN_POINT('Ctrl Pts',(13.464,21.4328877903851,7.63426595635721));
#92092=CARTESIAN_POINT('Ctrl Pts',(13.4640019704155,21.4337726990646,7.63159841823831));
#92093=CARTESIAN_POINT('Ctrl Pts',(13.4643000556231,21.5011431619309,7.42777296889831));
#92094=CARTESIAN_POINT('Ctrl Pts',(13.4751026001365,21.5511743231396,7.22145350213754));
#92095=CARTESIAN_POINT('Ctrl Pts',(13.488947201541,21.6048568406253,6.84989504199625));
#92096=CARTESIAN_POINT('Ctrl Pts',(13.4931034769768,21.6166,6.68976413584994));
#92097=CARTESIAN_POINT('Ctrl Pts',(13.4931034769768,21.6166,6.36623586415006));
#92098=CARTESIAN_POINT('Ctrl Pts',(13.488947201541,21.6048568406253,6.20610495800375));
#92099=CARTESIAN_POINT('Ctrl Pts',(13.4751026001365,21.5511743231396,5.83454649786246));
#92100=CARTESIAN_POINT('Ctrl Pts',(13.4643000556231,21.5011431619309,5.62822703110169));
#92101=CARTESIAN_POINT('Ctrl Pts',(13.4640019704155,21.4337726990639,5.42440158175944));
#92102=CARTESIAN_POINT('Ctrl Pts',(13.464,21.4328877903859,5.42173404364504));
#92103=CARTESIAN_POINT('Ctrl Pts',(13.464,21.432,5.41906746823803));
#92104=CARTESIAN_POINT('Origin',(14.064,21.432,-9.384));
#92105=CARTESIAN_POINT('',(14.064,22.032,9.192));
#92106=CARTESIAN_POINT('Origin',(14.064,21.432,9.192));
#92107=CARTESIAN_POINT('',(14.064,22.032,-11.208));
#92108=CARTESIAN_POINT('',(14.064,22.032,-9.384));
#92109=CARTESIAN_POINT('Origin',(14.064,21.432,-11.208));
#92110=CARTESIAN_POINT('Origin',(12.138,15.72,7.128));
#92111=CARTESIAN_POINT('',(8.976,15.72,6.528));
#92112=CARTESIAN_POINT('',(12.138,15.72,6.528));
#92113=CARTESIAN_POINT('',(8.976,16.32,7.128));
#92114=CARTESIAN_POINT('Origin',(8.976,15.72,7.128));
#92115=CARTESIAN_POINT('',(12.138,16.32,7.128));
#92116=CARTESIAN_POINT('Origin',(13.464,8.16,6.528));
#92117=CARTESIAN_POINT('',(8.976,8.16,6.528));
#92118=CARTESIAN_POINT('Origin',(4.08,8.76,9.192));
#92119=CARTESIAN_POINT('',(4.08,8.76,9.792));
#92120=CARTESIAN_POINT('Origin',(8.16,8.16,9.792));
#92121=CARTESIAN_POINT('',(14.904,21.432,9.792));
#92122=CARTESIAN_POINT('',(14.904,7.752,9.792));
#92123=CARTESIAN_POINT('',(14.064,21.432,9.792));
#92124=CARTESIAN_POINT('',(4.08,21.432,9.792));
#92125=CARTESIAN_POINT('',(14.064,15.72,9.792));
#92126=CARTESIAN_POINT('',(14.064,7.752,9.792));
#92127=CARTESIAN_POINT('',(9.486,15.72,9.792));
#92128=CARTESIAN_POINT('Origin',(9.486,15.72,9.192));
#92129=CARTESIAN_POINT('Origin',(14.064,15.72,9.192));
#92130=CARTESIAN_POINT('',(9.486,16.32,9.192));
#92131=CARTESIAN_POINT('Origin',(10.812,16.32,8.16));
#92132=CARTESIAN_POINT('',(8.976,16.32,8.568));
#92133=CARTESIAN_POINT('Origin',(14.064,7.752,9.192));
#92134=CARTESIAN_POINT('Origin',(14.064,21.432,9.192));
#92135=CARTESIAN_POINT('Origin',(4.08,21.432,9.192));
#92136=CARTESIAN_POINT('Origin',(14.064,21.432,9.192));
#92137=CARTESIAN_POINT('Origin',(14.904,21.432,9.192));
#92138=CARTESIAN_POINT('',(4.08,22.032,9.192));
#92139=CARTESIAN_POINT('Origin',(14.064,21.432,9.192));
#92140=CARTESIAN_POINT('Origin',(14.904,7.752,9.192));
#92141=CARTESIAN_POINT('Origin',(14.904,21.432,9.192));
#92142=CARTESIAN_POINT('Origin',(14.904,21.432,9.192));
#92143=CARTESIAN_POINT('Origin',(0.,22.032,-8.16));
#92144=CARTESIAN_POINT('',(8.976,22.032,-13.272));
#92145=CARTESIAN_POINT('',(14.892,22.032,-13.272));
#92146=CARTESIAN_POINT('',(8.976,22.032,8.976));
#92147=CARTESIAN_POINT('',(-3.07332505037306,22.032,-19.3985100942983));
#92148=CARTESIAN_POINT('Origin',(-4.896,22.032,-21.216));
#92149=CARTESIAN_POINT('Origin',(-4.896,22.032,-21.216));
#92150=CARTESIAN_POINT('',(-29.184,22.032,-13.272));
#92151=CARTESIAN_POINT('',(-4.08,22.032,-13.272));
#92152=CARTESIAN_POINT('',(-29.184,22.032,9.792));
#92153=CARTESIAN_POINT('',(-29.184,22.032,-11.016));
#92154=CARTESIAN_POINT('',(-27.528,22.032,9.792));
#92155=CARTESIAN_POINT('',(-26.928,22.032,9.792));
#92156=CARTESIAN_POINT('',(-26.928,22.032,9.192));
#92157=CARTESIAN_POINT('Origin',(-27.528,22.032,9.192));
#92158=CARTESIAN_POINT('',(-26.928,22.032,-11.208));
#92159=CARTESIAN_POINT('',(-26.928,22.032,-10.608));
#92160=CARTESIAN_POINT('',(-14.904,22.032,-11.208));
#92161=CARTESIAN_POINT('',(-14.892,22.032,-11.208));
#92162=CARTESIAN_POINT('',(-14.904,22.032,9.192));
#92163=CARTESIAN_POINT('',(-14.904,22.032,-9.384));
#92164=CARTESIAN_POINT('',(-14.064,22.032,9.192));
#92165=CARTESIAN_POINT('',(-7.752,22.032,9.192));
#92166=CARTESIAN_POINT('',(-14.064,22.032,-11.208));
#92167=CARTESIAN_POINT('',(-14.064,22.032,0.816000000000001));
#92168=CARTESIAN_POINT('',(-8.376,22.032,-11.208));
#92169=CARTESIAN_POINT('',(-14.892,22.032,-11.208));
#92170=CARTESIAN_POINT('',(-8.376,22.032,8.976));
#92171=CARTESIAN_POINT('',(-8.376,22.032,-12.24));
#92172=CARTESIAN_POINT('',(-8.976,22.032,8.976));
#92173=CARTESIAN_POINT('',(8.376,22.032,8.976));
#92174=CARTESIAN_POINT('',(-8.976,22.032,8.976));
#92175=CARTESIAN_POINT('',(8.376,22.032,-11.208));
#92176=CARTESIAN_POINT('',(8.376,22.032,0.408000000000001));
#92177=CARTESIAN_POINT('',(4.08,22.032,-11.208));
#92178=CARTESIAN_POINT('',(27.528,22.032,-11.208));
#92179=CARTESIAN_POINT('',(4.08,22.032,-11.208));
#92180=CARTESIAN_POINT('',(27.528,22.032,-9.384));
#92181=CARTESIAN_POINT('',(-6.72,22.032,-18.552));
#92182=CARTESIAN_POINT('',(-6.72,22.032,-5.112));
#92183=CARTESIAN_POINT('',(-6.72,22.032,-6.936));
#92184=CARTESIAN_POINT('',(6.72,22.032,-18.552));
#92185=CARTESIAN_POINT('',(-3.06,22.032,-18.552));
#92186=CARTESIAN_POINT('',(6.72,22.032,-5.112));
#92187=CARTESIAN_POINT('',(6.72,22.032,-13.056));
#92188=CARTESIAN_POINT('',(3.06,22.032,-5.112));
#92189=CARTESIAN_POINT('',(-6.72,22.032,-1.416));
#92190=CARTESIAN_POINT('',(-6.72,22.032,6.312));
#92191=CARTESIAN_POINT('',(-6.72,22.032,-1.224));
#92192=CARTESIAN_POINT('',(-0.830275135120883,22.032,-1.416));
#92193=CARTESIAN_POINT('',(-3.06,22.032,-1.416));
#92194=CARTESIAN_POINT('',(0.830275135120883,22.032,-1.416));
#92195=CARTESIAN_POINT('Origin',(0.,22.032,-2.1216));
#92196=CARTESIAN_POINT('',(6.72,22.032,-1.416));
#92197=CARTESIAN_POINT('',(-3.06,22.032,-1.416));
#92198=CARTESIAN_POINT('',(6.72,22.032,6.312));
#92199=CARTESIAN_POINT('',(6.72,22.032,-4.488));
#92200=CARTESIAN_POINT('',(3.06,22.032,6.312));
#92201=CARTESIAN_POINT('',(3.672,22.032,-2.0112));
#92202=CARTESIAN_POINT('Origin',(3.672,22.032,-3.264));
#92203=CARTESIAN_POINT('',(-3.672,22.032,-2.0112));
#92204=CARTESIAN_POINT('Origin',(-3.672,22.032,-3.264));
#92205=CARTESIAN_POINT('Origin',(13.566,7.944,-11.208));
#92206=CARTESIAN_POINT('',(26.928,7.944,-10.608));
#92207=CARTESIAN_POINT('Origin',(27.528,7.944,-11.208));
#92208=CARTESIAN_POINT('',(13.566,7.944,-10.608));
#92209=CARTESIAN_POINT('Origin',(27.528,7.944,-11.424));
#92210=CARTESIAN_POINT('',(26.928,7.944,-11.424));
#92211=CARTESIAN_POINT('Origin',(27.528,19.9512,6.528));
#92212=CARTESIAN_POINT('',(26.928,21.432,5.41906746823804));
#92213=CARTESIAN_POINT('',(26.928,19.9512,8.378));
#92214=CARTESIAN_POINT('Origin',(26.928,19.9512,6.528));
#92215=CARTESIAN_POINT('Origin',(27.528,19.9512,8.378));
#92216=CARTESIAN_POINT('',(26.928,21.432,7.63693253176196));
#92217=CARTESIAN_POINT('Origin',(26.928,19.9512,6.528));
#92218=CARTESIAN_POINT('Ctrl Pts',(26.928,21.432,7.63693253176197));
#92219=CARTESIAN_POINT('Ctrl Pts',(26.928,21.4328877904121,7.63426595627616));
#92220=CARTESIAN_POINT('Ctrl Pts',(26.9280019704154,21.4337726990382,7.63159841831919));
#92221=CARTESIAN_POINT('Ctrl Pts',(26.9283000556252,21.501143162412,7.42777296742251));
#92222=CARTESIAN_POINT('Ctrl Pts',(26.9391026001865,21.5511743233338,7.22145350079341));
#92223=CARTESIAN_POINT('Ctrl Pts',(26.952947201541,21.6048568406253,6.84989504199634));
#92224=CARTESIAN_POINT('Ctrl Pts',(26.9571034769768,21.6166,6.68976413584999));
#92225=CARTESIAN_POINT('Ctrl Pts',(26.9571034769768,21.6166,6.36623586415001));
#92226=CARTESIAN_POINT('Ctrl Pts',(26.952947201541,21.6048568406253,6.20610495800366));
#92227=CARTESIAN_POINT('Ctrl Pts',(26.9391026001865,21.5511743233338,5.83454649920659));
#92228=CARTESIAN_POINT('Ctrl Pts',(26.9283000556252,21.501143162412,5.6282270325775));
#92229=CARTESIAN_POINT('Ctrl Pts',(26.9280019704154,21.4337726990375,5.42440158167857));
#92230=CARTESIAN_POINT('Ctrl Pts',(26.928,21.4328877904128,5.42173404372609));
#92231=CARTESIAN_POINT('Ctrl Pts',(26.928,21.432,5.41906746823803));
#92232=CARTESIAN_POINT('Origin',(27.528,21.432,-9.384));
#92233=CARTESIAN_POINT('',(26.928,21.432,-10.608));
#92234=CARTESIAN_POINT('Origin',(27.528,21.432,-11.208));
#92235=CARTESIAN_POINT('',(26.928,21.432,-9.384));
#92236=CARTESIAN_POINT('',(26.928,21.432,-9.384));
#92237=CARTESIAN_POINT('Origin',(29.784,14.688,0.59750406305912));
#92238=CARTESIAN_POINT('',(28.968,14.688,0.59750406305912));
#92239=CARTESIAN_POINT('',(29.784,14.688,0.59750406305912));
#92240=CARTESIAN_POINT('',(28.968,9.01726475149214,8.8128));
#92241=CARTESIAN_POINT('',(28.968,9.01726475149214,8.8128));
#92242=CARTESIAN_POINT('',(29.784,9.01726475149214,8.8128));
#92243=CARTESIAN_POINT('Origin',(29.184,11.2069968487015,-5.40029406097811));
#92244=CARTESIAN_POINT('',(29.184,15.3820647514921,-0.408));
#92245=CARTESIAN_POINT('Origin',(29.184,14.6530051385802,-0.408000000000001));
#92246=CARTESIAN_POINT('',(29.184,11.7007836305014,-5.74113803425587));
#92247=CARTESIAN_POINT('Origin',(29.784,15.3820647514921,-0.407999999999999));
#92248=CARTESIAN_POINT('',(28.968,15.3820647514921,-0.408));
#92249=CARTESIAN_POINT('',(29.784,15.3820647514921,-0.408));
#92250=CARTESIAN_POINT('',(28.968,21.0528,7.80729593694088));
#92251=CARTESIAN_POINT('Origin',(29.184,18.810984851675,-6.43173984076555));
#92252=CARTESIAN_POINT('',(29.184,21.0528,-8.62329593694088));
#92253=CARTESIAN_POINT('Origin',(29.184,21.0528,-9.67949768385172));
#92254=CARTESIAN_POINT('',(29.184,19.3047716334749,-6.09089586748779));
#92255=CARTESIAN_POINT('Origin',(29.784,21.0528,-8.62329593694088));
#92256=CARTESIAN_POINT('',(28.968,21.0528,-8.62329593694088));
#92257=CARTESIAN_POINT('',(29.784,21.0528,-8.62329593694088));
#92258=CARTESIAN_POINT('',(28.968,15.3820647514921,-0.408));
#92259=CARTESIAN_POINT('Origin',(29.184,13.8513676242539,-10.2288));
#92260=CARTESIAN_POINT('',(29.184,13.8513676242539,-9.6288));
#92261=CARTESIAN_POINT('',(29.7662589059854,7.8680259866208,-10.0839740133792));
#92262=CARTESIAN_POINT('Origin',(29.184,7.7232,-10.2288));
#92263=CARTESIAN_POINT('Origin',(29.184,7.94403556938437,-10.2288));
#92264=CARTESIAN_POINT('Origin',(29.784,20.3587352485079,-9.6288));
#92265=CARTESIAN_POINT('',(28.968,9.01726475149214,-9.6288));
#92266=CARTESIAN_POINT('Origin',(29.184,7.944,-13.272));
#92267=CARTESIAN_POINT('Origin',(29.184,7.944,-13.272));
#92268=CARTESIAN_POINT('Origin',(29.184,7.7232,-9.61564796847044));
#92269=CARTESIAN_POINT('Origin',(29.184,7.7232,-10.5487284530825));
#92270=CARTESIAN_POINT('',(29.184,8.3232,-9.61564796847044));
#92271=CARTESIAN_POINT('Origin',(29.184,11.0304206445356,-5.7574985449732));
#92272=CARTESIAN_POINT('Origin',(29.184,7.344,-13.272));
#92273=CARTESIAN_POINT('Origin',(29.184,21.432,-13.272));
#92274=CARTESIAN_POINT('Origin',(14.892,21.432,-13.272));
#92275=CARTESIAN_POINT('Origin',(29.184,21.432,-13.272));
#92276=CARTESIAN_POINT('Origin',(8.976,21.432,-13.272));
#92277=CARTESIAN_POINT('Origin',(29.184,21.432,-13.272));
#92278=CARTESIAN_POINT('Origin',(-7.752,8.76,9.192));
#92279=CARTESIAN_POINT('',(-14.064,8.76,9.792));
#92280=CARTESIAN_POINT('',(-7.752,8.76,9.792));
#92281=CARTESIAN_POINT('Origin',(-14.064,8.76,9.192));
#92282=CARTESIAN_POINT('Origin',(-15.504,7.344,9.792));
#92283=CARTESIAN_POINT('',(-14.064,7.944,9.792));
#92284=CARTESIAN_POINT('',(-14.064,7.344,9.792));
#92285=CARTESIAN_POINT('',(-14.064,15.72,9.792));
#92286=CARTESIAN_POINT('',(-13.158,15.72,9.792));
#92287=CARTESIAN_POINT('',(-14.064,21.432,9.792));
#92288=CARTESIAN_POINT('',(-14.064,7.344,9.792));
#92289=CARTESIAN_POINT('',(-14.904,21.432,9.792));
#92290=CARTESIAN_POINT('',(-7.752,21.432,9.792));
#92291=CARTESIAN_POINT('',(-14.904,7.944,9.792));
#92292=CARTESIAN_POINT('',(-14.904,7.344,9.792));
#92293=CARTESIAN_POINT('',(-17.238,7.944,9.792));
#92294=CARTESIAN_POINT('Origin',(-13.158,15.72,9.192));
#92295=CARTESIAN_POINT('',(-13.464,16.32,9.192));
#92296=CARTESIAN_POINT('Origin',(-14.064,15.72,9.192));
#92297=CARTESIAN_POINT('',(-13.158,16.32,9.192));
#92298=CARTESIAN_POINT('Origin',(-14.904,10.6896,-3.264));
#92299=CARTESIAN_POINT('',(-15.504,10.6896,-1.164));
#92300=CARTESIAN_POINT('Origin',(-15.504,10.6896,-3.264));
#92301=CARTESIAN_POINT('',(-14.904,10.6896,-1.764));
#92302=CARTESIAN_POINT('Origin',(-14.904,10.6896,-1.164));
#92303=CARTESIAN_POINT('Origin',(-14.904,10.6896,-3.264));
#92304=CARTESIAN_POINT('Origin',(-13.464,10.6896,-3.264));
#92305=CARTESIAN_POINT('',(-14.064,10.6896,-4.764));
#92306=CARTESIAN_POINT('',(-14.064,10.6896,-1.764));
#92307=CARTESIAN_POINT('Origin',(-14.064,10.6896,-3.264));
#92308=CARTESIAN_POINT('Origin',(-14.064,10.6896,-3.264));
#92309=CARTESIAN_POINT('',(-13.464,10.6896,-1.764));
#92310=CARTESIAN_POINT('Origin',(-15.504,7.344,-10.608));
#92311=CARTESIAN_POINT('',(-15.504,21.432,5.41906746823804));
#92312=CARTESIAN_POINT('',(-15.504,19.9512,8.378));
#92313=CARTESIAN_POINT('Origin',(-15.504,19.9512,6.528));
#92314=CARTESIAN_POINT('',(-15.504,21.432,-10.608));
#92315=CARTESIAN_POINT('',(-15.504,21.432,-9.384));
#92316=CARTESIAN_POINT('',(-15.504,7.944,-10.608));
#92317=CARTESIAN_POINT('',(-15.504,7.344,-10.608));
#92318=CARTESIAN_POINT('',(-15.504,7.944,9.192));
#92319=CARTESIAN_POINT('',(-15.504,7.944,-11.424));
#92320=CARTESIAN_POINT('',(-15.504,21.432,9.192));
#92321=CARTESIAN_POINT('',(-15.504,7.344,9.192));
#92322=CARTESIAN_POINT('',(-15.504,21.432,7.63693253176196));
#92323=CARTESIAN_POINT('',(-15.504,21.432,-9.384));
#92324=CARTESIAN_POINT('Origin',(-15.504,19.9512,6.528));
#92325=CARTESIAN_POINT('Origin',(-14.904,19.9512,6.528));
#92326=CARTESIAN_POINT('',(-14.904,19.9512,7.778));
#92327=CARTESIAN_POINT('Origin',(-14.904,19.9512,8.378));
#92328=CARTESIAN_POINT('Origin',(-14.904,19.9512,6.528));
#92329=CARTESIAN_POINT('Ctrl Pts',(-15.504,21.432,7.63693253176197));
#92330=CARTESIAN_POINT('Ctrl Pts',(-15.504,21.4328877903851,7.63426595635721));
#92331=CARTESIAN_POINT('Ctrl Pts',(-15.5039980295845,21.4337726990646,7.63159841823831));
#92332=CARTESIAN_POINT('Ctrl Pts',(-15.5036999443769,21.5011431619309,7.42777296889831));
#92333=CARTESIAN_POINT('Ctrl Pts',(-15.4928973998635,21.5511743231396,7.22145350213754));
#92334=CARTESIAN_POINT('Ctrl Pts',(-15.479052798459,21.6048568406253,6.84989504199625));
#92335=CARTESIAN_POINT('Ctrl Pts',(-15.4748965230232,21.6166,6.68976413584994));
#92336=CARTESIAN_POINT('Ctrl Pts',(-15.4748965230232,21.6166,6.36623586415006));
#92337=CARTESIAN_POINT('Ctrl Pts',(-15.479052798459,21.6048568406253,6.20610495800375));
#92338=CARTESIAN_POINT('Ctrl Pts',(-15.4928973998635,21.5511743231396,5.83454649786246));
#92339=CARTESIAN_POINT('Ctrl Pts',(-15.5036999443769,21.5011431619309,5.62822703110169));
#92340=CARTESIAN_POINT('Ctrl Pts',(-15.5039980295845,21.4337726990639,5.42440158175944));
#92341=CARTESIAN_POINT('Ctrl Pts',(-15.504,21.4328877903859,5.42173404364504));
#92342=CARTESIAN_POINT('Ctrl Pts',(-15.504,21.432,5.41906746823803));
#92343=CARTESIAN_POINT('Origin',(-14.904,21.432,-9.384));
#92344=CARTESIAN_POINT('Origin',(-14.904,21.432,9.192));
#92345=CARTESIAN_POINT('Origin',(-14.904,21.432,-11.208));
#92346=CARTESIAN_POINT('Origin',(-13.464,19.9512,6.528));
#92347=CARTESIAN_POINT('',(-14.064,19.9512,5.278));
#92348=CARTESIAN_POINT('',(-14.064,19.9512,7.778));
#92349=CARTESIAN_POINT('Origin',(-14.064,19.9512,6.528));
#92350=CARTESIAN_POINT('Origin',(-14.064,19.9512,6.528));
#92351=CARTESIAN_POINT('',(-13.464,19.9512,7.778));
#92352=CARTESIAN_POINT('Origin',(26.928,7.344,-10.608));
#92353=CARTESIAN_POINT('',(26.928,7.344,-10.608));
#92354=CARTESIAN_POINT('',(26.928,10.6896,-1.164));
#92355=CARTESIAN_POINT('Origin',(26.928,10.6896,-3.264));
#92356=CARTESIAN_POINT('Origin',(4.08,21.432,-11.208));
#92357=CARTESIAN_POINT('',(4.08,21.432,-10.608));
#92358=CARTESIAN_POINT('Origin',(8.16,7.344,-10.608));
#92359=CARTESIAN_POINT('Origin',(4.08,21.432,-11.208));
#92360=CARTESIAN_POINT('Origin',(8.376,21.432,-11.208));
#92361=CARTESIAN_POINT('Origin',(8.376,21.432,0.408000000000001));
#92362=CARTESIAN_POINT('',(8.976,21.432,8.976));
#92363=CARTESIAN_POINT('Origin',(8.376,21.432,8.976));
#92364=CARTESIAN_POINT('',(8.976,21.432,0.408000000000001));
#92365=CARTESIAN_POINT('Origin',(-8.976,8.16,8.976));
#92366=CARTESIAN_POINT('',(8.976,8.16,8.976));
#92367=CARTESIAN_POINT('Origin',(-8.376,21.432,-12.24));
#92368=CARTESIAN_POINT('',(-8.976,21.432,8.976));
#92369=CARTESIAN_POINT('Origin',(-8.376,21.432,8.976));
#92370=CARTESIAN_POINT('',(-8.976,21.432,-10.608));
#92371=CARTESIAN_POINT('Origin',(-8.376,21.432,-11.208));
#92372=CARTESIAN_POINT('',(-8.976,21.432,-12.24));
#92373=CARTESIAN_POINT('Origin',(-8.976,8.16,-16.32));
#92374=CARTESIAN_POINT('',(-8.976,16.32,-4.08));
#92375=CARTESIAN_POINT('',(-8.976,8.16,8.976));
#92376=CARTESIAN_POINT('',(-8.976,7.752,-10.608));
#92377=CARTESIAN_POINT('Origin',(-14.892,21.432,-11.208));
#92378=CARTESIAN_POINT('',(-13.464,21.432,-10.608));
#92379=CARTESIAN_POINT('Origin',(-14.064,21.432,-11.208));
#92380=CARTESIAN_POINT('',(-14.892,21.432,-10.608));
#92381=CARTESIAN_POINT('Origin',(-29.784,7.344,-10.608));
#92382=CARTESIAN_POINT('',(-13.464,7.944,-10.608));
#92383=CARTESIAN_POINT('',(-13.464,7.344,-10.608));
#92384=CARTESIAN_POINT('',(-8.76,7.944,-10.608));
#92385=CARTESIAN_POINT('',(-24.378,7.944,-10.608));
#92386=CARTESIAN_POINT('',(-8.76,7.344,-10.608));
#92387=CARTESIAN_POINT('Origin',(-14.892,21.432,-11.208));
#92388=CARTESIAN_POINT('',(-26.928,21.432,-10.608));
#92389=CARTESIAN_POINT('Origin',(-26.928,21.432,-11.208));
#92390=CARTESIAN_POINT('',(-14.892,21.432,-10.608));
#92391=CARTESIAN_POINT('Origin',(-29.784,7.344,-10.608));
#92392=CARTESIAN_POINT('',(-26.928,7.944,-10.608));
#92393=CARTESIAN_POINT('',(-26.928,7.344,-10.608));
#92394=CARTESIAN_POINT('',(-24.378,7.944,-10.608));
#92395=CARTESIAN_POINT('Origin',(3.06,21.432,-5.112));
#92396=CARTESIAN_POINT('',(6.12,21.432,-5.712));
#92397=CARTESIAN_POINT('Origin',(6.72,21.432,-5.112));
#92398=CARTESIAN_POINT('',(-6.12,21.432,-5.712));
#92399=CARTESIAN_POINT('',(3.06,21.432,-5.712));
#92400=CARTESIAN_POINT('Origin',(-6.72,21.432,-5.112));
#92401=CARTESIAN_POINT('Origin',(6.12,22.032,-5.712));
#92402=CARTESIAN_POINT('',(6.12,16.32,-5.712));
#92403=CARTESIAN_POINT('',(6.12,22.032,-5.712));
#92404=CARTESIAN_POINT('',(5.47389440891949,16.32,-5.712));
#92405=CARTESIAN_POINT('',(6.12,16.32,-5.712));
#92406=CARTESIAN_POINT('',(-5.47389440891949,16.32,-5.712));
#92407=CARTESIAN_POINT('Origin',(0.,14.688,-5.712));
#92408=CARTESIAN_POINT('',(-6.12,16.32,-5.712));
#92409=CARTESIAN_POINT('',(6.12,16.32,-5.712));
#92410=CARTESIAN_POINT('',(-6.12,22.032,-5.712));
#92411=CARTESIAN_POINT('Origin',(-3.06,21.432,-18.552));
#92412=CARTESIAN_POINT('',(-6.12,21.432,-17.952));
#92413=CARTESIAN_POINT('Origin',(-6.72,21.432,-18.552));
#92414=CARTESIAN_POINT('',(6.12,21.432,-17.952));
#92415=CARTESIAN_POINT('',(-3.06,21.432,-17.952));
#92416=CARTESIAN_POINT('Origin',(6.72,21.432,-18.552));
#92417=CARTESIAN_POINT('Origin',(-6.12,22.032,-17.952));
#92418=CARTESIAN_POINT('',(-6.12,16.32,-17.952));
#92419=CARTESIAN_POINT('',(-6.12,22.032,-17.952));
#92420=CARTESIAN_POINT('',(-5.47389440891949,16.32,-17.952));
#92421=CARTESIAN_POINT('',(-6.12,16.32,-17.952));
#92422=CARTESIAN_POINT('',(5.47389440891949,16.32,-17.952));
#92423=CARTESIAN_POINT('Origin',(0.,14.688,-17.952));
#92424=CARTESIAN_POINT('',(6.12,16.32,-17.952));
#92425=CARTESIAN_POINT('',(-6.12,16.32,-17.952));
#92426=CARTESIAN_POINT('',(6.12,22.032,-17.952));
#92427=CARTESIAN_POINT('Origin',(3.06,21.432,6.312));
#92428=CARTESIAN_POINT('',(6.12,21.432,5.712));
#92429=CARTESIAN_POINT('Origin',(6.72,21.432,6.312));
#92430=CARTESIAN_POINT('',(-6.12,21.432,5.712));
#92431=CARTESIAN_POINT('',(3.06,21.432,5.712));
#92432=CARTESIAN_POINT('Origin',(-6.72,21.432,6.312));
#92433=CARTESIAN_POINT('Origin',(6.12,22.032,5.712));
#92434=CARTESIAN_POINT('',(6.12,16.32,5.712));
#92435=CARTESIAN_POINT('',(6.12,22.032,5.712));
#92436=CARTESIAN_POINT('',(5.47389440891949,16.32,5.712));
#92437=CARTESIAN_POINT('',(6.12,16.32,5.712));
#92438=CARTESIAN_POINT('',(-5.47389440891949,16.32,5.712));
#92439=CARTESIAN_POINT('Origin',(0.,14.688,5.712));
#92440=CARTESIAN_POINT('',(-6.12,16.32,5.712));
#92441=CARTESIAN_POINT('',(6.12,16.32,5.712));
#92442=CARTESIAN_POINT('',(-6.12,22.032,5.712));
#92443=CARTESIAN_POINT('Origin',(-3.06,21.432,-1.416));
#92444=CARTESIAN_POINT('',(-1.07003852625037E-16,22.0004505255517,-1.224));
#92445=CARTESIAN_POINT('Ctrl Pts',(0.830275135120883,22.032,-1.416));
#92446=CARTESIAN_POINT('Ctrl Pts',(0.828552577377265,22.032,-1.4152033217116));
#92447=CARTESIAN_POINT('Ctrl Pts',(0.826829075614662,22.0319984132633,-1.41440868610083));
#92448=CARTESIAN_POINT('Ctrl Pts',(0.70474528426719,22.0317754702238,-1.35829688696515));
#92449=CARTESIAN_POINT('Ctrl Pts',(0.580104214213408,22.024045489527,-1.31311205364223));
#92450=CARTESIAN_POINT('Ctrl Pts',(0.30409125108285,22.0079879748714,-1.24371396306971));
#92451=CARTESIAN_POINT('Ctrl Pts',(0.153641828682257,22.0004505255517,-1.224));
#92452=CARTESIAN_POINT('Ctrl Pts',(6.93889390390723E-17,22.0004505255517,
-1.224));
#92453=CARTESIAN_POINT('Ctrl Pts',(-1.04083408558608E-16,22.0004505255517,
-1.224));
#92454=CARTESIAN_POINT('Ctrl Pts',(-0.153641828682253,22.0004505255517,
-1.224));
#92455=CARTESIAN_POINT('Ctrl Pts',(-0.304091251082843,22.0079879748714,
-1.24371396306971));
#92456=CARTESIAN_POINT('Ctrl Pts',(-0.580104214214111,22.024045489527,-1.31311205364241));
#92457=CARTESIAN_POINT('Ctrl Pts',(-0.704745284267943,22.0317754702238,
-1.35829688696549));
#92458=CARTESIAN_POINT('Ctrl Pts',(-0.826829075614615,22.0319984132633,
-1.41440868610081));
#92459=CARTESIAN_POINT('Ctrl Pts',(-0.828552577377312,22.032,-1.41520332171162));
#92460=CARTESIAN_POINT('Ctrl Pts',(-0.830275135120883,22.032,-1.416));
#92461=CARTESIAN_POINT('',(-6.12,21.432,-0.816));
#92462=CARTESIAN_POINT('Origin',(-6.72,21.432,-1.416));
#92463=CARTESIAN_POINT('',(6.12,21.432,-0.816));
#92464=CARTESIAN_POINT('',(-3.06,21.432,-0.816));
#92465=CARTESIAN_POINT('Origin',(6.72,21.432,-1.416));
#92466=CARTESIAN_POINT('Origin',(-6.12,22.032,-0.816));
#92467=CARTESIAN_POINT('',(-6.12,16.32,-0.816));
#92468=CARTESIAN_POINT('',(-6.12,22.032,-0.816));
#92469=CARTESIAN_POINT('',(-5.47389440891949,16.32,-0.815999999999999));
#92470=CARTESIAN_POINT('',(-6.12,16.32,-0.816));
#92471=CARTESIAN_POINT('',(5.47389440891949,16.32,-0.815999999999999));
#92472=CARTESIAN_POINT('Origin',(0.,14.688,-0.815999999999999));
#92473=CARTESIAN_POINT('',(6.12,16.32,-0.816));
#92474=CARTESIAN_POINT('',(-6.12,16.32,-0.816));
#92475=CARTESIAN_POINT('',(6.12,22.032,-0.816));
#92476=CARTESIAN_POINT('Origin',(0.,21.432,-2.1216));
#92477=CARTESIAN_POINT('',(-5.99587072862544E-17,21.432,-1.632));
#92478=CARTESIAN_POINT('Origin',(-1.33437515235096E-16,21.432,-1.032));
#92479=CARTESIAN_POINT('',(-0.4896,21.432,-2.1216));
#92480=CARTESIAN_POINT('Origin',(0.,21.432,-2.1216));
#92481=CARTESIAN_POINT('Origin',(0.,21.432,-2.1216));
#92482=CARTESIAN_POINT('Origin',(-6.72,21.432,-1.224));
#92483=CARTESIAN_POINT('',(-6.12,21.432,-1.224));
#92484=CARTESIAN_POINT('Origin',(-6.12,22.032,5.712));
#92485=CARTESIAN_POINT('',(-6.12,16.32,5.712));
#92486=CARTESIAN_POINT('Origin',(6.72,21.432,-4.488));
#92487=CARTESIAN_POINT('',(6.12,21.432,-4.488));
#92488=CARTESIAN_POINT('Origin',(6.12,22.032,-0.816));
#92489=CARTESIAN_POINT('',(6.12,16.32,-0.816));
#92490=CARTESIAN_POINT('Origin',(-6.72,21.432,-6.936));
#92491=CARTESIAN_POINT('',(-6.12,21.432,-6.936));
#92492=CARTESIAN_POINT('Origin',(-6.12,22.032,-5.712));
#92493=CARTESIAN_POINT('',(-6.12,16.32,-5.712));
#92494=CARTESIAN_POINT('Origin',(6.72,21.432,-13.056));
#92495=CARTESIAN_POINT('',(6.12,21.432,-13.056));
#92496=CARTESIAN_POINT('Origin',(6.12,22.032,-17.952));
#92497=CARTESIAN_POINT('',(6.12,16.32,-17.952));
#92498=CARTESIAN_POINT('Origin',(-3.672,21.432,-3.264));
#92499=CARTESIAN_POINT('',(-3.672,21.432,-2.6112));
#92500=CARTESIAN_POINT('Origin',(-3.672,21.432,-2.0112));
#92501=CARTESIAN_POINT('',(-4.3248,21.432,-3.264));
#92502=CARTESIAN_POINT('Origin',(-3.672,21.432,-3.264));
#92503=CARTESIAN_POINT('Origin',(-3.672,21.432,-3.264));
#92504=CARTESIAN_POINT('Origin',(-3.672,22.032,-3.264));
#92505=CARTESIAN_POINT('',(-4.3248,20.808,-3.264));
#92506=CARTESIAN_POINT('',(-4.3248,22.032,-3.264));
#92507=CARTESIAN_POINT('Origin',(-3.672,20.808,-3.264));
#92508=CARTESIAN_POINT('Origin',(3.672,21.432,-3.264));
#92509=CARTESIAN_POINT('',(3.672,21.432,-2.6112));
#92510=CARTESIAN_POINT('Origin',(3.672,21.432,-2.0112));
#92511=CARTESIAN_POINT('',(3.0192,21.432,-3.264));
#92512=CARTESIAN_POINT('Origin',(3.672,21.432,-3.264));
#92513=CARTESIAN_POINT('Origin',(3.672,21.432,-3.264));
#92514=CARTESIAN_POINT('Origin',(3.672,22.032,-3.264));
#92515=CARTESIAN_POINT('',(3.0192,20.808,-3.264));
#92516=CARTESIAN_POINT('',(3.0192,22.032,-3.264));
#92517=CARTESIAN_POINT('Origin',(3.672,20.808,-3.264));
#92518=CARTESIAN_POINT('Origin',(0.,22.032,-2.1216));
#92519=CARTESIAN_POINT('',(-0.4896,20.808,-2.1216));
#92520=CARTESIAN_POINT('',(-0.4896,22.032,-2.1216));
#92521=CARTESIAN_POINT('Origin',(0.,20.808,-2.1216));
#92522=CARTESIAN_POINT('Origin',(-4.896,21.432,-21.216));
#92523=CARTESIAN_POINT('',(-3.45144894062868,21.7056,-19.775558318824));
#92524=CARTESIAN_POINT('Origin',(-4.896,21.7056,-21.216));
#92525=CARTESIAN_POINT('Origin',(-3.07332505037306,21.432,-19.3985100942983));
#92526=CARTESIAN_POINT('Origin',(-14.064,19.9512,6.528));
#92527=CARTESIAN_POINT('',(-13.464,21.432,7.63693253176196));
#92528=CARTESIAN_POINT('',(-13.464,19.9512,4.678));
#92529=CARTESIAN_POINT('Origin',(-13.464,19.9512,6.528));
#92530=CARTESIAN_POINT('Origin',(-14.064,19.9512,4.678));
#92531=CARTESIAN_POINT('',(-13.464,21.432,5.41906746823804));
#92532=CARTESIAN_POINT('Origin',(-13.464,19.9512,6.528));
#92533=CARTESIAN_POINT('Ctrl Pts',(-13.464,21.432,5.41906746823803));
#92534=CARTESIAN_POINT('Ctrl Pts',(-13.464,21.4328877903851,5.42173404364279));
#92535=CARTESIAN_POINT('Ctrl Pts',(-13.4640019704155,21.4337726990646,5.42440158176169));
#92536=CARTESIAN_POINT('Ctrl Pts',(-13.4643000556231,21.5011431619309,5.62822703110169));
#92537=CARTESIAN_POINT('Ctrl Pts',(-13.4751026001365,21.5511743231396,5.83454649786246));
#92538=CARTESIAN_POINT('Ctrl Pts',(-13.488947201541,21.6048568406253,6.20610495800375));
#92539=CARTESIAN_POINT('Ctrl Pts',(-13.4931034769768,21.6166,6.36623586415006));
#92540=CARTESIAN_POINT('Ctrl Pts',(-13.4931034769768,21.6166,6.68976413584994));
#92541=CARTESIAN_POINT('Ctrl Pts',(-13.488947201541,21.6048568406253,6.84989504199625));
#92542=CARTESIAN_POINT('Ctrl Pts',(-13.4751026001365,21.5511743231396,7.22145350213754));
#92543=CARTESIAN_POINT('Ctrl Pts',(-13.4643000556231,21.5011431619309,7.42777296889831));
#92544=CARTESIAN_POINT('Ctrl Pts',(-13.4640019704155,21.4337726990639,7.63159841824056));
#92545=CARTESIAN_POINT('Ctrl Pts',(-13.464,21.4328877903859,7.63426595635496));
#92546=CARTESIAN_POINT('Ctrl Pts',(-13.464,21.432,7.63693253176197));
#92547=CARTESIAN_POINT('Origin',(-14.064,21.432,0.816000000000001));
#92548=CARTESIAN_POINT('',(-13.464,21.432,0.816000000000001));
#92549=CARTESIAN_POINT('',(-13.464,21.432,9.192));
#92550=CARTESIAN_POINT('Origin',(-14.064,21.432,9.192));
#92551=CARTESIAN_POINT('',(-13.464,21.432,0.816000000000001));
#92552=CARTESIAN_POINT('Origin',(-14.064,10.6896,-3.264));
#92553=CARTESIAN_POINT('',(-13.464,10.6896,-5.364));
#92554=CARTESIAN_POINT('Origin',(-13.464,10.6896,-3.264));
#92555=CARTESIAN_POINT('Origin',(-14.064,10.6896,-5.364));
#92556=CARTESIAN_POINT('Origin',(-13.464,7.344,9.792));
#92557=CARTESIAN_POINT('',(-13.464,7.344,9.192));
#92558=CARTESIAN_POINT('',(-13.464,16.32,8.976));
#92559=CARTESIAN_POINT('',(-13.464,7.944,9.192));
#92560=CARTESIAN_POINT('',(-13.464,7.344,9.192));
#92561=CARTESIAN_POINT('',(-13.464,7.944,-1.224));
#92562=CARTESIAN_POINT('Origin',(-7.752,21.432,9.192));
#92563=CARTESIAN_POINT('Origin',(-14.904,21.432,9.192));
#92564=CARTESIAN_POINT('Origin',(-14.064,21.432,9.192));
#92565=CARTESIAN_POINT('Origin',(-14.064,7.344,9.192));
#92566=CARTESIAN_POINT('Origin',(-14.064,21.432,9.192));
#92567=CARTESIAN_POINT('Origin',(-14.064,21.432,9.192));
#92568=CARTESIAN_POINT('Origin',(-14.904,21.432,9.192));
#92569=CARTESIAN_POINT('Origin',(-14.904,21.432,9.192));
#92570=CARTESIAN_POINT('Origin',(-14.904,7.344,9.192));
#92571=CARTESIAN_POINT('Origin',(-14.904,7.944,9.192));
#92572=CARTESIAN_POINT('Origin',(-14.064,7.944,-1.224));
#92573=CARTESIAN_POINT('',(-14.064,7.344,9.192));
#92574=CARTESIAN_POINT('Origin',(-14.064,7.944,9.192));
#92575=CARTESIAN_POINT('',(-14.064,7.344,-11.208));
#92576=CARTESIAN_POINT('',(-14.064,7.344,-1.224));
#92577=CARTESIAN_POINT('Origin',(-14.064,7.944,-11.208));
#92578=CARTESIAN_POINT('Origin',(-14.064,7.344,9.192));
#92579=CARTESIAN_POINT('Origin',(-14.064,7.944,9.192));
#92580=CARTESIAN_POINT('Origin',(-14.064,7.944,9.192));
#92581=CARTESIAN_POINT('Origin',(-14.064,7.944,9.192));
#92582=CARTESIAN_POINT('Origin',(-18.972,7.344,-12.24));
#92583=CARTESIAN_POINT('',(-8.76,7.344,-11.208));
#92584=CARTESIAN_POINT('',(-24.378,7.344,-11.208));
#92585=CARTESIAN_POINT('',(-14.904,7.344,9.192));
#92586=CARTESIAN_POINT('',(-17.238,7.344,9.192));
#92587=CARTESIAN_POINT('',(-14.904,7.344,-11.208));
#92588=CARTESIAN_POINT('',(-14.904,7.344,-11.424));
#92589=CARTESIAN_POINT('',(-26.928,7.344,-11.208));
#92590=CARTESIAN_POINT('',(-24.378,7.344,-11.208));
#92591=CARTESIAN_POINT('',(-26.928,7.344,9.192));
#92592=CARTESIAN_POINT('',(-26.928,7.344,-10.608));
#92593=CARTESIAN_POINT('',(-27.528,7.344,9.792));
#92594=CARTESIAN_POINT('Origin',(-27.528,7.344,9.192));
#92595=CARTESIAN_POINT('',(-29.184,7.344,9.792));
#92596=CARTESIAN_POINT('',(-26.928,7.344,9.792));
#92597=CARTESIAN_POINT('',(-29.184,7.344,-13.272));
#92598=CARTESIAN_POINT('',(-29.184,7.344,-13.056));
#92599=CARTESIAN_POINT('',(-8.76,7.344,-13.272));
#92600=CARTESIAN_POINT('',(-13.566,7.344,-13.272));
#92601=CARTESIAN_POINT('',(-8.76,7.344,-11.424));
#92602=CARTESIAN_POINT('Origin',(-17.238,7.944,9.192));
#92603=CARTESIAN_POINT('Origin',(-14.904,7.944,9.192));
#92604=CARTESIAN_POINT('Origin',(-8.76,7.344,-13.272));
#92605=CARTESIAN_POINT('',(-8.16,7.944,-13.272));
#92606=CARTESIAN_POINT('',(-8.76,7.944,-13.872));
#92607=CARTESIAN_POINT('Origin',(-8.76,7.944,-13.272));
#92608=CARTESIAN_POINT('',(-8.76,7.344,-13.872));
#92609=CARTESIAN_POINT('',(-8.16,7.344,-13.272));
#92610=CARTESIAN_POINT('Origin',(-8.76,7.944,-11.424));
#92611=CARTESIAN_POINT('Origin',(-8.76,7.944,-13.272));
#92612=CARTESIAN_POINT('',(-8.16,7.944,-11.208));
#92613=CARTESIAN_POINT('',(-8.16,7.944,-11.424));
#92614=CARTESIAN_POINT('Origin',(-8.76,7.944,-11.208));
#92615=CARTESIAN_POINT('Origin',(-8.76,7.344,-11.208));
#92616=CARTESIAN_POINT('Origin',(-8.76,7.944,-11.208));
#92617=CARTESIAN_POINT('',(-8.16,7.344,-11.208));
#92618=CARTESIAN_POINT('Origin',(-8.76,7.944,-11.208));
#92619=CARTESIAN_POINT('Origin',(-8.76,7.944,-11.208));
#92620=CARTESIAN_POINT('Origin',(-8.76,7.944,-13.272));
#92621=CARTESIAN_POINT('Origin',(-8.76,7.944,-13.272));
#92622=CARTESIAN_POINT('Origin',(-8.16,7.344,-13.872));
#92623=CARTESIAN_POINT('',(-29.184,7.944,-13.872));
#92624=CARTESIAN_POINT('',(-13.566,7.944,-13.872));
#92625=CARTESIAN_POINT('',(-29.184,21.432,-13.872));
#92626=CARTESIAN_POINT('',(-29.184,7.344,-13.872));
#92627=CARTESIAN_POINT('',(-4.08,21.432,-13.872));
#92628=CARTESIAN_POINT('Origin',(-13.566,7.944,-13.272));
#92629=CARTESIAN_POINT('Origin',(-29.184,7.944,-13.272));
#92630=CARTESIAN_POINT('Origin',(-24.378,7.944,-11.208));
#92631=CARTESIAN_POINT('Origin',(-14.904,7.944,-11.424));
#92632=CARTESIAN_POINT('Origin',(-14.904,7.944,9.192));
#92633=CARTESIAN_POINT('Origin',(-14.904,7.944,-11.208));
#92634=CARTESIAN_POINT('Origin',(-14.904,7.944,9.192));
#92635=CARTESIAN_POINT('Origin',(-27.528,19.9512,6.528));
#92636=CARTESIAN_POINT('',(-26.928,19.9512,4.678));
#92637=CARTESIAN_POINT('Origin',(-26.928,19.9512,6.528));
#92638=CARTESIAN_POINT('',(-27.528,19.9512,5.278));
#92639=CARTESIAN_POINT('Origin',(-27.528,19.9512,4.678));
#92640=CARTESIAN_POINT('',(-27.528,19.9512,7.778));
#92641=CARTESIAN_POINT('Origin',(-27.528,19.9512,6.528));
#92642=CARTESIAN_POINT('Origin',(-27.528,19.9512,6.528));
#92643=CARTESIAN_POINT('Origin',(-13.464,19.9512,6.528));
#92644=CARTESIAN_POINT('',(-29.6730897616957,19.9512000004902,7.778));
#92645=CARTESIAN_POINT('',(-13.464,19.9512,7.778));
#92646=CARTESIAN_POINT('',(-29.784,20.3324059608682,7.71845454150864));
#92647=CARTESIAN_POINT('Ctrl Pts',(-29.784,20.3324059608683,7.71845454150862));
#92648=CARTESIAN_POINT('Ctrl Pts',(-29.784,20.2498877771073,7.74487841779528));
#92649=CARTESIAN_POINT('Ctrl Pts',(-29.7660314239133,20.1601533655831,7.76339914860449));
#92650=CARTESIAN_POINT('Ctrl Pts',(-29.7162857661367,20.0320859161528,7.77611545312242));
#92651=CARTESIAN_POINT('Ctrl Pts',(-29.6960587249165,19.9904757157273,7.77799999996919));
#92652=CARTESIAN_POINT('Ctrl Pts',(-29.6730897616957,19.9512000009805,7.778));
#92653=CARTESIAN_POINT('',(-29.784,20.8019222240139,7.44384479993544));
#92654=CARTESIAN_POINT('Origin',(-29.784,19.9512,6.528));
#92655=CARTESIAN_POINT('',(-28.968,20.8019222240139,7.44384479993544));
#92656=CARTESIAN_POINT('',(-13.464,20.8019222240139,7.44384479993544));
#92657=CARTESIAN_POINT('',(-28.968,21.0528,7.11874312522449));
#92658=CARTESIAN_POINT('Origin',(-28.968,19.9512,6.528));
#92659=CARTESIAN_POINT('',(-29.784,21.0528,7.11874312522449));
#92660=CARTESIAN_POINT('',(-13.464,21.0528,7.11874312522449));
#92661=CARTESIAN_POINT('',(-29.784,21.2011648366643,6.5186241212227));
#92662=CARTESIAN_POINT('Origin',(-29.784,19.9512,6.528));
#92663=CARTESIAN_POINT('',(-29.184,21.0528,5.93725687477551));
#92664=CARTESIAN_POINT('Ctrl Pts',(-29.184,21.0528,5.93725687477551));
#92665=CARTESIAN_POINT('Ctrl Pts',(-29.1843643716593,21.0528,5.93725687477551));
#92666=CARTESIAN_POINT('Ctrl Pts',(-29.1847287348529,21.0528001568623,5.93725716728446));
#92667=CARTESIAN_POINT('Ctrl Pts',(-29.1850930927556,21.0528004705669,5.93725775227563));
#92668=CARTESIAN_POINT('Ctrl Pts',(-29.1854574506584,21.0528007842715,5.93725833726681));
#92669=CARTESIAN_POINT('Ctrl Pts',(-29.1858218032704,21.0528012548157,5.93725921473157));
#92670=CARTESIAN_POINT('Ctrl Pts',(-29.1861861682784,21.0528018822333,5.9372603847344));
#92671=CARTESIAN_POINT('Ctrl Pts',(-29.1869148982942,21.0528031370684,5.93726272474006));
#92672=CARTESIAN_POINT('Ctrl Pts',(-29.1876437020802,21.0528050195554,5.93726623516292));
#92673=CARTESIAN_POINT('Ctrl Pts',(-29.1883724308858,21.0528075292884,5.93727091538062));
#92674=CARTESIAN_POINT('Ctrl Pts',(-29.2140257893958,21.0528958791364,5.93743567255998));
#92675=CARTESIAN_POINT('Ctrl Pts',(-29.2395868437148,21.0537649140596,5.93904973301454));
#92676=CARTESIAN_POINT('Ctrl Pts',(-29.2648654234066,21.0553765973136,5.9420869196893));
#92677=CARTESIAN_POINT('Ctrl Pts',(-29.2911930452573,21.0570551642177,5.94525014734044));
#92678=CARTESIAN_POINT('Ctrl Pts',(-29.317214696756,21.059538683867,5.94995587684859));
#92679=CARTESIAN_POINT('Ctrl Pts',(-29.3427576953088,21.06274486309,5.95618814364165));
#92680=CARTESIAN_POINT('Ctrl Pts',(-29.3701245988851,21.0661799804457,5.96286542720468));
#92681=CARTESIAN_POINT('Ctrl Pts',(-29.3969434897638,21.0704443645938,5.97129396545307));
#92682=CARTESIAN_POINT('Ctrl Pts',(-29.4230353027292,21.0754000536626,5.9814884852252));
#92683=CARTESIAN_POINT('Ctrl Pts',(-29.436375271561,21.0779337502595,5.98670064032517));
#92684=CARTESIAN_POINT('Ctrl Pts',(-29.4495255641454,21.0806476187178,5.99237507558155));
#92685=CARTESIAN_POINT('Ctrl Pts',(-29.4624629247498,21.0835199890972,5.99851776017422));
#92686=CARTESIAN_POINT('Ctrl Pts',(-29.491900288897,21.0900557126817,6.01249467932527));
#92687=CARTESIAN_POINT('Ctrl Pts',(-29.5199069050774,21.0973412988018,6.02874058300624));
#92688=CARTESIAN_POINT('Ctrl Pts',(-29.546232223272,21.1050194431494,6.04716462401558));
#92689=CARTESIAN_POINT('Ctrl Pts',(-29.5761900183259,21.113757049778,6.06813089080651));
#92690=CARTESIAN_POINT('Ctrl Pts',(-29.6039758940397,21.123003229535,6.09192107855449));
#92691=CARTESIAN_POINT('Ctrl Pts',(-29.6292361556442,21.1321942394425,6.11842373510109));
#92692=CARTESIAN_POINT('Ctrl Pts',(-29.6318717651081,21.1331532125946,6.12118897377937));
#92693=CARTESIAN_POINT('Ctrl Pts',(-29.634479847044,21.1341115517782,6.12398372285587));
#92694=CARTESIAN_POINT('Ctrl Pts',(-29.637059970908,21.1350685929626,6.12680783333075));
#92695=CARTESIAN_POINT('Ctrl Pts',(-29.6606845986466,21.1438316380342,6.15266649833204));
#92696=CARTESIAN_POINT('Ctrl Pts',(-29.6816748166557,21.1523727019991,6.18066728533513));
#92697=CARTESIAN_POINT('Ctrl Pts',(-29.6998946563564,21.1602188363698,6.21055018568484));
#92698=CARTESIAN_POINT('Ctrl Pts',(-29.7145933027143,21.1665486151322,6.23465787222898));
#92699=CARTESIAN_POINT('Ctrl Pts',(-29.727488936724,21.1724272487578,6.25999254756523));
#92700=CARTESIAN_POINT('Ctrl Pts',(-29.7384895609047,21.1776282813931,6.28639364956891));
#92701=CARTESIAN_POINT('Ctrl Pts',(-29.7411248596723,21.1788742356833,6.29271827173847));
#92702=CARTESIAN_POINT('Ctrl Pts',(-29.7436513097999,21.1800813857086,6.2991039028086));
#92703=CARTESIAN_POINT('Ctrl Pts',(-29.74606747585,21.1812467758105,6.30554791680398));
#92704=CARTESIAN_POINT('Ctrl Pts',(-29.7558166581436,21.1859491018555,6.33154938600753));
#92705=CARTESIAN_POINT('Ctrl Pts',(-29.7636632911079,21.1899142199256,6.35820864735865));
#92706=CARTESIAN_POINT('Ctrl Pts',(-29.7696422788167,21.1930311323737,6.38535410754034));
#92707=CARTESIAN_POINT('Ctrl Pts',(-29.7754622120256,21.1960651279512,6.41177743752124));
#92708=CARTESIAN_POINT('Ctrl Pts',(-29.7795115673198,21.1982958942782,6.43866313565451));
#92709=CARTESIAN_POINT('Ctrl Pts',(-29.7817936299994,21.1996502871013,6.46582876709134));
#92710=CARTESIAN_POINT('Ctrl Pts',(-29.7832639221287,21.2005228981499,6.48333109708591));
#92711=CARTESIAN_POINT('Ctrl Pts',(-29.784,21.2010322571302,6.50094900407838));
#92712=CARTESIAN_POINT('Ctrl Pts',(-29.784,21.2011648366643,6.51862412122269));
#92713=CARTESIAN_POINT('',(-28.968,21.0528,5.93725687477551));
#92714=CARTESIAN_POINT('',(-13.464,21.0528,5.93725687477551));
#92715=CARTESIAN_POINT('',(-28.968,19.3965172404536,5.40780937503389));
#92716=CARTESIAN_POINT('Origin',(-28.968,19.9512,6.528));
#92717=CARTESIAN_POINT('',(-29.184,19.3965172404536,5.40780937503389));
#92718=CARTESIAN_POINT('',(-13.464,19.3965172404536,5.40780937503389));
#92719=CARTESIAN_POINT('',(-29.7833084014095,18.9547400881553,5.77330294456311));
#92720=CARTESIAN_POINT('Ctrl Pts',(-29.7833084013013,18.9547400885983,5.77330294490483));
#92721=CARTESIAN_POINT('Ctrl Pts',(-29.780236728844,18.9953746586557,5.71965132428977));
#92722=CARTESIAN_POINT('Ctrl Pts',(-29.7661621997996,19.0422228222755,5.66748165925228));
#92723=CARTESIAN_POINT('Ctrl Pts',(-29.7101860638315,19.1436049154608,5.57097131021595));
#92724=CARTESIAN_POINT('Ctrl Pts',(-29.664083283762,19.1980745167137,5.52887551744315));
#92725=CARTESIAN_POINT('Ctrl Pts',(-29.5569063007166,19.2872387664837,5.46754555210684));
#92726=CARTESIAN_POINT('Ctrl Pts',(-29.4892209293256,19.327765216772,5.4441184609697));
#92727=CARTESIAN_POINT('Ctrl Pts',(-29.3407268100904,19.3825207083351,5.41441389821227));
#92728=CARTESIAN_POINT('Ctrl Pts',(-29.259898021901,19.3965172404535,5.4078093750339));
#92729=CARTESIAN_POINT('Ctrl Pts',(-29.184,19.3965172404535,5.4078093750339));
#92730=CARTESIAN_POINT('',(-29.184,18.7060084170374,6.41846497492097));
#92731=CARTESIAN_POINT('Ctrl Pts',(-29.184,18.7060084170374,6.41846497492091));
#92732=CARTESIAN_POINT('Ctrl Pts',(-29.2236153010039,18.7060084170374,6.41846497492091));
#92733=CARTESIAN_POINT('Ctrl Pts',(-29.2633091750366,18.7065151598125,6.41221228695973));
#92734=CARTESIAN_POINT('Ctrl Pts',(-29.3404403169687,18.7089486562131,6.38854540292828));
#92735=CARTESIAN_POINT('Ctrl Pts',(-29.3778828026048,18.7108927130172,6.37114999797291));
#92736=CARTESIAN_POINT('Ctrl Pts',(-29.4840885147569,18.7201044508453,6.30718343562169));
#92737=CARTESIAN_POINT('Ctrl Pts',(-29.5468609707651,18.7312561019511,6.2486788128922));
#92738=CARTESIAN_POINT('Ctrl Pts',(-29.6514157141007,18.7661319382575,6.1247154358701));
#92739=CARTESIAN_POINT('Ctrl Pts',(-29.6996533413331,18.7937050469554,6.04833557739996));
#92740=CARTESIAN_POINT('Ctrl Pts',(-29.7621956886305,18.8657461678681,5.9034546521282));
#92741=CARTESIAN_POINT('Ctrl Pts',(-29.7797742106915,18.9079869437835,5.83503319047208));
#92742=CARTESIAN_POINT('Ctrl Pts',(-29.7833084015176,18.9547400885983,5.77330294490483));
#92743=CARTESIAN_POINT('',(-28.968,18.7060084170374,6.41846497492097));
#92744=CARTESIAN_POINT('',(-13.464,18.7060084170374,6.41846497492097));
#92745=CARTESIAN_POINT('',(-28.968,19.6120909823364,7.73112305029005));
#92746=CARTESIAN_POINT('Origin',(-28.968,19.9512,6.528));
#92747=CARTESIAN_POINT('',(-29.184,19.6120909823364,7.73112305029005));
#92748=CARTESIAN_POINT('',(-13.464,19.6120909823364,7.73112305029005));
#92749=CARTESIAN_POINT('Ctrl Pts',(-29.6730897616957,19.9512000009805,7.778));
#92750=CARTESIAN_POINT('Ctrl Pts',(-29.6500156297378,19.9117444532444,7.77800000003095));
#92751=CARTESIAN_POINT('Ctrl Pts',(-29.6241709396688,19.8746468475679,7.77610895998165));
#92752=CARTESIAN_POINT('Ctrl Pts',(-29.5468609707651,19.779797513811,7.76771957622778));
#92753=CARTESIAN_POINT('Ctrl Pts',(-29.4840885147569,19.7211400971072,7.75740174366776));
#92754=CARTESIAN_POINT('Ctrl Pts',(-29.3778828026048,19.6580635030103,7.74333332193733));
#92755=CARTESIAN_POINT('Ctrl Pts',(-29.3404403169687,19.6411090544722,7.73898290297035));
#92756=CARTESIAN_POINT('Ctrl Pts',(-29.2633091750366,19.6181170767952,7.73286634617826));
#92757=CARTESIAN_POINT('Ctrl Pts',(-29.2236153010039,19.6120909823365,7.73112305029007));
#92758=CARTESIAN_POINT('Ctrl Pts',(-29.184,19.6120909823365,7.73112305029007));
#92759=CARTESIAN_POINT('Origin',(-26.928,7.344,9.792));
#92760=CARTESIAN_POINT('',(-26.928,7.344,9.192));
#92761=CARTESIAN_POINT('Origin',(-26.928,7.944,-11.208));
#92762=CARTESIAN_POINT('',(-26.928,10.6896,-5.364));
#92763=CARTESIAN_POINT('Origin',(-26.928,10.6896,-3.264));
#92764=CARTESIAN_POINT('Origin',(-24.378,7.944,-11.208));
#92765=CARTESIAN_POINT('Origin',(-8.16,7.344,-10.608));
#92766=CARTESIAN_POINT('Origin',(-29.184,10.6144737596866,-6.36008826276735));
#92767=CARTESIAN_POINT('',(-29.7835166971462,21.456077579674,9.38872242032599));
#92768=CARTESIAN_POINT('',(-29.784,21.432,9.31145616230212));
#92769=CARTESIAN_POINT('Origin',(-29.184,21.432,9.31145616230212));
#92770=CARTESIAN_POINT('',(-29.784,10.6144737596866,-6.36008826276735));
#92771=CARTESIAN_POINT('',(-29.184,20.3587352485079,8.8128));
#92772=CARTESIAN_POINT('',(-29.184,10.1206869778867,-6.01924428948959));
#92773=CARTESIAN_POINT('Origin',(-29.184,21.5019541534552,9.4128));
#92774=CARTESIAN_POINT('Origin',(-29.784,14.688,0.59750406305912));
#92775=CARTESIAN_POINT('',(-28.968,20.3587352485079,8.8128));
#92776=CARTESIAN_POINT('',(-28.968,14.688,0.59750406305912));
#92777=CARTESIAN_POINT('',(-29.784,20.3587352485079,8.8128));
#92778=CARTESIAN_POINT('Origin',(-29.784,7.344,-13.872));
#92779=CARTESIAN_POINT('',(-29.784,21.432,6.4022379066467));
#92780=CARTESIAN_POINT('',(-29.784,21.432,-11.016));
#92781=CARTESIAN_POINT('Origin',(-29.784,21.0528,5.93725687477551));
#92782=CARTESIAN_POINT('',(-29.784,21.0528,7.80729593694088));
#92783=CARTESIAN_POINT('',(-29.784,21.0528,-11.2476479684704));
#92784=CARTESIAN_POINT('',(-29.784,13.7731719941602,-2.73883181510914));
#92785=CARTESIAN_POINT('Origin',(-29.784,7.344,-13.872));
#92786=CARTESIAN_POINT('',(-29.784,21.432,9.4128));
#92787=CARTESIAN_POINT('',(-29.784,7.944,9.4128));
#92788=CARTESIAN_POINT('',(-29.784,13.8513676242539,9.4128));
#92789=CARTESIAN_POINT('',(-29.784,7.944,9.792));
#92790=CARTESIAN_POINT('',(-29.784,7.944,-13.056));
#92791=CARTESIAN_POINT('',(-29.784,21.432,9.792));
#92792=CARTESIAN_POINT('',(-29.784,7.344,9.792));
#92793=CARTESIAN_POINT('',(-29.784,21.432,-11.016));
#92794=CARTESIAN_POINT('Origin',(-29.184,8.18063237574607,-10.2288));
#92795=CARTESIAN_POINT('',(-29.7835166971462,21.456077579674,-10.204722420326));
#92796=CARTESIAN_POINT('',(-29.784,21.432,-10.2288));
#92797=CARTESIAN_POINT('Origin',(-29.184,21.432,-10.2288));
#92798=CARTESIAN_POINT('',(-29.784,7.944,-10.2288));
#92799=CARTESIAN_POINT('',(-29.784,8.18063237574607,-10.2288));
#92800=CARTESIAN_POINT('',(-29.7835166971462,7.91992242032599,-10.204722420326));
#92801=CARTESIAN_POINT('Origin',(-29.184,7.944,-10.2288));
#92802=CARTESIAN_POINT('',(-29.184,9.01726475149214,-9.6288));
#92803=CARTESIAN_POINT('Origin',(-29.184,7.87404584654483,-10.2288));
#92804=CARTESIAN_POINT('',(-29.184,20.3587352485079,-9.6288));
#92805=CARTESIAN_POINT('',(-29.184,8.18063237574607,-9.6288));
#92806=CARTESIAN_POINT('Origin',(-29.184,21.5019541534552,-10.2288));
#92807=CARTESIAN_POINT('Origin',(-29.184,7.944,-13.056));
#92808=CARTESIAN_POINT('',(-29.784,7.944,-10.1274561623021));
#92809=CARTESIAN_POINT('Origin',(-29.184,7.944,-10.1274561623021));
#92810=CARTESIAN_POINT('',(-29.784,7.944,-13.272));
#92811=CARTESIAN_POINT('',(-29.784,7.944,-13.056));
#92812=CARTESIAN_POINT('Origin',(-29.184,7.944,-13.272));
#92813=CARTESIAN_POINT('Origin',(-29.184,7.944,9.792));
#92814=CARTESIAN_POINT('',(-29.7835166971462,7.91992242032593,9.38872242032602));
#92815=CARTESIAN_POINT('Origin',(-29.184,7.944,9.4128));
#92816=CARTESIAN_POINT('',(-29.784,7.944,9.31145616230212));
#92817=CARTESIAN_POINT('Origin',(-29.184,7.944,9.31145616230212));
#92818=CARTESIAN_POINT('',(-29.784,7.944,8.35664978309472));
#92819=CARTESIAN_POINT('',(-29.784,7.944,-13.056));
#92820=CARTESIAN_POINT('',(-29.7737557460509,7.83359999999999,8.5165882446332));
#92821=CARTESIAN_POINT('Origin',(-29.184,7.944,8.35664978309472));
#92822=CARTESIAN_POINT('',(-29.7737557460509,7.83359999999999,-9.3325882446332));
#92823=CARTESIAN_POINT('',(-29.7737557460508,7.83359999999999,-13.056));
#92824=CARTESIAN_POINT('',(-29.784,7.944,-9.17264978309472));
#92825=CARTESIAN_POINT('Origin',(-29.184,7.944,-9.17264978309472));
#92826=CARTESIAN_POINT('',(-29.784,7.944,-13.056));
#92827=CARTESIAN_POINT('Origin',(-29.784,7.344,-13.872));
#92828=CARTESIAN_POINT('',(-29.784,21.432,-13.272));
#92829=CARTESIAN_POINT('',(-29.784,21.432,-11.016));
#92830=CARTESIAN_POINT('',(-29.784,7.344,-13.272));
#92831=CARTESIAN_POINT('Origin',(-29.784,7.344,-13.872));
#92832=CARTESIAN_POINT('',(-29.784,21.432,-10.1274561623021));
#92833=CARTESIAN_POINT('',(-29.784,14.7229948614198,-0.408000000000001));
#92834=CARTESIAN_POINT('',(-29.784,19.7444202838503,-7.68262913762374));
#92835=CARTESIAN_POINT('',(-29.784,15.052529806456,0.0694031896036967));
#92836=CARTESIAN_POINT('',(-29.784,10.6144737596866,-6.36008826276735));
#92837=CARTESIAN_POINT('',(-29.784,21.432,-9.17264978309473));
#92838=CARTESIAN_POINT('',(-29.784,17.2323832698161,-3.08858964834107));
#92839=CARTESIAN_POINT('',(-29.784,21.432,-11.016));
#92840=CARTESIAN_POINT('Origin',(-29.784,7.344,-13.872));
#92841=CARTESIAN_POINT('',(-29.784,12.4742196642688,-3.56444562304089));
#92842=CARTESIAN_POINT('',(-29.784,10.0969852123603,-7.00838784183138));
#92843=CARTESIAN_POINT('',(-29.784,11.0112188528984,-4.72911477825469));
#92844=CARTESIAN_POINT('',(-29.784,6.93828697788673,-10.6296442894896));
#92845=CARTESIAN_POINT('',(-29.784,12.1405883340853,-3.64430626388261));
#92846=CARTESIAN_POINT('Origin',(-29.784,10.6896,-3.264));
#92847=CARTESIAN_POINT('Origin',(-29.784,12.1735582741579,-3.0452127961736));
#92848=CARTESIAN_POINT('Origin',(-29.184,10.0969852123603,-7.00838784183138));
#92849=CARTESIAN_POINT('',(-29.784,14.6530051385802,-0.408000000000001));
#92850=CARTESIAN_POINT('',(-29.7833084014095,14.688,-0.407999999999989));
#92851=CARTESIAN_POINT('Origin',(-29.184,14.6530051385802,-0.408000000000002));
#92852=CARTESIAN_POINT('',(-29.184,14.688,-1.41350406305912));
#92853=CARTESIAN_POINT('Origin',(-29.184,14.688,-0.357302316148279));
#92854=CARTESIAN_POINT('',(-29.184,10.5907719941602,-7.34923181510914));
#92855=CARTESIAN_POINT('',(-29.7833084014095,12.6436432904313,-3.369696258734));
#92856=CARTESIAN_POINT('Ctrl Pts',(-29.784,12.4742196642688,-3.56444562304089));
#92857=CARTESIAN_POINT('Ctrl Pts',(-29.784,12.4770960656062,-3.56178870707269));
#92858=CARTESIAN_POINT('Ctrl Pts',(-29.7839981607211,12.4799597304405,-3.55911809821074));
#92859=CARTESIAN_POINT('Ctrl Pts',(-29.7839947131496,12.4828105409336,-3.55643374451523));
#92860=CARTESIAN_POINT('Ctrl Pts',(-29.7839651892816,12.5072239441763,-3.53344582252835));
#92861=CARTESIAN_POINT('Ctrl Pts',(-29.7838218910197,12.5306539102921,-3.50948777896365));
#92862=CARTESIAN_POINT('Ctrl Pts',(-29.783683917326,12.5530399267613,-3.48453639277156));
#92863=CARTESIAN_POINT('Ctrl Pts',(-29.7836552812666,12.5576860827128,-3.47935780141234));
#92864=CARTESIAN_POINT('Ctrl Pts',(-29.7836266970853,12.562287284019,-3.47413643089436));
#92865=CARTESIAN_POINT('Ctrl Pts',(-29.7835989418307,12.5668430063734,-3.46887208513704));
#92866=CARTESIAN_POINT('Ctrl Pts',(-29.7834716813667,12.5877314237255,-3.44473456254201));
#92867=CARTESIAN_POINT('Ctrl Pts',(-29.7833664628523,12.60758001705,-3.41979037882897));
#92868=CARTESIAN_POINT('Ctrl Pts',(-29.7833269962461,12.6263747771475,-3.39402765987634));
#92869=CARTESIAN_POINT('Ctrl Pts',(-29.7833146936516,12.6322335102483,-3.38599686333995));
#92870=CARTESIAN_POINT('Ctrl Pts',(-29.7833084014095,12.6379898333541,-3.37788652347427));
#92871=CARTESIAN_POINT('Ctrl Pts',(-29.7833084014095,12.6436432904314,-3.36969625873406));
#92872=CARTESIAN_POINT('',(-29.7833084014095,14.3409676242539,-0.910752031529554));
#92873=CARTESIAN_POINT('',(-29.7833084014095,10.1206869778867,-7.02474835254872));
#92874=CARTESIAN_POINT('',(-29.784,14.323470193544,-0.885403189603699));
#92875=CARTESIAN_POINT('Origin',(-29.184,14.323470193544,-0.885403189603698));
#92876=CARTESIAN_POINT('',(-29.784,10.0969852123603,-7.00838784183138));
#92877=CARTESIAN_POINT('Origin',(-29.184,10.6144737596866,-6.36008826276735));
#92878=CARTESIAN_POINT('Origin',(-29.184,14.7229948614198,-0.408000000000003));
#92879=CARTESIAN_POINT('',(-29.184,14.688,0.59750406305912));
#92880=CARTESIAN_POINT('Origin',(-29.184,14.688,-0.458697683851722));
#92881=CARTESIAN_POINT('',(-29.184,10.1206869778867,-6.01924428948959));
#92882=CARTESIAN_POINT('',(-29.7833084014095,15.0350323757461,0.0947520315295554));
#92883=CARTESIAN_POINT('',(-29.7833084014095,10.5907719941602,-6.34372775205002));
#92884=CARTESIAN_POINT('Origin',(-29.184,15.052529806456,0.0694031896036995));
#92885=CARTESIAN_POINT('Origin',(-29.184,13.5561964880162,1.18096637838117));
#92886=CARTESIAN_POINT('',(-29.784,13.5561964880162,1.18096637838117));
#92887=CARTESIAN_POINT('',(-29.184,9.01726475149214,8.8128));
#92888=CARTESIAN_POINT('Origin',(-29.184,7.87404584654483,9.4128));
#92889=CARTESIAN_POINT('',(-29.184,14.0499832698161,1.52181035165893));
#92890=CARTESIAN_POINT('Origin',(-29.784,7.344,-13.872));
#92891=CARTESIAN_POINT('',(-29.784,16.0682335020505,-3.41307311090149));
#92892=CARTESIAN_POINT('Origin',(-29.784,13.9939352485079,-0.408));
#92893=CARTESIAN_POINT('',(-29.184,13.9939352485079,-0.408));
#92894=CARTESIAN_POINT('Origin',(-29.184,14.3584650549638,-0.936100873455419));
#92895=CARTESIAN_POINT('',(-28.968,13.9939352485079,-0.408));
#92896=CARTESIAN_POINT('',(-29.784,13.9939352485079,-0.408));
#92897=CARTESIAN_POINT('',(-28.968,8.3232,7.80729593694088));
#92898=CARTESIAN_POINT('',(-28.968,13.9939352485079,-0.408));
#92899=CARTESIAN_POINT('',(-29.184,8.3232,7.80729593694088));
#92900=CARTESIAN_POINT('',(-29.784,8.3232,7.80729593694088));
#92901=CARTESIAN_POINT('Origin',(-29.184,7.7232,8.67652670617165));
#92902=CARTESIAN_POINT('Origin',(-29.184,7.43207375968655,-10.9704882627674));
#92903=CARTESIAN_POINT('',(-29.1857320434525,12.1735590034295,-3.04521774270319));
#92904=CARTESIAN_POINT('Origin',(-29.184,12.6673450559578,-3.38605676945136));
#92905=CARTESIAN_POINT('',(-29.184,6.93828697788673,-10.6296442894896));
#92906=CARTESIAN_POINT('Origin',(-29.784,15.3820647514921,-0.408));
#92907=CARTESIAN_POINT('',(-29.184,15.3820647514921,-0.408));
#92908=CARTESIAN_POINT('Origin',(-29.184,15.0175349450362,0.120100873455421));
#92909=CARTESIAN_POINT('',(-28.968,15.3820647514921,-0.408));
#92910=CARTESIAN_POINT('',(-29.784,15.3820647514921,-0.408));
#92911=CARTESIAN_POINT('',(-28.968,21.0528,-8.62329593694088));
#92912=CARTESIAN_POINT('',(-28.968,15.3820647514921,-0.408));
#92913=CARTESIAN_POINT('',(-29.184,21.0528,-8.62329593694088));
#92914=CARTESIAN_POINT('',(-29.784,21.0528,-8.62329593694088));
#92915=CARTESIAN_POINT('',(-29.7737557460508,21.5424,-9.3325882446332));
#92916=CARTESIAN_POINT('Origin',(-29.184,21.6528,-9.49252670617165));
#92917=CARTESIAN_POINT('Origin',(-29.184,21.432,-9.17264978309473));
#92918=CARTESIAN_POINT('Origin',(-29.184,13.2793852123603,-2.39798784183138));
#92919=CARTESIAN_POINT('',(-29.184,13.7731719941602,-2.73883181510914));
#92920=CARTESIAN_POINT('Origin',(-4.08,21.432,-13.272));
#92921=CARTESIAN_POINT('Origin',(-29.184,21.432,-13.272));
#92922=CARTESIAN_POINT('Origin',(-29.184,7.344,-13.272));
#92923=CARTESIAN_POINT('Origin',(-29.184,7.944,-13.272));
#92924=CARTESIAN_POINT('Origin',(-29.184,21.432,-13.272));
#92925=CARTESIAN_POINT('Origin',(-29.184,21.432,-13.272));
#92926=CARTESIAN_POINT('Origin',(-29.184,21.432,-13.272));
#92927=CARTESIAN_POINT('Origin',(-29.184,7.944,-13.272));
#92928=CARTESIAN_POINT('Origin',(-29.184,21.432,-11.016));
#92929=CARTESIAN_POINT('Origin',(-29.184,21.432,9.4128));
#92930=CARTESIAN_POINT('Origin',(-29.184,21.432,9.792));
#92931=CARTESIAN_POINT('Origin',(-29.184,21.432,-10.1274561623021));
#92932=CARTESIAN_POINT('',(-29.7737557460508,21.5424,5.93725687477551));
#92933=CARTESIAN_POINT('',(-29.7737557460508,21.5424,-11.016));
#92934=CARTESIAN_POINT('Ctrl Pts',(-29.7737557460509,21.5424,5.93725687477551));
#92935=CARTESIAN_POINT('Ctrl Pts',(-29.7737557460509,21.5424,5.96670869882893));
#92936=CARTESIAN_POINT('Ctrl Pts',(-29.7740088989078,21.5410717904559,5.9960597320568));
#92937=CARTESIAN_POINT('Ctrl Pts',(-29.7744834610748,21.5384391008847,6.02533043536184));
#92938=CARTESIAN_POINT('Ctrl Pts',(-29.7746717989984,21.5373942740489,6.03694700293919));
#92939=CARTESIAN_POINT('Ctrl Pts',(-29.7748944336911,21.5361438842468,6.04855091829811));
#92940=CARTESIAN_POINT('Ctrl Pts',(-29.7751471540983,21.534689055899,6.06014346040397));
#92941=CARTESIAN_POINT('Ctrl Pts',(-29.775853643425,21.5306220289779,6.09255084434131));
#92942=CARTESIAN_POINT('Ctrl Pts',(-29.7767945331539,21.5249853227474,6.12464572125983));
#92943=CARTESIAN_POINT('Ctrl Pts',(-29.7778229194578,21.5178739793336,6.15641892625882));
#92944=CARTESIAN_POINT('Ctrl Pts',(-29.7785157033164,21.5130833438392,6.17782329879137));
#92945=CARTESIAN_POINT('Ctrl Pts',(-29.7792468574529,21.5076233361447,6.19908169040163));
#92946=CARTESIAN_POINT('Ctrl Pts',(-29.7799584187364,21.5015238314338,6.22019129919245));
#92947=CARTESIAN_POINT('Ctrl Pts',(-29.7811964208663,21.4909116747602,6.25691862156105));
#92948=CARTESIAN_POINT('Ctrl Pts',(-29.7823703798565,21.4784143085855,6.29303346610638));
#92949=CARTESIAN_POINT('Ctrl Pts',(-29.7831330157742,21.4642432847158,6.32849767780225));
#92950=CARTESIAN_POINT('Ctrl Pts',(-29.7836200003229,21.4551943145547,6.35114350751594));
#92951=CARTESIAN_POINT('Ctrl Pts',(-29.7839381728052,21.4454635235311,6.37352404053474));
#92952=CARTESIAN_POINT('Ctrl Pts',(-29.7839919096164,21.4351158297269,6.39562934236959));
#92953=CARTESIAN_POINT('Ctrl Pts',(-29.7839972715979,21.4340833132552,6.397835059768));
#92954=CARTESIAN_POINT('Ctrl Pts',(-29.784,21.433044682114,6.40003791857));
#92955=CARTESIAN_POINT('Ctrl Pts',(-29.784,21.432,6.4022379066467));
#92956=CARTESIAN_POINT('Origin',(-27.528,7.344,9.192));
#92957=CARTESIAN_POINT('',(-27.528,7.344,9.792));
#92958=CARTESIAN_POINT('Origin',(-29.784,7.344,9.792));
#92959=CARTESIAN_POINT('Origin',(27.528,10.6896,-3.264));
#92960=CARTESIAN_POINT('Origin',(27.528,10.6896,-1.164));
#92961=CARTESIAN_POINT('Origin',(28.368,10.6896,-3.264));
#92962=CARTESIAN_POINT('',(28.968,12.609642670068,-2.4134495046629));
#92963=CARTESIAN_POINT('Ctrl Pts',(28.968,12.609642670068,-2.41344950466293));
#92964=CARTESIAN_POINT('Ctrl Pts',(28.968,12.5563563145717,-2.49064640429212));
#92965=CARTESIAN_POINT('Ctrl Pts',(28.9480231288294,12.4934277609683,-2.58181212938432));
#92966=CARTESIAN_POINT('Ctrl Pts',(28.8849632069594,12.3934003848311,-2.72672358455736));
#92967=CARTESIAN_POINT('Ctrl Pts',(28.8306825733401,12.3378273727896,-2.80723320456632));
#92968=CARTESIAN_POINT('Ctrl Pts',(28.719257430577,12.2610925274537,-2.91840035229654));
#92969=CARTESIAN_POINT('Ctrl Pts',(28.6451394651737,12.2244553812516,-2.97147724358932));
#92970=CARTESIAN_POINT('Ctrl Pts',(28.5128362786337,12.1855396693978,-3.02785513383895));
#92971=CARTESIAN_POINT('Ctrl Pts',(28.4351123331488,12.173558274158,-3.04521279617364));
#92972=CARTESIAN_POINT('Ctrl Pts',(28.368,12.173558274158,-3.04521279617364));
#92973=CARTESIAN_POINT('',(28.968,10.5751344569884,-5.3608780697654));
#92974=CARTESIAN_POINT('Origin',(28.968,10.6896,-3.264));
#92975=CARTESIAN_POINT('Ctrl Pts',(28.368,11.0112188528985,-4.72911477825469));
#92976=CARTESIAN_POINT('Ctrl Pts',(28.4351123331488,11.0112188528985,-4.72911477825469));
#92977=CARTESIAN_POINT('Ctrl Pts',(28.5128362786337,10.9992374576586,-4.74647244058937));
#92978=CARTESIAN_POINT('Ctrl Pts',(28.6451394651737,10.9603217458049,-4.802850330839));
#92979=CARTESIAN_POINT('Ctrl Pts',(28.719257430577,10.9236845996028,-4.85592722213179));
#92980=CARTESIAN_POINT('Ctrl Pts',(28.8306825733401,10.8469497542669,-4.967094369862));
#92981=CARTESIAN_POINT('Ctrl Pts',(28.8849632069594,10.7913767422253,-5.04760398987096));
#92982=CARTESIAN_POINT('Ctrl Pts',(28.9480231288294,10.6913493660881,-5.19251544504401));
#92983=CARTESIAN_POINT('Ctrl Pts',(28.968,10.6284208124847,-5.28368117013621));
#92984=CARTESIAN_POINT('Ctrl Pts',(28.968,10.5751344569884,-5.3608780697654));
#92985=CARTESIAN_POINT('Origin',(28.968,11.1585676242539,-0.408000000000002));
#92986=CARTESIAN_POINT('',(28.968,8.3232,-8.62329593694088));
#92987=CARTESIAN_POINT('',(28.968,8.3232,-8.62329593694088));
#92988=CARTESIAN_POINT('',(28.968,8.3232,7.80729593694088));
#92989=CARTESIAN_POINT('',(28.968,8.3232,-8.62329593694088));
#92990=CARTESIAN_POINT('Origin',(29.784,8.3232,-8.62329593694088));
#92991=CARTESIAN_POINT('',(29.784,8.3232,-8.62329593694088));
#92992=CARTESIAN_POINT('Origin',(29.784,13.9939352485079,-0.407999999999999));
#92993=CARTESIAN_POINT('Origin',(29.784,13.9939352485079,-0.407999999999999));
#92994=CARTESIAN_POINT('Ctrl Pts',(-29.784,21.2011648366643,6.51862412122269));
#92995=CARTESIAN_POINT('Ctrl Pts',(-29.784,21.6528,6.40336689328349));
#92996=CARTESIAN_POINT('Ctrl Pts',(-29.784,21.6528,5.93725687477551));
#92997=CARTESIAN_POINT('Ctrl Pts',(-29.784,21.0528,5.93725687477551));
#92998=CARTESIAN_POINT('Ctrl Pts',(-29.784,21.0528,5.93725687477551));
#92999=CARTESIAN_POINT('Ctrl Pts',(-29.784,21.0528,5.93725687477551));
#93000=CARTESIAN_POINT('Ctrl Pts',(-29.184,21.0528,5.93725687477551));
#93001=CARTESIAN_POINT('Ctrl Pts',(-29.184,21.0528,5.93725687477551));
#93002=CARTESIAN_POINT('Ctrl Pts',(-29.184,21.0528,5.93725687477551));
#93003=CARTESIAN_POINT('Origin',(-29.184,21.6528,5.93725687477551));
#93004=CARTESIAN_POINT('Origin',(-29.184,21.6528,-11.2476479684704));
#93005=CARTESIAN_POINT('',(-29.184,21.0528,-11.2476479684704));
#93006=CARTESIAN_POINT('Origin',(-29.784,8.3232,-8.62329593694088));
#93007=CARTESIAN_POINT('',(-29.184,8.3232,-8.62329593694088));
#93008=CARTESIAN_POINT('Origin',(-29.184,7.7232,-9.49252670617165));
#93009=CARTESIAN_POINT('',(-28.968,8.3232,-8.62329593694088));
#93010=CARTESIAN_POINT('',(-29.784,8.3232,-8.62329593694088));
#93011=CARTESIAN_POINT('',(-28.968,10.5751344569884,-5.3608780697654));
#93012=CARTESIAN_POINT('',(-28.968,8.3232,-8.62329593694088));
#93013=CARTESIAN_POINT('',(-28.368,11.0112188528984,-4.72911477825469));
#93014=CARTESIAN_POINT('Ctrl Pts',(-28.968,10.5751344569884,-5.3608780697654));
#93015=CARTESIAN_POINT('Ctrl Pts',(-28.968,10.6284208124846,-5.28368117013621));
#93016=CARTESIAN_POINT('Ctrl Pts',(-28.9480231288294,10.6913493660881,-5.192515445044));
#93017=CARTESIAN_POINT('Ctrl Pts',(-28.8849632069594,10.7913767422253,-5.04760398987097));
#93018=CARTESIAN_POINT('Ctrl Pts',(-28.8306825733401,10.8469497542668,-4.96709436986201));
#93019=CARTESIAN_POINT('Ctrl Pts',(-28.719257430577,10.9236845996027,-4.85592722213179));
#93020=CARTESIAN_POINT('Ctrl Pts',(-28.6451394651737,10.9603217458048,-4.80285033083901));
#93021=CARTESIAN_POINT('Ctrl Pts',(-28.5128362786337,10.9992374576586,-4.74647244058938));
#93022=CARTESIAN_POINT('Ctrl Pts',(-28.4351123331488,11.0112188528984,-4.72911477825469));
#93023=CARTESIAN_POINT('Ctrl Pts',(-28.368,11.0112188528984,-4.72911477825469));
#93024=CARTESIAN_POINT('',(-13.464,11.0112188528984,-4.72911477825469));
#93025=CARTESIAN_POINT('Origin',(-29.184,7.7232,-3.03235203152956));
#93026=CARTESIAN_POINT('',(-29.184,8.3232,-3.03235203152956));
#93027=CARTESIAN_POINT('Origin',(-29.784,9.01726475149214,8.8128));
#93028=CARTESIAN_POINT('',(-28.968,9.01726475149214,8.8128));
#93029=CARTESIAN_POINT('',(-29.784,9.01726475149214,8.8128));
#93030=CARTESIAN_POINT('',(-28.968,14.688,0.59750406305912));
#93031=CARTESIAN_POINT('',(-28.968,9.01726475149214,8.8128));
#93032=CARTESIAN_POINT('',(-29.784,14.688,0.59750406305912));
#93033=CARTESIAN_POINT('Origin',(-29.184,13.8513676242539,9.4128));
#93034=CARTESIAN_POINT('',(-29.184,13.8513676242539,8.8128));
#93035=CARTESIAN_POINT('Origin',(-29.784,20.3587352485079,8.8128));
#93036=CARTESIAN_POINT('',(-28.968,20.3587352485079,8.8128));
#93037=CARTESIAN_POINT('Origin',(-29.184,19.7444202838503,-7.68262913762374));
#93038=CARTESIAN_POINT('',(-29.184,19.2506335020505,-8.02347311090149));
#93039=CARTESIAN_POINT('Origin',(-29.784,20.3587352485079,-9.6288));
#93040=CARTESIAN_POINT('',(-28.968,20.3587352485079,-9.6288));
#93041=CARTESIAN_POINT('',(-29.784,20.3587352485079,-9.6288));
#93042=CARTESIAN_POINT('',(-28.968,14.688,-1.41350406305912));
#93043=CARTESIAN_POINT('',(-28.968,20.3587352485079,-9.6288));
#93044=CARTESIAN_POINT('',(-29.784,14.688,-1.41350406305912));
#93045=CARTESIAN_POINT('Origin',(-29.784,21.0528,-8.62329593694088));
#93046=CARTESIAN_POINT('',(-28.968,21.0528,-8.62329593694088));
#93047=CARTESIAN_POINT('Origin',(-27.528,10.6896,-3.264));
#93048=CARTESIAN_POINT('',(-27.528,10.6896,-4.764));
#93049=CARTESIAN_POINT('Origin',(-27.528,10.6896,-5.364));
#93050=CARTESIAN_POINT('',(-27.528,10.6896,-1.764));
#93051=CARTESIAN_POINT('Origin',(-27.528,10.6896,-3.264));
#93052=CARTESIAN_POINT('Origin',(-27.528,10.6896,-3.264));
#93053=CARTESIAN_POINT('Origin',(-13.464,10.6896,-3.264));
#93054=CARTESIAN_POINT('',(-28.368,10.6896,-1.764));
#93055=CARTESIAN_POINT('',(-13.464,10.6896,-1.764));
#93056=CARTESIAN_POINT('',(-28.368,12.1735582741579,-3.0452127961736));
#93057=CARTESIAN_POINT('Origin',(-28.368,10.6896,-3.264));
#93058=CARTESIAN_POINT('',(-13.464,12.1735582741579,-3.0452127961736));
#93059=CARTESIAN_POINT('Ctrl Pts',(-29.784,12.1405883340853,-3.64430626388261));
#93060=CARTESIAN_POINT('Ctrl Pts',(-29.784,12.147511185521,-3.6178934023925));
#93061=CARTESIAN_POINT('Ctrl Pts',(-29.7822104609222,12.1536772931533,-3.59140178696739));
#93062=CARTESIAN_POINT('Ctrl Pts',(-29.7786474905659,12.1590759523918,-3.56504634540795));
#93063=CARTESIAN_POINT('Ctrl Pts',(-29.7748844514047,12.1647777584978,-3.53721098648425));
#93064=CARTESIAN_POINT('Ctrl Pts',(-29.7691451014835,12.1696236218268,-3.50952645920431));
#93065=CARTESIAN_POINT('Ctrl Pts',(-29.7614332365283,12.1736419782786,-3.48220709085635));
#93066=CARTESIAN_POINT('Ctrl Pts',(-29.7564653648374,12.1762305452953,-3.46460834951199));
#93067=CARTESIAN_POINT('Ctrl Pts',(-29.7506784545669,12.1784765265179,-3.44716030561529));
#93068=CARTESIAN_POINT('Ctrl Pts',(-29.7440660203898,12.1803955912691,-3.42991716322555));
#93069=CARTESIAN_POINT('Ctrl Pts',(-29.7333900045645,12.1834939912084,-3.40207748178614));
#93070=CARTESIAN_POINT('Ctrl Pts',(-29.7206781216082,12.185706516543,-3.37507844369262));
#93071=CARTESIAN_POINT('Ctrl Pts',(-29.7060488214569,12.1871803802583,-3.34916282903413));
#93072=CARTESIAN_POINT('Ctrl Pts',(-29.6880947954994,12.1889892013999,-3.31735750591742));
#93073=CARTESIAN_POINT('Ctrl Pts',(-29.6672533785123,12.1896851014655,-3.28718063548158));
#93074=CARTESIAN_POINT('Ctrl Pts',(-29.6437054196481,12.1895918142645,-3.2590338036487));
#93075=CARTESIAN_POINT('Ctrl Pts',(-29.6391149556756,12.189573628759,-3.25354683052235));
#93076=CARTESIAN_POINT('Ctrl Pts',(-29.634421550843,12.1895255901819,-3.24813699762495));
#93077=CARTESIAN_POINT('Ctrl Pts',(-29.629626466634,12.1894502829085,-3.24280733949571));
#93078=CARTESIAN_POINT('Ctrl Pts',(-29.6034219992866,12.189038739148,-3.21368150012913));
#93079=CARTESIAN_POINT('Ctrl Pts',(-29.5745073160778,12.1878210298843,-3.18731184548696));
#93080=CARTESIAN_POINT('Ctrl Pts',(-29.5432973065778,12.1862640863858,-3.16400903809615));
#93081=CARTESIAN_POINT('Ctrl Pts',(-29.5172821877694,12.1849662953649,-3.14458497150485));
#93082=CARTESIAN_POINT('Ctrl Pts',(-29.4896684020062,12.1834330785157,-3.12728965954881));
#93083=CARTESIAN_POINT('Ctrl Pts',(-29.4607047388456,12.1819102823203,-3.1123093189926));
#93084=CARTESIAN_POINT('Ctrl Pts',(-29.4570107007678,12.1817160642375,-3.11039871990417));
#93085=CARTESIAN_POINT('Ctrl Pts',(-29.4532947581774,12.181521974349,-3.10852580118053));
#93086=CARTESIAN_POINT('Ctrl Pts',(-29.449557483041,12.1813284837015,-3.1066909700191));
#93087=CARTESIAN_POINT('Ctrl Pts',(-29.4234055951258,12.1799745170972,-3.09385158915324));
#93088=CARTESIAN_POINT('Ctrl Pts',(-29.3964447704895,12.1786654665046,-3.08299045789682));
#93089=CARTESIAN_POINT('Ctrl Pts',(-29.3688630741448,12.1775347113506,-3.07412927688624));
#93090=CARTESIAN_POINT('Ctrl Pts',(-29.342732972425,12.1764634666083,-3.06573445017687));
#93091=CARTESIAN_POINT('Ctrl Pts',(-29.3160437828719,12.1755521928172,-3.0591353667864));
#93092=CARTESIAN_POINT('Ctrl Pts',(-29.2889754148028,12.1748799314263,-3.05437250687602));
#93093=CARTESIAN_POINT('Ctrl Pts',(-29.2636838866422,12.174251799067,-3.04992229379924));
#93094=CARTESIAN_POINT('Ctrl Pts',(-29.2380607642433,12.1738323335988,-3.04707636428828));
#93095=CARTESIAN_POINT('Ctrl Pts',(-29.2122867480549,12.173655437531,-3.04587283722916));
#93096=CARTESIAN_POINT('Ctrl Pts',(-29.2043276450809,12.1736008114297,-3.04550118402132));
#93097=CARTESIAN_POINT('Ctrl Pts',(-29.1963544354037,12.1735690833018,-3.04528611569323));
#93098=CARTESIAN_POINT('Ctrl Pts',(-29.1883732215644,12.1735605987272,-3.04522856350714));
#93099=CARTESIAN_POINT('Ctrl Pts',(-29.1880701860807,12.1735602765798,-3.04522637833144));
#93100=CARTESIAN_POINT('Ctrl Pts',(-29.1877671376288,12.1735599878973,-3.04522442020813));
#93101=CARTESIAN_POINT('Ctrl Pts',(-29.187464086905,12.1735597327011,-3.04522268923278));
#93102=CARTESIAN_POINT('Origin',(-28.368,10.6896,-3.264));
#93103=CARTESIAN_POINT('Origin',(-29.784,8.3232,7.80729593694088));
#93104=CARTESIAN_POINT('',(-28.968,8.3232,7.80729593694088));
#93105=CARTESIAN_POINT('Ctrl Pts',(-29.784,12.6673450559584,-3.38605676945045));
#93106=CARTESIAN_POINT('Ctrl Pts',(-29.784,12.4763303711457,-3.66278317180831));
#93107=CARTESIAN_POINT('Ctrl Pts',(-29.784,12.1405883340853,-3.64430626388262));
#93108=CARTESIAN_POINT('Ctrl Pts',(-29.784,12.1735582741579,-3.04521279617361));
#93109=CARTESIAN_POINT('Ctrl Pts',(-29.784,12.1735582741579,-3.04521279617361));
#93110=CARTESIAN_POINT('Ctrl Pts',(-29.784,12.1735582741579,-3.04521279617361));
#93111=CARTESIAN_POINT('Ctrl Pts',(-29.184,12.1735582741579,-3.0452127961736));
#93112=CARTESIAN_POINT('Ctrl Pts',(-29.184,12.1735582741579,-3.04521279617361));
#93113=CARTESIAN_POINT('Ctrl Pts',(-29.184,12.1735582741579,-3.04521279617361));
#93114=CARTESIAN_POINT('Origin',(-28.368,10.6896,-3.264));
#93115=CARTESIAN_POINT('',(-28.968,12.609642670068,-2.4134495046629));
#93116=CARTESIAN_POINT('Origin',(-28.968,10.6896,-3.264));
#93117=CARTESIAN_POINT('Ctrl Pts',(-28.368,12.1735582741579,-3.0452127961736));
#93118=CARTESIAN_POINT('Ctrl Pts',(-28.4351123331488,12.1735582741579,-3.0452127961736));
#93119=CARTESIAN_POINT('Ctrl Pts',(-28.5128362786337,12.1855396693978,-3.02785513383891));
#93120=CARTESIAN_POINT('Ctrl Pts',(-28.6451394651737,12.2244553812515,-2.97147724358928));
#93121=CARTESIAN_POINT('Ctrl Pts',(-28.719257430577,12.2610925274536,-2.9184003522965));
#93122=CARTESIAN_POINT('Ctrl Pts',(-28.8306825733401,12.3378273727895,-2.80723320456628));
#93123=CARTESIAN_POINT('Ctrl Pts',(-28.8849632069594,12.3934003848311,-2.72672358455733));
#93124=CARTESIAN_POINT('Ctrl Pts',(-28.9480231288294,12.4934277609683,-2.58181212938429));
#93125=CARTESIAN_POINT('Ctrl Pts',(-28.968,12.5563563145717,-2.49064640429208));
#93126=CARTESIAN_POINT('Ctrl Pts',(-28.968,12.609642670068,-2.4134495046629));
#93127=CARTESIAN_POINT('Origin',(-28.968,11.1585676242539,-0.408000000000002));
#93128=CARTESIAN_POINT('',(-28.968,8.3232,-8.62329593694088));
#93129=CARTESIAN_POINT('Origin',(-29.784,8.3232,-8.62329593694088));
#93130=CARTESIAN_POINT('Origin',(-28.968,18.2174323757461,-0.407999999999999));
#93131=CARTESIAN_POINT('',(-28.968,21.0528,7.80729593694088));
#93132=CARTESIAN_POINT('Origin',(-29.784,21.0528,7.80729593694088));
#93133=CARTESIAN_POINT('Origin',(-29.784,21.0528,-8.62329593694088));
#93134=CARTESIAN_POINT('',(-28.968,21.0528,7.80729593694088));
#93135=CARTESIAN_POINT('',(-28.968,21.0528,-8.62329593694088));
#93136=CARTESIAN_POINT('',(-29.784,21.0528,7.80729593694088));
#93137=CARTESIAN_POINT('Origin',(-29.784,21.0528,7.80729593694088));
#93138=CARTESIAN_POINT('',(-28.968,21.0528,7.80729593694088));
#93139=CARTESIAN_POINT('Origin',(-28.968,18.2174323757461,-0.407999999999999));
#93140=CARTESIAN_POINT('Origin',(-29.784,14.688,0.59750406305912));
#93141=CARTESIAN_POINT('',(-28.968,14.688,0.59750406305912));
#93142=CARTESIAN_POINT('Origin',(-28.968,14.688,4.70515203152956));
#93143=CARTESIAN_POINT('Origin',(-29.784,9.01726475149214,-9.6288));
#93144=CARTESIAN_POINT('',(-28.968,9.01726475149214,-9.6288));
#93145=CARTESIAN_POINT('',(-29.784,9.01726475149214,-9.6288));
#93146=CARTESIAN_POINT('',(-28.968,9.01726475149214,-9.6288));
#93147=CARTESIAN_POINT('Origin',(-29.784,14.688,-1.41350406305912));
#93148=CARTESIAN_POINT('',(-28.968,14.688,-1.41350406305912));
#93149=CARTESIAN_POINT('Origin',(-28.968,14.688,-5.52115203152956));
#93150=CARTESIAN_POINT('Origin',(28.968,18.2174323757461,-0.407999999999999));
#93151=CARTESIAN_POINT('',(28.968,21.0528,-8.62329593694088));
#93152=CARTESIAN_POINT('Origin',(29.784,21.0528,7.80729593694088));
#93153=CARTESIAN_POINT('Origin',(29.784,15.3820647514921,-0.407999999999999));
#93154=CARTESIAN_POINT('',(28.968,21.0528,7.80729593694088));
#93155=CARTESIAN_POINT('',(28.968,21.0528,7.80729593694088));
#93156=CARTESIAN_POINT('',(29.784,21.0528,7.80729593694088));
#93157=CARTESIAN_POINT('Origin',(29.784,21.0528,7.80729593694088));
#93158=CARTESIAN_POINT('',(28.968,21.0528,-8.62329593694088));
#93159=CARTESIAN_POINT('Origin',(28.968,18.2174323757461,-0.407999999999999));
#93160=CARTESIAN_POINT('Origin',(29.784,20.3587352485079,8.8128));
#93161=CARTESIAN_POINT('',(28.968,20.3587352485079,8.8128));
#93162=CARTESIAN_POINT('',(29.784,20.3587352485079,8.8128));
#93163=CARTESIAN_POINT('',(28.968,14.688,0.59750406305912));
#93164=CARTESIAN_POINT('Origin',(29.784,9.01726475149214,8.8128));
#93165=CARTESIAN_POINT('',(28.968,20.3587352485079,8.8128));
#93166=CARTESIAN_POINT('Origin',(29.784,20.3587352485079,8.8128));
#93167=CARTESIAN_POINT('',(28.968,14.688,0.59750406305912));
#93168=CARTESIAN_POINT('Origin',(28.968,14.688,4.70515203152956));
#93169=CARTESIAN_POINT('Origin',(28.968,14.688,-5.52115203152956));
#93170=CARTESIAN_POINT('Origin',(-4.896,21.7056,-21.216));
#93171=CARTESIAN_POINT('Origin',(0.,20.808,-2.1216));
#93172=CARTESIAN_POINT('Origin',(3.672,20.808,-3.264));
#93173=CARTESIAN_POINT('Origin',(-3.672,20.808,-3.264));
#93174=CARTESIAN_POINT('Origin',(0.,14.688,-22.032));
#93175=CARTESIAN_POINT('',(-5.47389440891949,16.32,-22.032));
#93176=CARTESIAN_POINT('',(5.47389440891949,16.32,-22.032));
#93177=CARTESIAN_POINT('Origin',(0.,14.688,-22.032));
#93178=CARTESIAN_POINT('',(-5.47389440891949,16.32,-22.032));
#93179=CARTESIAN_POINT('',(5.47389440891949,16.32,-22.032));
#93180=CARTESIAN_POINT('Origin',(0.,16.32,-11.832));
#93181=CARTESIAN_POINT('Origin',(0.,16.32,2.448));
#93182=CARTESIAN_POINT('Origin',(0.,16.32,-11.832));
#93183=CARTESIAN_POINT('Origin',(0.,16.32,2.448));
#93184=CARTESIAN_POINT('Origin',(-10.812,16.32,8.16));
#93185=CARTESIAN_POINT('Origin',(8.16,7.344,-13.872));
#93186=CARTESIAN_POINT('Origin',(8.976,8.16,8.976));
#93187=CARTESIAN_POINT('Origin',(16.32,5.712,8.568));
#93188=CARTESIAN_POINT('Origin',(-8.976,8.16,8.976));
#93189=CARTESIAN_POINT('Origin',(8.976,8.16,8.976));
#99999=UNCERTAINTY_MEASURE_WITH_UNIT(LENGTH_MEASURE(0.01),#100032,
'DISTANCE_ACCURACY_VALUE',
'Maximum model space distance between geometric entities at asserted c
onnectivities');
#100011=UNCERTAINTY_MEASURE_WITH_UNIT(LENGTH_MEASURE(0.01),#100032,
'DISTANCE_ACCURACY_VALUE',
'Maximum model space distance between geometric entities at asserted c
onnectivities');
#100019=(
GEOMETRIC_REPRESENTATION_CONTEXT(3)
GLOBAL_UNCERTAINTY_ASSIGNED_CONTEXT((#99999))
GLOBAL_UNIT_ASSIGNED_CONTEXT((#100032,#100034,#100035))
REPRESENTATION_CONTEXT('','3D')
);
#100031=(
GEOMETRIC_REPRESENTATION_CONTEXT(3)
GLOBAL_UNCERTAINTY_ASSIGNED_CONTEXT((#100011))
GLOBAL_UNIT_ASSIGNED_CONTEXT((#100032,#100034,#100035))
REPRESENTATION_CONTEXT('','3D')
);
#100032=(
LENGTH_UNIT()
NAMED_UNIT(*)
SI_UNIT(.MILLI.,.METRE.)
);
#100034=(
NAMED_UNIT(*)
PLANE_ANGLE_UNIT()
SI_UNIT($,.RADIAN.)
);
#100035=(
NAMED_UNIT(*)
SI_UNIT($,.STERADIAN.)
SOLID_ANGLE_UNIT()
);
#100043=SHAPE_DEFINITION_REPRESENTATION(#100062,#100107);
#100062=PRODUCT_DEFINITION_SHAPE('',$,#100127);
#100107=SHAPE_REPRESENTATION('',(#21611),#100019);
#100119=PRODUCT_DEFINITION_CONTEXT('part definition',#100178,'design');
#100127=PRODUCT_DEFINITION('2026-10-12-11-55-02-014',
'07_Spindle_Nut_Roller_Carriage',#100146,#100119);
#100146=PRODUCT_DEFINITION_FORMATION('',$,#100187);
#100178=APPLICATION_CONTEXT(
'Core Data for Automotive Mechanical Design Process');
#100179=PRODUCT_CONTEXT('part definition',#100178,'mechanical');
#100187=PRODUCT('2026-10-12-11-55-02-014',
'07_Spindle_Nut_Roller_Carriage',$,(#100179));
#100202=PRESENTATION_STYLE_ASSIGNMENT((#100208));
#100208=SURFACE_STYLE_USAGE(.BOTH.,#100214);
#100214=SURFACE_SIDE_STYLE('',(#100220));
#100220=SURFACE_STYLE_FILL_AREA(#100226);
#100226=FILL_AREA_STYLE('Opaque(31,36,43)',(#100232));
#100232=FILL_AREA_STYLE_COLOUR('Opaque(31,36,43)',#100238);
#100238=COLOUR_RGB('Opaque(31,36,43)',0.12156862745098,0.141176470588235,
0.168627450980392);
ENDSEC;
END-ISO-10303-21;
